ISO-10303-21;
HEADER;
/* Generated by software containing ST-Developer
 * from STEP Tools, Inc. (www.steptools.com) 
 */
/* OPTION: using custom renumber hook */

FILE_DESCRIPTION(
/* description */ ('STEP AP242 Edition 2', 'CAx-IF Rec.Pracs.---Representation and Presentation of Product Manufa
cturing Information (PMI)---4.0---2014-10-13', 'CAx-IF Rec.Pracs.---3D Tessellated Geometry---0.4---2014-09-14', '2;1', 'CAx-IF Rec.Pracs.---User Defined Attributes---1.5---2016-08-15'),
/* implementation_level */ '2;1');

FILE_NAME(
/* name */ 'HubBody__ DE       35.step',
/* time_stamp */ '2026-10-09T00:23:50Z',
/* author */ (''),
/* organization */ (''),
/* preprocessor_version */ 'ST-DEVELOPER v20',
/* originating_system */ 'ONSHAPE BY PTC INC, 1.221',
/* authorisation */ '  ');

FILE_SCHEMA (('AP242_MANAGED_MODEL_BASED_3D_ENGINEERING_MIM_LF { 1 0 10303 442 3 1 4 }'));
ENDSEC;

DATA;
#10=(
BOUNDED_SURFACE()
B_SPLINE_SURFACE(3,2,((#16553,#16554,#16555),(#16556,#16557,#16558),(#16559,
#16560,#16561),(#16562,#16563,#16564),(#16565,#16566,#16567),(#16568,#16569,
#16570),(#16571,#16572,#16573),(#16574,#16575,#16576),(#16577,#16578,#16579),
(#16580,#16581,#16582),(#16583,#16584,#16585),(#16586,#16587,#16588),(#16589,
#16590,#16591),(#16592,#16593,#16594),(#16595,#16596,#16597),(#16598,#16599,
#16600),(#16601,#16602,#16603),(#16604,#16605,#16606),(#16607,#16608,#16609),
(#16610,#16611,#16612),(#16613,#16614,#16615),(#16616,#16617,#16618),(#16619,
#16620,#16621),(#16622,#16623,#16624),(#16625,#16626,#16627),(#16628,#16629,
#16630),(#16631,#16632,#16633),(#16634,#16635,#16636),(#16637,#16638,#16639),
(#16640,#16641,#16642),(#16643,#16644,#16645),(#16646,#16647,#16648),(#16649,
#16650,#16651),(#16652,#16653,#16654),(#16655,#16656,#16657),(#16658,#16659,
#16660),(#16661,#16662,#16663),(#16664,#16665,#16666),(#16667,#16668,#16669),
(#16670,#16671,#16672),(#16673,#16674,#16675),(#16676,#16677,#16678),(#16679,
#16680,#16681),(#16682,#16683,#16684),(#16685,#16686,#16687),(#16688,#16689,
#16690),(#16691,#16692,#16693),(#16694,#16695,#16696),(#16697,#16698,#16699),
(#16700,#16701,#16702),(#16703,#16704,#16705),(#16706,#16707,#16708),(#16709,
#16710,#16711),(#16712,#16713,#16714),(#16715,#16716,#16717),(#16718,#16719,
#16720),(#16721,#16722,#16723),(#16724,#16725,#16726),(#16727,#16728,#16729),
(#16730,#16731,#16732),(#16733,#16734,#16735),(#16736,#16737,#16738),(#16739,
#16740,#16741),(#16742,#16743,#16744),(#16745,#16746,#16747),(#16748,#16749,
#16750)),.UNSPECIFIED.,.F.,.F.,.F.)
B_SPLINE_SURFACE_WITH_KNOTS((4,2,2,2,2,2,2,2,2,2,2,2,2,2,2,2,2,2,2,2,2,
2,2,2,2,2,2,2,2,2,2,2,4),(3,3),(0.,0.000514244430931465,0.00102848886186293,
0.0011570499695958,0.00128561107732866,0.00154273329279439,0.00205697772372586,
0.00218553883145873,0.00231409993919159,0.00257122215465732,0.00282834437012306,
0.00295690547785592,0.00308546658558879,0.00359971101652025,0.00372827212425312,
0.00385683323198599,0.00411395544745172,0.00424251655518458,0.00437107766291745,
0.00462819987838318,0.00488532209384892,0.00514244430931465,0.00565668874024611,
0.00591381095571184,0.00617093317117758,0.00668517760210904,0.00681373870984191,
0.00694229981757478,0.00719942203304051,0.00771366646397197,0.00784222757170484,
0.00797078867943771,0.00822791089490344),(0.,1.),.UNSPECIFIED.)
GEOMETRIC_REPRESENTATION_ITEM()
RATIONAL_B_SPLINE_SURFACE(((1.,0.727605019291272,1.),(1.,0.738269745261549,
1.),(1.,0.748592075286312,1.),(1.,0.768595657332798,1.),(1.,0.77827867017842,
1.),(1.,0.78996120454497,1.),(1.,0.792280826878612,1.),(1.,0.796828421990593,
1.),(1.,0.799061536127563,1.),(1.,0.805638929370508,1.),(1.,0.809861611074041,
1.),(1.,0.822031308701411,1.),(1.,0.829487589673691,1.),(1.,0.83785145435952,
1.),(1.,0.839480856802847,1.),(1.,0.842608559784881,1.),(1.,0.844105726044166,
1.),(1.,0.8483952491525,1.),(1.,0.850986216864091,1.),(1.,0.855606962686796,
1.),(1.,0.857636888703679,1.),(1.,0.860227819923722,1.),(1.,0.861017295679437,
1.),(1.,0.862419224745769,1.),(1.,0.863034322359247,1.),(1.,0.865683471685309,
1.),(1.,0.866451432203696,1.),(1.,0.865641730003757,1.),(1.,0.865389467353766,
1.),(1.,0.864714302219203,1.),(1.,0.864291039129295,1.),(1.,0.862771536048431,
1.),(1.,0.861426213021586,1.),(1.,0.858926691433347,1.),(1.,0.858013099107922,
1.),(1.,0.856026014492249,1.),(1.,0.854948935558792,1.),(1.,0.851506192237994,
1.),(1.,0.848937517425832,1.),(1.,0.843296974763866,1.),(1.,0.840224952153795,
1.),(1.,0.833601620182266,1.),(1.,0.830031077299106,1.),(1.,0.818809152212353,
1.),(1.,0.810636621270602,1.),(1.,0.797446978165117,1.),(1.,0.792872941755034,
1.),(1.,0.78353694939152,1.),(1.,0.778775433925334,1.),(1.,0.764221056564085,
1.),(1.,0.754161223208667,1.),(1.,0.741128124491465,1.),(1.,0.738495960101253,
1.),(1.,0.733227832409848,1.),(1.,0.730586739908481,1.),(1.,0.722641688562764,
1.),(1.,0.717316009840664,1.),(1.,0.701244534517323,1.),(1.,0.690405239081963,
1.),(1.,0.676661477613385,1.),(1.,0.673899376379498,1.),(1.,0.66840092468647,
1.),(1.,0.665659348664159,1.),(1.,0.657456353546285,1.),(1.,0.652016628878168,
1.),(1.,0.646603422936517,1.)))
REPRESENTATION_ITEM('')
SURFACE()
);
#11=(
BOUNDED_SURFACE()
B_SPLINE_SURFACE(3,2,((#16753,#16754,#16755),(#16756,#16757,#16758),(#16759,
#16760,#16761),(#16762,#16763,#16764),(#16765,#16766,#16767),(#16768,#16769,
#16770),(#16771,#16772,#16773),(#16774,#16775,#16776),(#16777,#16778,#16779),
(#16780,#16781,#16782),(#16783,#16784,#16785),(#16786,#16787,#16788),(#16789,
#16790,#16791),(#16792,#16793,#16794),(#16795,#16796,#16797),(#16798,#16799,
#16800),(#16801,#16802,#16803),(#16804,#16805,#16806),(#16807,#16808,#16809),
(#16810,#16811,#16812),(#16813,#16814,#16815),(#16816,#16817,#16818),(#16819,
#16820,#16821),(#16822,#16823,#16824),(#16825,#16826,#16827),(#16828,#16829,
#16830),(#16831,#16832,#16833),(#16834,#16835,#16836),(#16837,#16838,#16839),
(#16840,#16841,#16842),(#16843,#16844,#16845),(#16846,#16847,#16848),(#16849,
#16850,#16851),(#16852,#16853,#16854),(#16855,#16856,#16857),(#16858,#16859,
#16860),(#16861,#16862,#16863),(#16864,#16865,#16866),(#16867,#16868,#16869),
(#16870,#16871,#16872),(#16873,#16874,#16875),(#16876,#16877,#16878),(#16879,
#16880,#16881),(#16882,#16883,#16884),(#16885,#16886,#16887),(#16888,#16889,
#16890),(#16891,#16892,#16893),(#16894,#16895,#16896),(#16897,#16898,#16899),
(#16900,#16901,#16902),(#16903,#16904,#16905),(#16906,#16907,#16908),(#16909,
#16910,#16911),(#16912,#16913,#16914),(#16915,#16916,#16917),(#16918,#16919,
#16920),(#16921,#16922,#16923),(#16924,#16925,#16926)),.UNSPECIFIED.,.F.,
 .F.,.F.)
B_SPLINE_SURFACE_WITH_KNOTS((4,2,2,2,2,2,2,2,2,2,2,2,2,2,2,2,2,2,2,2,2,
2,2,2,2,2,2,2,4),(3,3),(0.00822791099999177,0.0087421553258349,0.00899927754130063,
0.00925639975676636,0.00951352197223209,0.00964208307996496,0.00977064418769782,
0.0102848886186293,0.010542010834095,0.0106705719418279,0.0107991330495608,
0.0113133774804922,0.011570499695958,0.0118276219114237,0.0120847441268894,
0.0123418663423552,0.0128561107732866,0.0129846718810195,0.0131132329887523,
0.0133703552042181,0.0136274774196838,0.0137560385274167,0.0138845996351495,
0.014398844066081,0.0146559662815467,0.0149130884970125,0.0154273329279439,
0.0159415773588754,0.0164558217898069),(0.,1.),.UNSPECIFIED.)
GEOMETRIC_REPRESENTATION_ITEM()
RATIONAL_B_SPLINE_SURFACE(((1.,0.646603416299741,1.),(1.,0.635777845415767,
1.),(1.,0.625055607928809,1.),(1.,0.609127621650672,1.),(1.,0.603886597603737,
1.),(1.,0.593641123894353,1.),(1.,0.588621119622323,1.),(1.,0.578794287069315,
1.),(1.,0.573987397424529,1.),(1.,0.566949594156529,1.),(1.,0.564632492256596,
1.),(1.,0.560059142358784,1.),(1.,0.557801592065244,1.),(1.,0.546803856262994,
1.),(1.,0.538816844550094,1.),(1.,0.528181154475445,1.),(1.,0.524861837914593,
1.),(1.,0.520257295698364,1.),(1.,0.518780914891828,1.),(1.,0.51599600081368,
1.),(1.,0.514683858232128,1.),(1.,0.508526013773749,1.),(1.,0.50487673783709,
1.),(1.,0.50148708526461,1.),(1.,0.500708624573298,1.),(1.,0.499919057301541,
1.),(1.,0.499897805772348,1.),(1.,0.500588074464456,1.),(1.,0.501299602522433,
1.),(1.,0.503460750293262,1.),(1.,0.504920849886873,1.),(1.,0.510276775109774,
1.),(1.,0.515155530687803,1.),(1.,0.522754639298001,1.),(1.,0.524354452613133,
1.),(1.,0.527668122842079,1.),(1.,0.529384771533693,1.),(1.,0.534705395354146,
1.),(1.,0.538479529845963,1.),(1.,0.546449215356828,1.),(1.,0.550644846474471,
1.),(1.,0.55724182544749,1.),(1.,0.559494088256891,1.),(1.,0.564052482183535,
1.),(1.,0.566363881497447,1.),(1.,0.578074130679415,1.),(1.,0.587926629008193,
1.),(1.,0.603363711869573,1.),(1.,0.608631647709976,1.),(1.,0.619200799287789,
1.),(1.,0.624523791984934,1.),(1.,0.640605786326143,1.),(1.,0.65147620310061,
1.),(1.,0.67354644028781,1.),(1.,0.684474150861673,1.),(1.,0.706154675135368,
1.),(1.,0.716910539945706,1.),(1.,0.727605019291272,1.)))
REPRESENTATION_ITEM('')
SURFACE()
);
#12=(
BOUNDED_SURFACE()
B_SPLINE_SURFACE(3,2,((#16928,#16929,#16930),(#16931,#16932,#16933),(#16934,
#16935,#16936),(#16937,#16938,#16939),(#16940,#16941,#16942),(#16943,#16944,
#16945),(#16946,#16947,#16948),(#16949,#16950,#16951),(#16952,#16953,#16954),
(#16955,#16956,#16957),(#16958,#16959,#16960),(#16961,#16962,#16963),(#16964,
#16965,#16966),(#16967,#16968,#16969),(#16970,#16971,#16972),(#16973,#16974,
#16975),(#16976,#16977,#16978),(#16979,#16980,#16981),(#16982,#16983,#16984),
(#16985,#16986,#16987),(#16988,#16989,#16990),(#16991,#16992,#16993),(#16994,
#16995,#16996),(#16997,#16998,#16999),(#17000,#17001,#17002),(#17003,#17004,
#17005),(#17006,#17007,#17008),(#17009,#17010,#17011),(#17012,#17013,#17014),
(#17015,#17016,#17017),(#17018,#17019,#17020),(#17021,#17022,#17023),(#17024,
#17025,#17026),(#17027,#17028,#17029),(#17030,#17031,#17032),(#17033,#17034,
#17035),(#17036,#17037,#17038),(#17039,#17040,#17041),(#17042,#17043,#17044),
(#17045,#17046,#17047),(#17048,#17049,#17050),(#17051,#17052,#17053),(#17054,
#17055,#17056),(#17057,#17058,#17059),(#17060,#17061,#17062),(#17063,#17064,
#17065),(#17066,#17067,#17068),(#17069,#17070,#17071),(#17072,#17073,#17074),
(#17075,#17076,#17077),(#17078,#17079,#17080),(#17081,#17082,#17083),(#17084,
#17085,#17086),(#17087,#17088,#17089),(#17090,#17091,#17092),(#17093,#17094,
#17095),(#17096,#17097,#17098),(#17099,#17100,#17101),(#17102,#17103,#17104),
(#17105,#17106,#17107),(#17108,#17109,#17110),(#17111,#17112,#17113),(#17114,
#17115,#17116),(#17117,#17118,#17119),(#17120,#17121,#17122),(#17123,#17124,
#17125)),.UNSPECIFIED.,.F.,.F.,.F.)
B_SPLINE_SURFACE_WITH_KNOTS((4,2,2,2,2,2,2,2,2,2,2,2,2,2,2,2,2,2,2,2,2,
2,2,2,2,2,2,2,2,2,2,2,4),(3,3),(0.,0.000514244430931465,0.00102848886186293,
0.0011570499695958,0.00128561107732866,0.00154273329279439,0.00205697772372586,
0.00218553883145873,0.00231409993919159,0.00257122215465732,0.00282834437012306,
0.00295690547785592,0.00308546658558879,0.00359971101652025,0.00372827212425312,
0.00385683323198599,0.00411395544745172,0.00424251655518459,0.00437107766291745,
0.00462819987838319,0.00488532209384892,0.00514244430931465,0.00565668874024611,
0.00591381095571185,0.00617093317117758,0.00668517760210904,0.00681373870984191,
0.00694229981757478,0.00719942203304051,0.00771366646397197,0.00784222757170484,
0.00797078867943771,0.00822791089490344),(0.,1.),.UNSPECIFIED.)
GEOMETRIC_REPRESENTATION_ITEM()
RATIONAL_B_SPLINE_SURFACE(((1.,0.727605019291273,1.),(1.,0.738269745261463,
1.),(1.,0.748592075286425,1.),(1.,0.768595657332682,1.),(1.,0.778278670178458,
1.),(1.,0.78996120454496,1.),(1.,0.792280826878572,1.),(1.,0.79682842199063,
1.),(1.,0.799061536127604,1.),(1.,0.805638929370428,1.),(1.,0.809861611074089,
1.),(1.,0.822031308701317,1.),(1.,0.829487589673701,1.),(1.,0.837851454359518,
1.),(1.,0.839480856802835,1.),(1.,0.842608559784893,1.),(1.,0.84410572604416,
1.),(1.,0.848395249152509,1.),(1.,0.850986216864149,1.),(1.,0.85560696268674,
1.),(1.,0.857636888703671,1.),(1.,0.860227819923728,1.),(1.,0.861017295679411,
1.),(1.,0.862419224745796,1.),(1.,0.863034322359203,1.),(1.,0.865683471685481,
1.),(1.,0.86645143220361,1.),(1.,0.865641730003779,1.),(1.,0.865389467353773,
1.),(1.,0.864714302219195,1.),(1.,0.864291039129257,1.),(1.,0.862771536048502,
1.),(1.,0.861426213021595,1.),(1.,0.858926691433342,1.),(1.,0.858013099107929,
1.),(1.,0.856026014492242,1.),(1.,0.854948935558757,1.),(1.,0.851506192238061,
1.),(1.,0.848937517425937,1.),(1.,0.84329697476376,1.),(1.,0.84022495215382,
1.),(1.,0.833601620182241,1.),(1.,0.830031077299101,1.),(1.,0.818809152212363,
1.),(1.,0.810636621270581,1.),(1.,0.797446978165125,1.),(1.,0.792872941755087,
1.),(1.,0.783536949391466,1.),(1.,0.778775433925213,1.),(1.,0.764221056564323,
1.),(1.,0.754161223208549,1.),(1.,0.741128124491493,1.),(1.,0.738495960101291,
1.),(1.,0.73322783240981,1.),(1.,0.73058673990848,1.),(1.,0.722641688562763,
1.),(1.,0.717316009840587,1.),(1.,0.701244534517476,1.),(1.,0.690405239082108,
1.),(1.,0.676661477613348,1.),(1.,0.673899376379507,1.),(1.,0.66840092468646,
1.),(1.,0.665659348664103,1.),(1.,0.657456353546395,1.),(1.,0.652016628878089,
1.),(1.,0.646603422936514,1.)))
REPRESENTATION_ITEM('')
SURFACE()
);
#13=(
BOUNDED_SURFACE()
B_SPLINE_SURFACE(3,2,((#17128,#17129,#17130),(#17131,#17132,#17133),(#17134,
#17135,#17136),(#17137,#17138,#17139),(#17140,#17141,#17142),(#17143,#17144,
#17145),(#17146,#17147,#17148),(#17149,#17150,#17151),(#17152,#17153,#17154),
(#17155,#17156,#17157),(#17158,#17159,#17160),(#17161,#17162,#17163),(#17164,
#17165,#17166),(#17167,#17168,#17169),(#17170,#17171,#17172),(#17173,#17174,
#17175),(#17176,#17177,#17178),(#17179,#17180,#17181),(#17182,#17183,#17184),
(#17185,#17186,#17187),(#17188,#17189,#17190),(#17191,#17192,#17193),(#17194,
#17195,#17196),(#17197,#17198,#17199),(#17200,#17201,#17202),(#17203,#17204,
#17205),(#17206,#17207,#17208),(#17209,#17210,#17211),(#17212,#17213,#17214),
(#17215,#17216,#17217),(#17218,#17219,#17220),(#17221,#17222,#17223),(#17224,
#17225,#17226),(#17227,#17228,#17229),(#17230,#17231,#17232),(#17233,#17234,
#17235),(#17236,#17237,#17238),(#17239,#17240,#17241),(#17242,#17243,#17244),
(#17245,#17246,#17247),(#17248,#17249,#17250),(#17251,#17252,#17253),(#17254,
#17255,#17256),(#17257,#17258,#17259),(#17260,#17261,#17262),(#17263,#17264,
#17265),(#17266,#17267,#17268),(#17269,#17270,#17271),(#17272,#17273,#17274),
(#17275,#17276,#17277),(#17278,#17279,#17280),(#17281,#17282,#17283),(#17284,
#17285,#17286),(#17287,#17288,#17289),(#17290,#17291,#17292),(#17293,#17294,
#17295),(#17296,#17297,#17298),(#17299,#17300,#17301)),.UNSPECIFIED.,.F.,
 .F.,.F.)
B_SPLINE_SURFACE_WITH_KNOTS((4,2,2,2,2,2,2,2,2,2,2,2,2,2,2,2,2,2,2,2,2,
2,2,2,2,2,2,2,4),(3,3),(0.00822791099999177,0.0087421553258349,0.00899927754130063,
0.00925639975676636,0.0095135219722321,0.00964208307996496,0.00977064418769783,
0.0102848886186293,0.010542010834095,0.0106705719418279,0.0107991330495608,
0.0113133774804922,0.011570499695958,0.0118276219114237,0.0120847441268894,
0.0123418663423552,0.0128561107732866,0.0129846718810195,0.0131132329887524,
0.0133703552042181,0.0136274774196838,0.0137560385274167,0.0138845996351495,
0.014398844066081,0.0146559662815467,0.0149130884970125,0.0154273329279439,
0.0159415773588754,0.0164558217898069),(0.,1.),.UNSPECIFIED.)
GEOMETRIC_REPRESENTATION_ITEM()
RATIONAL_B_SPLINE_SURFACE(((1.,0.646603416299739,1.),(1.,0.635777845415872,
1.),(1.,0.625055607928666,1.),(1.,0.609127621650746,1.),(1.,0.603886597603766,
1.),(1.,0.593641123894325,1.),(1.,0.588621119622213,1.),(1.,0.578794287069424,
1.),(1.,0.573987397424613,1.),(1.,0.566949594156483,1.),(1.,0.564632492256567,
1.),(1.,0.560059142358813,1.),(1.,0.557801592065364,1.),(1.,0.546803856262498,
1.),(1.,0.538816844550381,1.),(1.,0.528181154475289,1.),(1.,0.524861837914536,
1.),(1.,0.520257295698394,1.),(1.,0.518780914891774,1.),(1.,0.515996000813732,
1.),(1.,0.514683858232152,1.),(1.,0.508526013773653,1.),(1.,0.504876737837329,
1.),(1.,0.501487085264488,1.),(1.,0.500708624573413,1.),(1.,0.499919057301424,
1.),(1.,0.499897805772289,1.),(1.,0.500588074464511,1.),(1.,0.501299602522455,
1.),(1.,0.503460750293236,1.),(1.,0.504920849887092,1.),(1.,0.510276775109342,
1.),(1.,0.515155530687803,1.),(1.,0.522754639298001,1.),(1.,0.52435445261312,
1.),(1.,0.527668122842095,1.),(1.,0.529384771533763,1.),(1.,0.534705395354007,
1.),(1.,0.538479529845905,1.),(1.,0.546449215356886,1.),(1.,0.550644846474304,
1.),(1.,0.55724182544757,1.),(1.,0.559494088256935,1.),(1.,0.564052482183492,
1.),(1.,0.566363881497433,1.),(1.,0.578074130679462,1.),(1.,0.587926629008058,
1.),(1.,0.603363711869641,1.),(1.,0.608631647710066,1.),(1.,0.619200799287697,
1.),(1.,0.624523791984965,1.),(1.,0.640605786326088,1.),(1.,0.651476203100892,
1.),(1.,0.67354644028753,1.),(1.,0.684474150861655,1.),(1.,0.706154675135388,
1.),(1.,0.716910539945691,1.),(1.,0.727605019291273,1.)))
REPRESENTATION_ITEM('')
SURFACE()
);
#14=(
BOUNDED_SURFACE()
B_SPLINE_SURFACE(3,2,((#17308,#17309,#17310),(#17311,#17312,#17313),(#17314,
#17315,#17316),(#17317,#17318,#17319),(#17320,#17321,#17322),(#17323,#17324,
#17325),(#17326,#17327,#17328),(#17329,#17330,#17331),(#17332,#17333,#17334),
(#17335,#17336,#17337),(#17338,#17339,#17340),(#17341,#17342,#17343),(#17344,
#17345,#17346),(#17347,#17348,#17349),(#17350,#17351,#17352),(#17353,#17354,
#17355),(#17356,#17357,#17358),(#17359,#17360,#17361),(#17362,#17363,#17364),
(#17365,#17366,#17367),(#17368,#17369,#17370),(#17371,#17372,#17373),(#17374,
#17375,#17376),(#17377,#17378,#17379),(#17380,#17381,#17382),(#17383,#17384,
#17385),(#17386,#17387,#17388),(#17389,#17390,#17391),(#17392,#17393,#17394),
(#17395,#17396,#17397),(#17398,#17399,#17400),(#17401,#17402,#17403),(#17404,
#17405,#17406),(#17407,#17408,#17409),(#17410,#17411,#17412),(#17413,#17414,
#17415),(#17416,#17417,#17418),(#17419,#17420,#17421),(#17422,#17423,#17424),
(#17425,#17426,#17427),(#17428,#17429,#17430),(#17431,#17432,#17433),(#17434,
#17435,#17436),(#17437,#17438,#17439),(#17440,#17441,#17442),(#17443,#17444,
#17445),(#17446,#17447,#17448),(#17449,#17450,#17451),(#17452,#17453,#17454),
(#17455,#17456,#17457),(#17458,#17459,#17460),(#17461,#17462,#17463),(#17464,
#17465,#17466),(#17467,#17468,#17469),(#17470,#17471,#17472),(#17473,#17474,
#17475),(#17476,#17477,#17478),(#17479,#17480,#17481),(#17482,#17483,#17484),
(#17485,#17486,#17487),(#17488,#17489,#17490),(#17491,#17492,#17493),(#17494,
#17495,#17496),(#17497,#17498,#17499),(#17500,#17501,#17502),(#17503,#17504,
#17505)),.UNSPECIFIED.,.F.,.F.,.F.)
B_SPLINE_SURFACE_WITH_KNOTS((4,2,2,2,2,2,2,2,2,2,2,2,2,2,2,2,2,2,2,2,2,
2,2,2,2,2,2,2,2,2,2,2,4),(3,3),(0.,0.000514244430931465,0.00102848886186293,
0.0011570499695958,0.00128561107732866,0.00154273329279439,0.00205697772372586,
0.00218553883145873,0.00231409993919159,0.00257122215465732,0.00282834437012306,
0.00295690547785592,0.00308546658558879,0.00359971101652025,0.00372827212425312,
0.00385683323198599,0.00411395544745172,0.00424251655518459,0.00437107766291745,
0.00462819987838319,0.00488532209384892,0.00514244430931465,0.00565668874024611,
0.00591381095571185,0.00617093317117758,0.00668517760210904,0.00681373870984191,
0.00694229981757478,0.00719942203304051,0.00771366646397197,0.00784222757170484,
0.00797078867943771,0.00822791089490344),(0.,1.),.UNSPECIFIED.)
GEOMETRIC_REPRESENTATION_ITEM()
RATIONAL_B_SPLINE_SURFACE(((1.,0.727605019291271,1.),(1.,0.738269745261525,
1.),(1.,0.748592075286343,1.),(1.,0.768595657332771,1.),(1.,0.778278670178227,
1.),(1.,0.789961204545018,1.),(1.,0.792280826878548,1.),(1.,0.796828421990654,
1.),(1.,0.799061536127593,1.),(1.,0.805638929370445,1.),(1.,0.809861611074169,
1.),(1.,0.822031308701155,1.),(1.,0.82948758967367,1.),(1.,0.837851454359524,
1.),(1.,0.839480856802831,1.),(1.,0.842608559784899,1.),(1.,0.844105726044111,
1.),(1.,0.848395249152611,1.),(1.,0.850986216864154,1.),(1.,0.855606962686734,
1.),(1.,0.85763688870368,1.),(1.,0.860227819923723,1.),(1.,0.861017295679384,
1.),(1.,0.862419224745822,1.),(1.,0.863034322359218,1.),(1.,0.865683471685424,
1.),(1.,0.866451432203608,1.),(1.,0.865641730003778,1.),(1.,0.865389467353742,
1.),(1.,0.864714302219227,1.),(1.,0.86429103912928,1.),(1.,0.862771536048459,
1.),(1.,0.861426213021567,1.),(1.,0.858926691433357,1.),(1.,0.858013099107913,
1.),(1.,0.856026014492259,1.),(1.,0.854948935558786,1.),(1.,0.851506192238003,
1.),(1.,0.848937517425855,1.),(1.,0.843296974763842,1.),(1.,0.840224952153848,
1.),(1.,0.833601620182212,1.),(1.,0.830031077299101,1.),(1.,0.818809152212363,
1.),(1.,0.810636621270486,1.),(1.,0.797446978165174,1.),(1.,0.792872941755086,
1.),(1.,0.783536949391466,1.),(1.,0.778775433925242,1.),(1.,0.764221056564266,
1.),(1.,0.754161223208754,1.),(1.,0.741128124491444,1.),(1.,0.738495960101248,
1.),(1.,0.733227832409853,1.),(1.,0.730586739908468,1.),(1.,0.722641688562787,
1.),(1.,0.717316009840591,1.),(1.,0.701244534517466,1.),(1.,0.69040523908203,
1.),(1.,0.676661477613367,1.),(1.,0.67389937637949,1.),(1.,0.668400924686476,
1.),(1.,0.665659348664088,1.),(1.,0.65745635354643,1.),(1.,0.652016628878062,
1.),(1.,0.646603422936515,1.)))
REPRESENTATION_ITEM('')
SURFACE()
);
#15=(
BOUNDED_SURFACE()
B_SPLINE_SURFACE(3,2,((#17508,#17509,#17510),(#17511,#17512,#17513),(#17514,
#17515,#17516),(#17517,#17518,#17519),(#17520,#17521,#17522),(#17523,#17524,
#17525),(#17526,#17527,#17528),(#17529,#17530,#17531),(#17532,#17533,#17534),
(#17535,#17536,#17537),(#17538,#17539,#17540),(#17541,#17542,#17543),(#17544,
#17545,#17546),(#17547,#17548,#17549),(#17550,#17551,#17552),(#17553,#17554,
#17555),(#17556,#17557,#17558),(#17559,#17560,#17561),(#17562,#17563,#17564),
(#17565,#17566,#17567),(#17568,#17569,#17570),(#17571,#17572,#17573),(#17574,
#17575,#17576),(#17577,#17578,#17579),(#17580,#17581,#17582),(#17583,#17584,
#17585),(#17586,#17587,#17588),(#17589,#17590,#17591),(#17592,#17593,#17594),
(#17595,#17596,#17597),(#17598,#17599,#17600),(#17601,#17602,#17603),(#17604,
#17605,#17606),(#17607,#17608,#17609),(#17610,#17611,#17612),(#17613,#17614,
#17615),(#17616,#17617,#17618),(#17619,#17620,#17621),(#17622,#17623,#17624),
(#17625,#17626,#17627),(#17628,#17629,#17630),(#17631,#17632,#17633),(#17634,
#17635,#17636),(#17637,#17638,#17639),(#17640,#17641,#17642),(#17643,#17644,
#17645),(#17646,#17647,#17648),(#17649,#17650,#17651),(#17652,#17653,#17654),
(#17655,#17656,#17657),(#17658,#17659,#17660),(#17661,#17662,#17663),(#17664,
#17665,#17666),(#17667,#17668,#17669),(#17670,#17671,#17672),(#17673,#17674,
#17675),(#17676,#17677,#17678),(#17679,#17680,#17681)),.UNSPECIFIED.,.F.,
 .F.,.F.)
B_SPLINE_SURFACE_WITH_KNOTS((4,2,2,2,2,2,2,2,2,2,2,2,2,2,2,2,2,2,2,2,2,
2,2,2,2,2,2,2,4),(3,3),(0.00822791099999177,0.0087421553258349,0.00899927754130063,
0.00925639975676637,0.0095135219722321,0.00964208307996496,0.00977064418769783,
0.0102848886186293,0.010542010834095,0.0106705719418279,0.0107991330495608,
0.0113133774804922,0.011570499695958,0.0118276219114237,0.0120847441268894,
0.0123418663423552,0.0128561107732866,0.0129846718810195,0.0131132329887524,
0.0133703552042181,0.0136274774196838,0.0137560385274167,0.0138845996351496,
0.014398844066081,0.0146559662815468,0.0149130884970125,0.015427332927944,
0.0159415773588754,0.0164558217898069),(0.,1.),.UNSPECIFIED.)
GEOMETRIC_REPRESENTATION_ITEM()
RATIONAL_B_SPLINE_SURFACE(((1.,0.646603416299741,1.),(1.,0.635777845415857,
1.),(1.,0.625055607928685,1.),(1.,0.609127621650736,1.),(1.,0.603886597603802,
1.),(1.,0.593641123894284,1.),(1.,0.588621119622386,1.),(1.,0.578794287069253,
1.),(1.,0.573987397424614,1.),(1.,0.566949594156484,1.),(1.,0.564632492256556,
1.),(1.,0.560059142358826,1.),(1.,0.557801592065362,1.),(1.,0.546803856262521,
1.),(1.,0.538816844550013,1.),(1.,0.528181154475479,1.),(1.,0.524861837914558,
1.),(1.,0.52025729569838,1.),(1.,0.518780914891758,1.),(1.,0.51599600081375,
1.),(1.,0.514683858232071,1.),(1.,0.50852601377398,1.),(1.,0.504876737836812,
1.),(1.,0.50148708526475,1.),(1.,0.500708624573357,1.),(1.,0.499919057301484,
1.),(1.,0.499897805772248,1.),(1.,0.500588074464557,1.),(1.,0.501299602522294,
1.),(1.,0.503460750293403,1.),(1.,0.504920849886794,1.),(1.,0.510276775109926,
1.),(1.,0.515155530687822,1.),(1.,0.522754639297996,1.),(1.,0.524354452613109,
1.),(1.,0.527668122842108,1.),(1.,0.529384771533807,1.),(1.,0.534705395353914,
1.),(1.,0.538479529846021,1.),(1.,0.546449215356772,1.),(1.,0.550644846474468,
1.),(1.,0.557241825447494,1.),(1.,0.559494088256949,1.),(1.,0.564052482183478,
1.),(1.,0.566363881497384,1.),(1.,0.578074130679665,1.),(1.,0.587926629008355,
1.),(1.,0.603363711869489,1.),(1.,0.608631647709893,1.),(1.,0.61920079928787,
1.),(1.,0.624523791984875,1.),(1.,0.640605786326271,1.),(1.,0.651476203100745,
1.),(1.,0.673546440287674,1.),(1.,0.684474150861577,1.),(1.,0.706154675135463,
1.),(1.,0.716910539945636,1.),(1.,0.727605019291271,1.)))
REPRESENTATION_ITEM('')
SURFACE()
);
#16=(
BOUNDED_SURFACE()
B_SPLINE_SURFACE(3,2,((#17683,#17684,#17685),(#17686,#17687,#17688),(#17689,
#17690,#17691),(#17692,#17693,#17694),(#17695,#17696,#17697),(#17698,#17699,
#17700),(#17701,#17702,#17703),(#17704,#17705,#17706),(#17707,#17708,#17709),
(#17710,#17711,#17712),(#17713,#17714,#17715),(#17716,#17717,#17718),(#17719,
#17720,#17721),(#17722,#17723,#17724),(#17725,#17726,#17727),(#17728,#17729,
#17730),(#17731,#17732,#17733),(#17734,#17735,#17736),(#17737,#17738,#17739),
(#17740,#17741,#17742),(#17743,#17744,#17745),(#17746,#17747,#17748),(#17749,
#17750,#17751),(#17752,#17753,#17754),(#17755,#17756,#17757),(#17758,#17759,
#17760),(#17761,#17762,#17763),(#17764,#17765,#17766),(#17767,#17768,#17769),
(#17770,#17771,#17772),(#17773,#17774,#17775),(#17776,#17777,#17778),(#17779,
#17780,#17781),(#17782,#17783,#17784),(#17785,#17786,#17787),(#17788,#17789,
#17790),(#17791,#17792,#17793),(#17794,#17795,#17796),(#17797,#17798,#17799),
(#17800,#17801,#17802),(#17803,#17804,#17805),(#17806,#17807,#17808),(#17809,
#17810,#17811),(#17812,#17813,#17814),(#17815,#17816,#17817),(#17818,#17819,
#17820),(#17821,#17822,#17823),(#17824,#17825,#17826),(#17827,#17828,#17829),
(#17830,#17831,#17832),(#17833,#17834,#17835),(#17836,#17837,#17838),(#17839,
#17840,#17841),(#17842,#17843,#17844),(#17845,#17846,#17847),(#17848,#17849,
#17850),(#17851,#17852,#17853),(#17854,#17855,#17856),(#17857,#17858,#17859),
(#17860,#17861,#17862),(#17863,#17864,#17865),(#17866,#17867,#17868),(#17869,
#17870,#17871),(#17872,#17873,#17874),(#17875,#17876,#17877),(#17878,#17879,
#17880)),.UNSPECIFIED.,.F.,.F.,.F.)
B_SPLINE_SURFACE_WITH_KNOTS((4,2,2,2,2,2,2,2,2,2,2,2,2,2,2,2,2,2,2,2,2,
2,2,2,2,2,2,2,2,2,2,2,4),(3,3),(0.,0.000514244430931465,0.00102848886186293,
0.0011570499695958,0.00128561107732866,0.0015427332927944,0.00205697772372586,
0.00218553883145873,0.00231409993919159,0.00257122215465733,0.00282834437012306,
0.00295690547785592,0.00308546658558879,0.00359971101652026,0.00372827212425312,
0.00385683323198599,0.00411395544745172,0.00424251655518459,0.00437107766291745,
0.00462819987838319,0.00488532209384892,0.00514244430931465,0.00565668874024612,
0.00591381095571185,0.00617093317117758,0.00668517760210905,0.00681373870984191,
0.00694229981757478,0.00719942203304051,0.00771366646397198,0.00784222757170484,
0.00797078867943771,0.00822791089490344),(0.,1.),.UNSPECIFIED.)
GEOMETRIC_REPRESENTATION_ITEM()
RATIONAL_B_SPLINE_SURFACE(((1.,0.727605019291271,1.),(1.,0.73826974526155,
1.),(1.,0.748592075286311,1.),(1.,0.768595657332797,1.),(1.,0.778278670178333,
1.),(1.,0.789961204544991,1.),(1.,0.792280826878628,1.),(1.,0.796828421990575,
1.),(1.,0.799061536127595,1.),(1.,0.805638929370441,1.),(1.,0.809861611074004,
1.),(1.,0.822031308701488,1.),(1.,0.829487589673555,1.),(1.,0.837851454359553,
1.),(1.,0.839480856802828,1.),(1.,0.842608559784896,1.),(1.,0.844105726044104,
1.),(1.,0.848395249152619,1.),(1.,0.850986216864176,1.),(1.,0.855606962686709,
1.),(1.,0.857636888703722,1.),(1.,0.8602278199237,1.),(1.,0.861017295679405,
1.),(1.,0.862419224745804,1.),(1.,0.863034322359246,1.),(1.,0.865683471685309,
1.),(1.,0.866451432203406,1.),(1.,0.865641730003829,1.),(1.,0.865389467353775,
1.),(1.,0.864714302219193,1.),(1.,0.864291039129234,1.),(1.,0.86277153604855,
1.),(1.,0.861426213021591,1.),(1.,0.858926691433344,1.),(1.,0.858013099107921,
1.),(1.,0.856026014492253,1.),(1.,0.854948935558772,1.),(1.,0.851506192238033,
1.),(1.,0.848937517425913,1.),(1.,0.843296974763785,1.),(1.,0.840224952153864,
1.),(1.,0.8336016201822,1.),(1.,0.830031077299088,1.),(1.,0.818809152212393,
1.),(1.,0.81063662127041,1.),(1.,0.797446978165214,1.),(1.,0.79287294175514,
1.),(1.,0.783536949391413,1.),(1.,0.778775433925223,1.),(1.,0.764221056564304,
1.),(1.,0.754161223208502,1.),(1.,0.741128124491506,1.),(1.,0.738495960101228,
1.),(1.,0.733227832409877,1.),(1.,0.73058673990845,1.),(1.,0.722641688562826,
1.),(1.,0.717316009840618,1.),(1.,0.701244534517407,1.),(1.,0.69040523908201,
1.),(1.,0.676661477613371,1.),(1.,0.673899376379567,1.),(1.,0.668400924686399,
1.),(1.,0.665659348664101,1.),(1.,0.657456353546401,1.),(1.,0.652016628878085,
1.),(1.,0.646603422936515,1.)))
REPRESENTATION_ITEM('')
SURFACE()
);
#17=(
BOUNDED_SURFACE()
B_SPLINE_SURFACE(3,2,((#17883,#17884,#17885),(#17886,#17887,#17888),(#17889,
#17890,#17891),(#17892,#17893,#17894),(#17895,#17896,#17897),(#17898,#17899,
#17900),(#17901,#17902,#17903),(#17904,#17905,#17906),(#17907,#17908,#17909),
(#17910,#17911,#17912),(#17913,#17914,#17915),(#17916,#17917,#17918),(#17919,
#17920,#17921),(#17922,#17923,#17924),(#17925,#17926,#17927),(#17928,#17929,
#17930),(#17931,#17932,#17933),(#17934,#17935,#17936),(#17937,#17938,#17939),
(#17940,#17941,#17942),(#17943,#17944,#17945),(#17946,#17947,#17948),(#17949,
#17950,#17951),(#17952,#17953,#17954),(#17955,#17956,#17957),(#17958,#17959,
#17960),(#17961,#17962,#17963),(#17964,#17965,#17966),(#17967,#17968,#17969),
(#17970,#17971,#17972),(#17973,#17974,#17975),(#17976,#17977,#17978),(#17979,
#17980,#17981),(#17982,#17983,#17984),(#17985,#17986,#17987),(#17988,#17989,
#17990),(#17991,#17992,#17993),(#17994,#17995,#17996),(#17997,#17998,#17999),
(#18000,#18001,#18002),(#18003,#18004,#18005),(#18006,#18007,#18008),(#18009,
#18010,#18011),(#18012,#18013,#18014),(#18015,#18016,#18017),(#18018,#18019,
#18020),(#18021,#18022,#18023),(#18024,#18025,#18026),(#18027,#18028,#18029),
(#18030,#18031,#18032),(#18033,#18034,#18035),(#18036,#18037,#18038),(#18039,
#18040,#18041),(#18042,#18043,#18044),(#18045,#18046,#18047),(#18048,#18049,
#18050),(#18051,#18052,#18053),(#18054,#18055,#18056)),.UNSPECIFIED.,.F.,
 .F.,.F.)
B_SPLINE_SURFACE_WITH_KNOTS((4,2,2,2,2,2,2,2,2,2,2,2,2,2,2,2,2,2,2,2,2,
2,2,2,2,2,2,2,4),(3,3),(0.00822791099999177,0.0087421553258349,0.00899927754130063,
0.00925639975676637,0.0095135219722321,0.00964208307996496,0.00977064418769783,
0.0102848886186293,0.010542010834095,0.0106705719418279,0.0107991330495608,
0.0113133774804922,0.011570499695958,0.0118276219114237,0.0120847441268894,
0.0123418663423552,0.0128561107732866,0.0129846718810195,0.0131132329887524,
0.0133703552042181,0.0136274774196838,0.0137560385274167,0.0138845996351496,
0.014398844066081,0.0146559662815468,0.0149130884970125,0.015427332927944,
0.0159415773588754,0.0164558217898069),(0.,1.),.UNSPECIFIED.)
GEOMETRIC_REPRESENTATION_ITEM()
RATIONAL_B_SPLINE_SURFACE(((1.,0.646603416299739,1.),(1.,0.635777845416042,
1.),(1.,0.625055607928442,1.),(1.,0.609127621650856,1.),(1.,0.603886597603835,
1.),(1.,0.593641123894259,1.),(1.,0.588621119622324,1.),(1.,0.578794287069315,
1.),(1.,0.573987397424525,1.),(1.,0.566949594156524,1.),(1.,0.56463249225661,
1.),(1.,0.560059142358769,1.),(1.,0.557801592065279,1.),(1.,0.546803856262847,
1.),(1.,0.538816844549984,1.),(1.,0.528181154475494,1.),(1.,0.524861837914484,
1.),(1.,0.520257295698421,1.),(1.,0.518780914891841,1.),(1.,0.515996000813673,
1.),(1.,0.514683858232072,1.),(1.,0.508526013773969,1.),(1.,0.504876737837079,
1.),(1.,0.501487085264613,1.),(1.,0.500708624573569,1.),(1.,0.499919057301272,
1.),(1.,0.499897805772071,1.),(1.,0.500588074464734,1.),(1.,0.501299602522428,
1.),(1.,0.503460750293267,1.),(1.,0.504920849886908,1.),(1.,0.510276775109707,
1.),(1.,0.515155530687388,1.),(1.,0.522754639298105,1.),(1.,0.524354452613123,
1.),(1.,0.527668122842088,1.),(1.,0.529384771533702,1.),(1.,0.534705395354127,
1.),(1.,0.538479529845934,1.),(1.,0.546449215356857,1.),(1.,0.550644846474326,
1.),(1.,0.557241825447563,1.),(1.,0.559494088256871,1.),(1.,0.564052482183554,
1.),(1.,0.566363881497371,1.),(1.,0.578074130679723,1.),(1.,0.58792662900804,
1.),(1.,0.603363711869652,1.),(1.,0.608631647710062,1.),(1.,0.619200799287702,
1.),(1.,0.624523791984873,1.),(1.,0.640605786326268,1.),(1.,0.651476203100977,
1.),(1.,0.673546440287441,1.),(1.,0.684474150861875,1.),(1.,0.706154675135167,
1.),(1.,0.716910539945856,1.),(1.,0.727605019291271,1.)))
REPRESENTATION_ITEM('')
SURFACE()
);
#18=(
BOUNDED_SURFACE()
B_SPLINE_SURFACE(3,2,((#18058,#18059,#18060),(#18061,#18062,#18063),(#18064,
#18065,#18066),(#18067,#18068,#18069),(#18070,#18071,#18072),(#18073,#18074,
#18075),(#18076,#18077,#18078),(#18079,#18080,#18081),(#18082,#18083,#18084),
(#18085,#18086,#18087),(#18088,#18089,#18090),(#18091,#18092,#18093),(#18094,
#18095,#18096),(#18097,#18098,#18099),(#18100,#18101,#18102),(#18103,#18104,
#18105),(#18106,#18107,#18108),(#18109,#18110,#18111),(#18112,#18113,#18114),
(#18115,#18116,#18117),(#18118,#18119,#18120),(#18121,#18122,#18123),(#18124,
#18125,#18126),(#18127,#18128,#18129),(#18130,#18131,#18132),(#18133,#18134,
#18135),(#18136,#18137,#18138),(#18139,#18140,#18141),(#18142,#18143,#18144),
(#18145,#18146,#18147),(#18148,#18149,#18150),(#18151,#18152,#18153),(#18154,
#18155,#18156),(#18157,#18158,#18159),(#18160,#18161,#18162),(#18163,#18164,
#18165),(#18166,#18167,#18168),(#18169,#18170,#18171),(#18172,#18173,#18174),
(#18175,#18176,#18177),(#18178,#18179,#18180),(#18181,#18182,#18183),(#18184,
#18185,#18186),(#18187,#18188,#18189),(#18190,#18191,#18192),(#18193,#18194,
#18195),(#18196,#18197,#18198),(#18199,#18200,#18201),(#18202,#18203,#18204),
(#18205,#18206,#18207),(#18208,#18209,#18210),(#18211,#18212,#18213),(#18214,
#18215,#18216),(#18217,#18218,#18219),(#18220,#18221,#18222),(#18223,#18224,
#18225),(#18226,#18227,#18228),(#18229,#18230,#18231),(#18232,#18233,#18234),
(#18235,#18236,#18237),(#18238,#18239,#18240),(#18241,#18242,#18243),(#18244,
#18245,#18246),(#18247,#18248,#18249),(#18250,#18251,#18252),(#18253,#18254,
#18255)),.UNSPECIFIED.,.F.,.F.,.F.)
B_SPLINE_SURFACE_WITH_KNOTS((4,2,2,2,2,2,2,2,2,2,2,2,2,2,2,2,2,2,2,2,2,
2,2,2,2,2,2,2,2,2,2,2,4),(3,3),(0.,0.000514244430931465,0.00102848886186293,
0.0011570499695958,0.00128561107732866,0.00154273329279439,0.00205697772372586,
0.00218553883145873,0.00231409993919159,0.00257122215465732,0.00282834437012306,
0.00295690547785592,0.00308546658558879,0.00359971101652025,0.00372827212425312,
0.00385683323198599,0.00411395544745172,0.00424251655518459,0.00437107766291745,
0.00462819987838319,0.00488532209384892,0.00514244430931465,0.00565668874024611,
0.00591381095571185,0.00617093317117758,0.00668517760210904,0.00681373870984191,
0.00694229981757478,0.00719942203304051,0.00771366646397197,0.00784222757170484,
0.00797078867943771,0.00822791089490344),(0.,1.),.UNSPECIFIED.)
GEOMETRIC_REPRESENTATION_ITEM()
RATIONAL_B_SPLINE_SURFACE(((1.,0.727605019291273,1.),(1.,0.738269745261463,
1.),(1.,0.748592075286425,1.),(1.,0.768595657332682,1.),(1.,0.778278670178458,
1.),(1.,0.78996120454496,1.),(1.,0.792280826878572,1.),(1.,0.79682842199063,
1.),(1.,0.799061536127604,1.),(1.,0.805638929370428,1.),(1.,0.809861611074089,
1.),(1.,0.822031308701317,1.),(1.,0.829487589673701,1.),(1.,0.837851454359518,
1.),(1.,0.839480856802835,1.),(1.,0.842608559784893,1.),(1.,0.84410572604416,
1.),(1.,0.848395249152509,1.),(1.,0.850986216864149,1.),(1.,0.85560696268674,
1.),(1.,0.857636888703671,1.),(1.,0.860227819923728,1.),(1.,0.861017295679411,
1.),(1.,0.862419224745796,1.),(1.,0.863034322359203,1.),(1.,0.865683471685481,
1.),(1.,0.86645143220361,1.),(1.,0.865641730003779,1.),(1.,0.865389467353773,
1.),(1.,0.864714302219195,1.),(1.,0.864291039129257,1.),(1.,0.862771536048502,
1.),(1.,0.861426213021595,1.),(1.,0.858926691433342,1.),(1.,0.858013099107929,
1.),(1.,0.856026014492242,1.),(1.,0.854948935558757,1.),(1.,0.851506192238061,
1.),(1.,0.848937517425937,1.),(1.,0.84329697476376,1.),(1.,0.84022495215382,
1.),(1.,0.833601620182241,1.),(1.,0.830031077299101,1.),(1.,0.818809152212363,
1.),(1.,0.810636621270581,1.),(1.,0.797446978165125,1.),(1.,0.792872941755087,
1.),(1.,0.783536949391466,1.),(1.,0.778775433925213,1.),(1.,0.764221056564323,
1.),(1.,0.754161223208549,1.),(1.,0.741128124491493,1.),(1.,0.738495960101291,
1.),(1.,0.73322783240981,1.),(1.,0.73058673990848,1.),(1.,0.722641688562763,
1.),(1.,0.717316009840587,1.),(1.,0.701244534517476,1.),(1.,0.690405239082108,
1.),(1.,0.676661477613348,1.),(1.,0.673899376379507,1.),(1.,0.66840092468646,
1.),(1.,0.665659348664103,1.),(1.,0.657456353546395,1.),(1.,0.652016628878089,
1.),(1.,0.646603422936514,1.)))
REPRESENTATION_ITEM('')
SURFACE()
);
#19=(
BOUNDED_SURFACE()
B_SPLINE_SURFACE(3,2,((#18258,#18259,#18260),(#18261,#18262,#18263),(#18264,
#18265,#18266),(#18267,#18268,#18269),(#18270,#18271,#18272),(#18273,#18274,
#18275),(#18276,#18277,#18278),(#18279,#18280,#18281),(#18282,#18283,#18284),
(#18285,#18286,#18287),(#18288,#18289,#18290),(#18291,#18292,#18293),(#18294,
#18295,#18296),(#18297,#18298,#18299),(#18300,#18301,#18302),(#18303,#18304,
#18305),(#18306,#18307,#18308),(#18309,#18310,#18311),(#18312,#18313,#18314),
(#18315,#18316,#18317),(#18318,#18319,#18320),(#18321,#18322,#18323),(#18324,
#18325,#18326),(#18327,#18328,#18329),(#18330,#18331,#18332),(#18333,#18334,
#18335),(#18336,#18337,#18338),(#18339,#18340,#18341),(#18342,#18343,#18344),
(#18345,#18346,#18347),(#18348,#18349,#18350),(#18351,#18352,#18353),(#18354,
#18355,#18356),(#18357,#18358,#18359),(#18360,#18361,#18362),(#18363,#18364,
#18365),(#18366,#18367,#18368),(#18369,#18370,#18371),(#18372,#18373,#18374),
(#18375,#18376,#18377),(#18378,#18379,#18380),(#18381,#18382,#18383),(#18384,
#18385,#18386),(#18387,#18388,#18389),(#18390,#18391,#18392),(#18393,#18394,
#18395),(#18396,#18397,#18398),(#18399,#18400,#18401),(#18402,#18403,#18404),
(#18405,#18406,#18407),(#18408,#18409,#18410),(#18411,#18412,#18413),(#18414,
#18415,#18416),(#18417,#18418,#18419),(#18420,#18421,#18422),(#18423,#18424,
#18425),(#18426,#18427,#18428),(#18429,#18430,#18431)),.UNSPECIFIED.,.F.,
 .F.,.F.)
B_SPLINE_SURFACE_WITH_KNOTS((4,2,2,2,2,2,2,2,2,2,2,2,2,2,2,2,2,2,2,2,2,
2,2,2,2,2,2,2,4),(3,3),(0.00822791099999177,0.0087421553258349,0.00899927754130063,
0.00925639975676636,0.0095135219722321,0.00964208307996496,0.00977064418769783,
0.0102848886186293,0.010542010834095,0.0106705719418279,0.0107991330495608,
0.0113133774804922,0.011570499695958,0.0118276219114237,0.0120847441268894,
0.0123418663423552,0.0128561107732866,0.0129846718810195,0.0131132329887524,
0.0133703552042181,0.0136274774196838,0.0137560385274167,0.0138845996351495,
0.014398844066081,0.0146559662815467,0.0149130884970125,0.0154273329279439,
0.0159415773588754,0.0164558217898069),(0.,1.),.UNSPECIFIED.)
GEOMETRIC_REPRESENTATION_ITEM()
RATIONAL_B_SPLINE_SURFACE(((1.,0.646603416299739,1.),(1.,0.635777845415872,
1.),(1.,0.625055607928666,1.),(1.,0.609127621650746,1.),(1.,0.603886597603766,
1.),(1.,0.593641123894325,1.),(1.,0.588621119622213,1.),(1.,0.578794287069424,
1.),(1.,0.573987397424613,1.),(1.,0.566949594156483,1.),(1.,0.564632492256567,
1.),(1.,0.560059142358813,1.),(1.,0.557801592065364,1.),(1.,0.546803856262498,
1.),(1.,0.538816844550381,1.),(1.,0.528181154475289,1.),(1.,0.524861837914536,
1.),(1.,0.520257295698394,1.),(1.,0.518780914891774,1.),(1.,0.515996000813732,
1.),(1.,0.514683858232152,1.),(1.,0.508526013773653,1.),(1.,0.504876737837329,
1.),(1.,0.501487085264488,1.),(1.,0.500708624573413,1.),(1.,0.499919057301424,
1.),(1.,0.499897805772289,1.),(1.,0.500588074464511,1.),(1.,0.501299602522455,
1.),(1.,0.503460750293236,1.),(1.,0.504920849887092,1.),(1.,0.510276775109342,
1.),(1.,0.515155530687803,1.),(1.,0.522754639298001,1.),(1.,0.52435445261312,
1.),(1.,0.527668122842095,1.),(1.,0.529384771533763,1.),(1.,0.534705395354007,
1.),(1.,0.538479529845905,1.),(1.,0.546449215356886,1.),(1.,0.550644846474304,
1.),(1.,0.55724182544757,1.),(1.,0.559494088256935,1.),(1.,0.564052482183492,
1.),(1.,0.566363881497433,1.),(1.,0.578074130679462,1.),(1.,0.587926629008058,
1.),(1.,0.603363711869641,1.),(1.,0.608631647710066,1.),(1.,0.619200799287697,
1.),(1.,0.624523791984965,1.),(1.,0.640605786326088,1.),(1.,0.651476203100892,
1.),(1.,0.67354644028753,1.),(1.,0.684474150861655,1.),(1.,0.706154675135388,
1.),(1.,0.716910539945691,1.),(1.,0.727605019291273,1.)))
REPRESENTATION_ITEM('')
SURFACE()
);
#20=(
BOUNDED_SURFACE()
B_SPLINE_SURFACE(3,2,((#18433,#18434,#18435),(#18436,#18437,#18438),(#18439,
#18440,#18441),(#18442,#18443,#18444),(#18445,#18446,#18447),(#18448,#18449,
#18450),(#18451,#18452,#18453),(#18454,#18455,#18456),(#18457,#18458,#18459),
(#18460,#18461,#18462),(#18463,#18464,#18465),(#18466,#18467,#18468),(#18469,
#18470,#18471),(#18472,#18473,#18474),(#18475,#18476,#18477),(#18478,#18479,
#18480),(#18481,#18482,#18483),(#18484,#18485,#18486),(#18487,#18488,#18489),
(#18490,#18491,#18492),(#18493,#18494,#18495),(#18496,#18497,#18498),(#18499,
#18500,#18501),(#18502,#18503,#18504),(#18505,#18506,#18507),(#18508,#18509,
#18510),(#18511,#18512,#18513),(#18514,#18515,#18516),(#18517,#18518,#18519),
(#18520,#18521,#18522),(#18523,#18524,#18525),(#18526,#18527,#18528),(#18529,
#18530,#18531),(#18532,#18533,#18534),(#18535,#18536,#18537),(#18538,#18539,
#18540),(#18541,#18542,#18543),(#18544,#18545,#18546),(#18547,#18548,#18549),
(#18550,#18551,#18552),(#18553,#18554,#18555),(#18556,#18557,#18558),(#18559,
#18560,#18561),(#18562,#18563,#18564),(#18565,#18566,#18567),(#18568,#18569,
#18570),(#18571,#18572,#18573),(#18574,#18575,#18576),(#18577,#18578,#18579),
(#18580,#18581,#18582),(#18583,#18584,#18585),(#18586,#18587,#18588),(#18589,
#18590,#18591),(#18592,#18593,#18594),(#18595,#18596,#18597),(#18598,#18599,
#18600),(#18601,#18602,#18603),(#18604,#18605,#18606),(#18607,#18608,#18609),
(#18610,#18611,#18612),(#18613,#18614,#18615),(#18616,#18617,#18618),(#18619,
#18620,#18621),(#18622,#18623,#18624),(#18625,#18626,#18627),(#18628,#18629,
#18630)),.UNSPECIFIED.,.F.,.F.,.F.)
B_SPLINE_SURFACE_WITH_KNOTS((4,2,2,2,2,2,2,2,2,2,2,2,2,2,2,2,2,2,2,2,2,
2,2,2,2,2,2,2,2,2,2,2,4),(3,3),(0.,0.000514244430931465,0.00102848886186293,
0.0011570499695958,0.00128561107732866,0.00154273329279439,0.00205697772372586,
0.00218553883145872,0.00231409993919159,0.00257122215465732,0.00282834437012306,
0.00295690547785592,0.00308546658558879,0.00359971101652025,0.00372827212425312,
0.00385683323198598,0.00411395544745172,0.00424251655518458,0.00437107766291745,
0.00462819987838318,0.00488532209384891,0.00514244430931465,0.00565668874024611,
0.00591381095571184,0.00617093317117758,0.00668517760210904,0.00681373870984191,
0.00694229981757477,0.0071994220330405,0.00771366646397197,0.00784222757170484,
0.0079707886794377,0.00822791089490343),(0.,1.),.UNSPECIFIED.)
GEOMETRIC_REPRESENTATION_ITEM()
RATIONAL_B_SPLINE_SURFACE(((1.,0.727605019291272,1.),(1.,0.738269745261418,
1.),(1.,0.748592075286484,1.),(1.,0.768595657332627,1.),(1.,0.778278670178632,
1.),(1.,0.789961204544917,1.),(1.,0.792280826878605,1.),(1.,0.7968284219906,
1.),(1.,0.79906153612763,1.),(1.,0.805638929370375,1.),(1.,0.809861611074038,
1.),(1.,0.822031308701422,1.),(1.,0.829487589673633,1.),(1.,0.837851454359535,
1.),(1.,0.839480856802865,1.),(1.,0.842608559784865,1.),(1.,0.844105726044142,
1.),(1.,0.848395249152548,1.),(1.,0.850986216864158,1.),(1.,0.855606962686729,
1.),(1.,0.857636888703733,1.),(1.,0.860227819923696,1.),(1.,0.861017295679429,
1.),(1.,0.862419224745775,1.),(1.,0.863034322359217,1.),(1.,0.865683471685423,
1.),(1.,0.8664514322036,1.),(1.,0.865641730003782,1.),(1.,0.865389467353701,
1.),(1.,0.864714302219268,1.),(1.,0.864291039129274,1.),(1.,0.862771536048468,
1.),(1.,0.861426213021662,1.),(1.,0.858926691433307,1.),(1.,0.858013099107948,
1.),(1.,0.856026014492222,1.),(1.,0.854948935558751,1.),(1.,0.851506192238077,
1.),(1.,0.848937517425951,1.),(1.,0.843296974763746,1.),(1.,0.840224952153844,
1.),(1.,0.833601620182217,1.),(1.,0.830031077299082,1.),(1.,0.818809152212401,
1.),(1.,0.810636621270399,1.),(1.,0.797446978165217,1.),(1.,0.792872941755192,
1.),(1.,0.78353694939136,1.),(1.,0.778775433925171,1.),(1.,0.76422105656441,
1.),(1.,0.754161223208599,1.),(1.,0.741128124491482,1.),(1.,0.738495960101249,
1.),(1.,0.733227832409854,1.),(1.,0.730586739908469,1.),(1.,0.722641688562787,
1.),(1.,0.717316009840657,1.),(1.,0.701244534517331,1.),(1.,0.69040523908203,
1.),(1.,0.676661477613367,1.),(1.,0.673899376379489,1.),(1.,0.668400924686475,
1.),(1.,0.665659348664065,1.),(1.,0.657456353546472,1.),(1.,0.652016628878031,
1.),(1.,0.646603422936515,1.)))
REPRESENTATION_ITEM('')
SURFACE()
);
#21=(
BOUNDED_SURFACE()
B_SPLINE_SURFACE(3,2,((#18633,#18634,#18635),(#18636,#18637,#18638),(#18639,
#18640,#18641),(#18642,#18643,#18644),(#18645,#18646,#18647),(#18648,#18649,
#18650),(#18651,#18652,#18653),(#18654,#18655,#18656),(#18657,#18658,#18659),
(#18660,#18661,#18662),(#18663,#18664,#18665),(#18666,#18667,#18668),(#18669,
#18670,#18671),(#18672,#18673,#18674),(#18675,#18676,#18677),(#18678,#18679,
#18680),(#18681,#18682,#18683),(#18684,#18685,#18686),(#18687,#18688,#18689),
(#18690,#18691,#18692),(#18693,#18694,#18695),(#18696,#18697,#18698),(#18699,
#18700,#18701),(#18702,#18703,#18704),(#18705,#18706,#18707),(#18708,#18709,
#18710),(#18711,#18712,#18713),(#18714,#18715,#18716),(#18717,#18718,#18719),
(#18720,#18721,#18722),(#18723,#18724,#18725),(#18726,#18727,#18728),(#18729,
#18730,#18731),(#18732,#18733,#18734),(#18735,#18736,#18737),(#18738,#18739,
#18740),(#18741,#18742,#18743),(#18744,#18745,#18746),(#18747,#18748,#18749),
(#18750,#18751,#18752),(#18753,#18754,#18755),(#18756,#18757,#18758),(#18759,
#18760,#18761),(#18762,#18763,#18764),(#18765,#18766,#18767),(#18768,#18769,
#18770),(#18771,#18772,#18773),(#18774,#18775,#18776),(#18777,#18778,#18779),
(#18780,#18781,#18782),(#18783,#18784,#18785),(#18786,#18787,#18788),(#18789,
#18790,#18791),(#18792,#18793,#18794),(#18795,#18796,#18797),(#18798,#18799,
#18800),(#18801,#18802,#18803),(#18804,#18805,#18806)),.UNSPECIFIED.,.F.,
 .F.,.F.)
B_SPLINE_SURFACE_WITH_KNOTS((4,2,2,2,2,2,2,2,2,2,2,2,2,2,2,2,2,2,2,2,2,
2,2,2,2,2,2,2,4),(3,3),(0.00822791099999177,0.00874215532583489,0.00899927754130062,
0.00925639975676636,0.00951352197223209,0.00964208307996495,0.00977064418769782,
0.0102848886186293,0.010542010834095,0.0106705719418279,0.0107991330495608,
0.0113133774804922,0.0115704996959579,0.0118276219114237,0.0120847441268894,
0.0123418663423551,0.0128561107732866,0.0129846718810195,0.0131132329887523,
0.0133703552042181,0.0136274774196838,0.0137560385274167,0.0138845996351495,
0.014398844066081,0.0146559662815467,0.0149130884970125,0.0154273329279439,
0.0159415773588754,0.0164558217898069),(0.,1.),.UNSPECIFIED.)
GEOMETRIC_REPRESENTATION_ITEM()
RATIONAL_B_SPLINE_SURFACE(((1.,0.64660341629974,1.),(1.,0.635777845416019,
1.),(1.,0.625055607928472,1.),(1.,0.609127621650842,1.),(1.,0.603886597603866,
1.),(1.,0.593641123894224,1.),(1.,0.588621119622273,1.),(1.,0.57879428706936,
1.),(1.,0.573987397424623,1.),(1.,0.566949594156479,1.),(1.,0.564632492256641,
1.),(1.,0.560059142358733,1.),(1.,0.557801592065363,1.),(1.,0.546803856262522,
1.),(1.,0.538816844550033,1.),(1.,0.52818115447547,1.),(1.,0.524861837914559,
1.),(1.,0.52025729569838,1.),(1.,0.518780914891759,1.),(1.,0.515996000813751,
1.),(1.,0.514683858231971,1.),(1.,0.508526013774383,1.),(1.,0.504876737837149,
1.),(1.,0.501487085264582,1.),(1.,0.500708624573323,1.),(1.,0.499919057301517,
1.),(1.,0.499897805772192,1.),(1.,0.500588074464606,1.),(1.,0.501299602522453,
1.),(1.,0.503460750293243,1.),(1.,0.504920849886778,1.),(1.,0.510276775109967,
1.),(1.,0.51515553068733,1.),(1.,0.52275463929812,1.),(1.,0.524354452613149,
1.),(1.,0.527668122842061,1.),(1.,0.529384771533734,1.),(1.,0.53470539535405,
1.),(1.,0.538479529845885,1.),(1.,0.546449215356904,1.),(1.,0.550644846474257,
1.),(1.,0.557241825447595,1.),(1.,0.559494088257005,1.),(1.,0.564052482183427,
1.),(1.,0.566363881497423,1.),(1.,0.578074130679511,1.),(1.,0.587926629007972,
1.),(1.,0.603363711869685,1.),(1.,0.608631647710115,1.),(1.,0.619200799287649,
1.),(1.,0.624523791984868,1.),(1.,0.640605786326278,1.),(1.,0.651476203100764,
1.),(1.,0.673546440287654,1.),(1.,0.684474150861837,1.),(1.,0.706154675135206,
1.),(1.,0.716910539945826,1.),(1.,0.727605019291272,1.)))
REPRESENTATION_ITEM('')
SURFACE()
);
#22=SPHERICAL_SURFACE('',#9159,0.000300000000137179);
#25=CONICAL_SURFACE('',#8779,0.,0.244978663126864);
#26=CONICAL_SURFACE('',#8826,0.,0.244978663126864);
#27=CONICAL_SURFACE('',#8832,0.,0.523598775627269);
#28=CONICAL_SURFACE('',#9139,0.,1.04719755119693);
#29=CONICAL_SURFACE('',#9140,0.,1.04719755119693);
#30=CONICAL_SURFACE('',#9143,0.,1.04719755119693);
#31=CONICAL_SURFACE('',#9144,0.,1.04719755119693);
#32=CONICAL_SURFACE('',#9145,0.,1.04719755119693);
#33=CONICAL_SURFACE('',#9146,0.,1.04719755119693);
#74=TOROIDAL_SURFACE('',#8817,0.0329999999999897,0.000999999999849241);
#75=TOROIDAL_SURFACE('',#8829,0.0329999999999897,0.000999999999849247);
#76=TOROIDAL_SURFACE('',#8836,0.0180358983802304,0.0019999999955971);
#77=TOROIDAL_SURFACE('',#8838,0.0180358983802304,0.00199999999559711);
#78=TOROIDAL_SURFACE('',#8844,0.0127999999998295,0.000300000000224998);
#79=TOROIDAL_SURFACE('',#8846,0.0175358983901566,0.00149999999951453);
#80=TOROIDAL_SURFACE('',#8849,0.0175358983836069,0.0015000000001222);
#81=TOROIDAL_SURFACE('',#8852,0.0175358984068633,0.00150000000032502);
#82=TOROIDAL_SURFACE('',#8854,0.017535898384194,0.00149999999953639);
#83=TOROIDAL_SURFACE('',#8857,0.0175358984068637,0.001500000000325);
#84=TOROIDAL_SURFACE('',#8859,0.0175358983836068,0.0015000000001222);
#85=TOROIDAL_SURFACE('',#8862,0.0175358983793295,0.00149999999977719);
#86=TOROIDAL_SURFACE('',#8864,0.0175358983793296,0.00149999999977719);
#87=TOROIDAL_SURFACE('',#8866,0.0175358983836071,0.0015000000001222);
#88=TOROIDAL_SURFACE('',#8869,0.0175358984068636,0.00150000000032501);
#89=TOROIDAL_SURFACE('',#8871,0.0175358983841942,0.00149999999953638);
#90=TOROIDAL_SURFACE('',#8874,0.0175358984068633,0.00150000000032502);
#91=TOROIDAL_SURFACE('',#8876,0.017535898383607,0.0015000000001222);
#92=TOROIDAL_SURFACE('',#8967,0.0157358983846276,0.000299999999947084);
#93=TOROIDAL_SURFACE('',#9056,0.0329999999999897,0.000999999999849243);
#94=TOROIDAL_SURFACE('',#9060,0.0163358983848296,0.000300000000224998);
#95=TOROIDAL_SURFACE('',#9062,0.0329999999999897,0.000999999999849251);
#96=TOROIDAL_SURFACE('',#9065,0.0163358983848296,0.000300000000224997);
#97=TOROIDAL_SURFACE('',#9090,0.0175358983853182,0.00150000000045805);
#98=TOROIDAL_SURFACE('',#9094,0.0175358983853182,0.00150000000045805);
#99=TOROIDAL_SURFACE('',#9095,0.0024500000000844,0.000300000000050416);
#100=TOROIDAL_SURFACE('',#9097,0.00244999999982957,0.000300000000225024);
#101=TOROIDAL_SURFACE('',#9099,0.00244999999982957,0.000300000000225024);
#102=TOROIDAL_SURFACE('',#9100,0.00245000000008441,0.000300000000050426);
#103=TOROIDAL_SURFACE('',#9103,0.00245000000008441,0.000300000000050429);
#104=TOROIDAL_SURFACE('',#9106,0.00244999999982957,0.000300000000225019);
#105=TOROIDAL_SURFACE('',#9108,0.00244999999982957,0.000300000000225023);
#106=TOROIDAL_SURFACE('',#9110,0.0024500000000844,0.000300000000050417);
#107=TOROIDAL_SURFACE('',#9113,0.0236999999712056,0.000299999999854375);
#108=TOROIDAL_SURFACE('',#9117,0.0236999999712051,0.000299999999854371);
#109=TOROIDAL_SURFACE('',#9122,0.0236999999559749,0.000300000000142203);
#110=TOROIDAL_SURFACE('',#9128,0.0236999999712049,0.00029999999985436);
#111=TOROIDAL_SURFACE('',#9132,0.0236999999712049,0.000299999999854394);
#112=TOROIDAL_SURFACE('',#9136,0.0236999999850598,0.000300000000477842);
#113=TOROIDAL_SURFACE('',#9174,0.0236999999761744,0.000300000000837741);
#114=TOROIDAL_SURFACE('',#9177,0.0236999999817642,0.000300000000595368);
#115=TOROIDAL_SURFACE('',#9181,0.0236999999761741,0.000300000000837734);
#116=TOROIDAL_SURFACE('',#9184,0.0236999999761741,0.000300000000837742);
#117=TOROIDAL_SURFACE('',#9187,0.0236999999817642,0.000300000000595372);
#118=TOROIDAL_SURFACE('',#9190,0.023699999976173,0.000300000000837742);
#148=SHAPE_REPRESENTATION_RELATIONSHIP('','',#8238,#154);
#154=ADVANCED_BREP_SHAPE_REPRESENTATION('',(#8224),#18816);
#539=B_SPLINE_CURVE_WITH_KNOTS('',3,(#13902,#13903,#13904,#13905,#13906,
#13907,#13908,#13909,#13910,#13911,#13912),.UNSPECIFIED.,.F.,.F.,(4,1,1,
1,1,1,1,1,4),(1.8213390095657E-10,0.125000000151206,0.250000000120279,0.375000000089351,
0.500000000058424,0.625000000027496,0.749999999996569,0.874999999965641,
0.999999999934714),.UNSPECIFIED.);
#540=B_SPLINE_CURVE_WITH_KNOTS('',3,(#13917,#13918,#13919,#13920,#13921,
#13922,#13923,#13924,#13925,#13926,#13927),.UNSPECIFIED.,.F.,.F.,(4,1,1,
1,1,1,1,1,4),(0.,0.124999999998599,0.249999999997198,0.374999999995797,
0.499999999994396,0.624999999992995,0.749999999991595,0.874999999990194,
0.999999999988793),.UNSPECIFIED.);
#541=B_SPLINE_CURVE_WITH_KNOTS('',3,(#13934,#13935,#13936,#13937,#13938,
#13939,#13940,#13941,#13942,#13943,#13944),.UNSPECIFIED.,.F.,.F.,(4,1,1,
1,1,1,1,1,4),(0.,0.125,0.25,0.375,0.5,0.625,0.75,0.875,1.),
 .UNSPECIFIED.);
#542=B_SPLINE_CURVE_WITH_KNOTS('',3,(#13952,#13953,#13954,#13955,#13956,
#13957,#13958,#13959,#13960,#13961,#13962),.UNSPECIFIED.,.F.,.F.,(4,1,1,
1,1,1,1,1,4),(0.,0.124999999998599,0.249999999997198,0.374999999995797,
0.499999999994396,0.624999999992995,0.749999999991595,0.874999999990194,
0.999999999988793),.UNSPECIFIED.);
#543=B_SPLINE_CURVE_WITH_KNOTS('',3,(#13964,#13965,#13966,#13967,#13968,
#13969,#13970,#13971,#13972,#13973,#13974),.UNSPECIFIED.,.F.,.F.,(4,1,1,
1,1,1,1,1,4),(0.,0.125,0.25,0.375,0.5,0.625,0.75,0.875,1.),
 .UNSPECIFIED.);
#544=B_SPLINE_CURVE_WITH_KNOTS('',3,(#13977,#13978,#13979,#13980,#13981,
#13982,#13983,#13984,#13985,#13986,#13987),.UNSPECIFIED.,.F.,.F.,(4,1,1,
1,1,1,1,1,4),(0.,0.125,0.25,0.375,0.5,0.625,0.75,0.875,1.),
 .UNSPECIFIED.);
#545=B_SPLINE_CURVE_WITH_KNOTS('',3,(#13993,#13994,#13995,#13996,#13997,
#13998,#13999,#14000,#14001,#14002,#14003),.UNSPECIFIED.,.F.,.F.,(4,1,1,
1,1,1,1,1,4),(0.,0.124999999995026,0.249999999990053,0.374999999985079,
0.499999999980106,0.624999999975132,0.749999999970159,0.874999999965185,
0.999999999960211),.UNSPECIFIED.);
#546=B_SPLINE_CURVE_WITH_KNOTS('',3,(#14011,#14012,#14013,#14014),
 .UNSPECIFIED.,.F.,.F.,(4,4),(0.,1.),.UNSPECIFIED.);
#547=B_SPLINE_CURVE_WITH_KNOTS('',3,(#14018,#14019,#14020,#14021),
 .UNSPECIFIED.,.F.,.F.,(4,4),(0.,1.),.UNSPECIFIED.);
#548=B_SPLINE_CURVE_WITH_KNOTS('',3,(#14023,#14024,#14025,#14026,#14027,
#14028,#14029,#14030,#14031,#14032,#14033),.UNSPECIFIED.,.F.,.F.,(4,1,1,
1,1,1,1,1,4),(6.52855121179665E-11,0.125000000057125,0.250000000048964,
0.375000000040804,0.500000000032643,0.625000000024482,0.750000000016322,
0.875000000008161,1.),.UNSPECIFIED.);
#549=B_SPLINE_CURVE_WITH_KNOTS('',3,(#14038,#14039,#14040,#14041,#14042,
#14043,#14044,#14045,#14046,#14047,#14048),.UNSPECIFIED.,.F.,.F.,(4,1,1,
1,1,1,1,1,4),(1.12066807818024E-11,0.125000000009806,0.250000000008405,
0.375000000007004,0.500000000005603,0.625000000004202,0.750000000002802,
0.875000000001401,1.),.UNSPECIFIED.);
#550=B_SPLINE_CURVE_WITH_KNOTS('',3,(#14050,#14051,#14052,#14053),
 .UNSPECIFIED.,.F.,.F.,(4,4),(-3.98872334206739E-9,1.),.UNSPECIFIED.);
#551=B_SPLINE_CURVE_WITH_KNOTS('',3,(#14056,#14057,#14058,#14059),
 .UNSPECIFIED.,.F.,.F.,(4,4),(0.,0.999999999803539),.UNSPECIFIED.);
#552=B_SPLINE_CURVE_WITH_KNOTS('',3,(#14061,#14062,#14063,#14064,#14065,
#14066,#14067,#14068,#14069,#14070),.UNSPECIFIED.,.F.,.F.,(4,1,1,1,1,1,
1,4),(0.,0.25,0.375,0.5,0.5625,0.625,0.75,1.),.UNSPECIFIED.);
#553=B_SPLINE_CURVE_WITH_KNOTS('',3,(#14072,#14073,#14074,#14075),
 .UNSPECIFIED.,.F.,.F.,(4,4),(0.,1.),.UNSPECIFIED.);
#554=B_SPLINE_CURVE_WITH_KNOTS('',3,(#14077,#14078,#14079,#14080,#14081,
#14082,#14083,#14084,#14085,#14086),.UNSPECIFIED.,.F.,.F.,(4,1,1,1,1,1,
1,4),(0.,0.25,0.375,0.4375,0.5,0.625,0.75,1.),.UNSPECIFIED.);
#555=B_SPLINE_CURVE_WITH_KNOTS('',3,(#14088,#14089,#14090,#14091),
 .UNSPECIFIED.,.F.,.F.,(4,4),(0.,1.),.UNSPECIFIED.);
#556=B_SPLINE_CURVE_WITH_KNOTS('',3,(#14093,#14094,#14095,#14096,#14097,
#14098,#14099,#14100,#14101,#14102),.UNSPECIFIED.,.F.,.F.,(4,1,1,1,1,1,
1,4),(0.,0.25,0.375,0.5,0.5625,0.625,0.75,1.),.UNSPECIFIED.);
#557=B_SPLINE_CURVE_WITH_KNOTS('',3,(#14104,#14105,#14106,#14107),
 .UNSPECIFIED.,.F.,.F.,(4,4),(0.,1.),.UNSPECIFIED.);
#558=B_SPLINE_CURVE_WITH_KNOTS('',3,(#14109,#14110,#14111,#14112,#14113,
#14114,#14115,#14116,#14117,#14118),.UNSPECIFIED.,.F.,.F.,(4,1,1,1,1,1,
1,4),(0.,0.25,0.375,0.4375,0.5,0.625,0.75,1.),.UNSPECIFIED.);
#559=B_SPLINE_CURVE_WITH_KNOTS('',3,(#14120,#14121,#14122,#14123),
 .UNSPECIFIED.,.F.,.F.,(4,4),(0.,1.),.UNSPECIFIED.);
#560=B_SPLINE_CURVE_WITH_KNOTS('',3,(#14125,#14126,#14127,#14128,#14129,
#14130,#14131,#14132,#14133,#14134),.UNSPECIFIED.,.F.,.F.,(4,1,1,1,1,1,
1,4),(0.,0.25,0.375,0.5,0.5625,0.625,0.75,1.),.UNSPECIFIED.);
#561=B_SPLINE_CURVE_WITH_KNOTS('',3,(#14136,#14137,#14138,#14139),
 .UNSPECIFIED.,.F.,.F.,(4,4),(0.,1.),.UNSPECIFIED.);
#562=B_SPLINE_CURVE_WITH_KNOTS('',3,(#14141,#14142,#14143,#14144,#14145,
#14146,#14147,#14148,#14149,#14150),.UNSPECIFIED.,.F.,.F.,(4,1,1,1,1,1,
1,4),(0.,0.25,0.375,0.4375,0.5,0.625,0.75,1.),.UNSPECIFIED.);
#563=B_SPLINE_CURVE_WITH_KNOTS('',3,(#14154,#14155,#14156,#14157),
 .UNSPECIFIED.,.F.,.F.,(4,4),(0.,1.),.UNSPECIFIED.);
#564=B_SPLINE_CURVE_WITH_KNOTS('',3,(#14159,#14160,#14161,#14162,#14163,
#14164,#14165,#14166,#14167,#14168),.UNSPECIFIED.,.F.,.F.,(4,1,1,1,1,1,
1,4),(0.,0.25,0.375,0.5,0.5625,0.625,0.75,1.),.UNSPECIFIED.);
#565=B_SPLINE_CURVE_WITH_KNOTS('',3,(#14170,#14171,#14172,#14173),
 .UNSPECIFIED.,.F.,.F.,(4,4),(0.,1.),.UNSPECIFIED.);
#566=B_SPLINE_CURVE_WITH_KNOTS('',3,(#14175,#14176,#14177,#14178,#14179,
#14180,#14181,#14182,#14183,#14184),.UNSPECIFIED.,.F.,.F.,(4,1,1,1,1,1,
1,4),(0.,0.25,0.375,0.4375,0.5,0.625,0.75,1.),.UNSPECIFIED.);
#567=B_SPLINE_CURVE_WITH_KNOTS('',3,(#14186,#14187,#14188,#14189),
 .UNSPECIFIED.,.F.,.F.,(4,4),(0.,1.),.UNSPECIFIED.);
#568=B_SPLINE_CURVE_WITH_KNOTS('',3,(#14191,#14192,#14193,#14194,#14195,
#14196,#14197,#14198,#14199,#14200),.UNSPECIFIED.,.F.,.F.,(4,1,1,1,1,1,
1,4),(0.,0.25,0.375,0.5,0.5625,0.625,0.75,1.),.UNSPECIFIED.);
#569=B_SPLINE_CURVE_WITH_KNOTS('',3,(#14204,#14205,#14206,#14207,#14208,
#14209,#14210,#14211,#14212,#14213),.UNSPECIFIED.,.F.,.F.,(4,1,1,1,1,1,
1,4),(0.,0.25,0.375,0.4375,0.5,0.625,0.75,1.),.UNSPECIFIED.);
#570=B_SPLINE_CURVE_WITH_KNOTS('',3,(#14215,#14216,#14217,#14218),
 .UNSPECIFIED.,.F.,.F.,(4,4),(0.,1.),.UNSPECIFIED.);
#571=B_SPLINE_CURVE_WITH_KNOTS('',3,(#14220,#14221,#14222,#14223,#14224,
#14225,#14226,#14227,#14228,#14229),.UNSPECIFIED.,.F.,.F.,(4,1,1,1,1,1,
1,4),(0.,0.25,0.375,0.5,0.5625,0.625,0.75,1.),.UNSPECIFIED.);
#572=B_SPLINE_CURVE_WITH_KNOTS('',3,(#14231,#14232,#14233,#14234),
 .UNSPECIFIED.,.F.,.F.,(4,4),(0.,1.),.UNSPECIFIED.);
#573=B_SPLINE_CURVE_WITH_KNOTS('',3,(#14236,#14237,#14238,#14239,#14240,
#14241,#14242,#14243,#14244,#14245),.UNSPECIFIED.,.F.,.F.,(4,1,1,1,1,1,
1,4),(0.,0.25,0.375,0.4375,0.5,0.625,0.75,1.),.UNSPECIFIED.);
#574=B_SPLINE_CURVE_WITH_KNOTS('',3,(#14253,#14254,#14255,#14256,#14257,
#14258,#14259,#14260,#14261,#14262,#14263,#14264),.UNSPECIFIED.,.F.,.F.,
(4,1,1,1,1,1,1,1,1,4),(0.,0.25,0.5,0.625,0.75,0.8125,0.875,0.9375,0.96875,
1.),.UNSPECIFIED.);
#575=B_SPLINE_CURVE_WITH_KNOTS('',3,(#14265,#14266,#14267,#14268,#14269,
#14270,#14271,#14272,#14273,#14274,#14275,#14276,#14277),.UNSPECIFIED.,
 .F.,.F.,(4,1,1,1,1,1,1,1,1,1,4),(0.,0.015625,0.03125,0.0625,0.125,0.1875,
0.25,0.375,0.5,0.75,1.),.UNSPECIFIED.);
#576=B_SPLINE_CURVE_WITH_KNOTS('',3,(#14279,#14280,#14281,#14282),
 .UNSPECIFIED.,.F.,.F.,(4,4),(-0.000951209283696458,0.00026784888500917),
 .UNSPECIFIED.);
#577=B_SPLINE_CURVE_WITH_KNOTS('',3,(#14284,#14285,#14286,#14287,#14288),
 .UNSPECIFIED.,.F.,.F.,(4,1,4),(0.,0.499999854922505,0.99999970984501),
 .UNSPECIFIED.);
#578=B_SPLINE_CURVE_WITH_KNOTS('',3,(#14292,#14293,#14294,#14295,#14296),
 .UNSPECIFIED.,.F.,.F.,(4,1,4),(2.901447796702E-7,0.50000014507239,1.),
 .UNSPECIFIED.);
#579=B_SPLINE_CURVE_WITH_KNOTS('',3,(#14298,#14299,#14300,#14301),
 .UNSPECIFIED.,.F.,.F.,(4,4),(0.,0.00120725234162079),.UNSPECIFIED.);
#580=B_SPLINE_CURVE_WITH_KNOTS('',3,(#14303,#14304,#14305,#14306,#14307,
#14308,#14309,#14310,#14311,#14312,#14313,#14314,#14315),.UNSPECIFIED.,
 .F.,.F.,(4,1,1,1,1,1,1,1,1,1,4),(0.,0.015625,0.03125,0.0625,0.125,0.1875,
0.25,0.375,0.5,0.75,1.),.UNSPECIFIED.);
#581=B_SPLINE_CURVE_WITH_KNOTS('',3,(#14317,#14318,#14319,#14320),
 .UNSPECIFIED.,.F.,.F.,(4,4),(0.,1.),.UNSPECIFIED.);
#582=B_SPLINE_CURVE_WITH_KNOTS('',3,(#14322,#14323,#14324,#14325,#14326,
#14327,#14328,#14329,#14330,#14331,#14332,#14333),.UNSPECIFIED.,.F.,.F.,
(4,1,1,1,1,1,1,1,1,4),(0.,0.25,0.5,0.625,0.75,0.8125,0.875,0.9375,0.96875,
1.),.UNSPECIFIED.);
#583=B_SPLINE_CURVE_WITH_KNOTS('',3,(#14335,#14336,#14337,#14338),
 .UNSPECIFIED.,.F.,.F.,(4,4),(0.,0.00120749967935418),.UNSPECIFIED.);
#584=B_SPLINE_CURVE_WITH_KNOTS('',3,(#14340,#14341,#14342,#14343,#14344),
 .UNSPECIFIED.,.F.,.F.,(4,1,4),(0.,0.499999854925028,0.999999709850055),
 .UNSPECIFIED.);
#585=B_SPLINE_CURVE_WITH_KNOTS('',3,(#14348,#14349,#14350,#14351,#14352),
 .UNSPECIFIED.,.F.,.F.,(4,1,4),(2.90144772198091E-7,0.500000145072386,1.),
 .UNSPECIFIED.);
#586=B_SPLINE_CURVE_WITH_KNOTS('',3,(#14354,#14355,#14356,#14357),
 .UNSPECIFIED.,.F.,.F.,(4,4),(0.,0.00120725233944049),.UNSPECIFIED.);
#587=B_SPLINE_CURVE_WITH_KNOTS('',3,(#14359,#14360,#14361,#14362,#14363,
#14364,#14365,#14366,#14367,#14368,#14369,#14370,#14371),.UNSPECIFIED.,
 .F.,.F.,(4,1,1,1,1,1,1,1,1,1,4),(0.,0.015625,0.03125,0.0625,0.125,0.1875,
0.25,0.375,0.5,0.75,1.),.UNSPECIFIED.);
#588=B_SPLINE_CURVE_WITH_KNOTS('',3,(#14373,#14374,#14375,#14376),
 .UNSPECIFIED.,.F.,.F.,(4,4),(0.,1.),.UNSPECIFIED.);
#589=B_SPLINE_CURVE_WITH_KNOTS('',3,(#14378,#14379,#14380,#14381,#14382,
#14383,#14384,#14385,#14386,#14387,#14388,#14389),.UNSPECIFIED.,.F.,.F.,
(4,1,1,1,1,1,1,1,1,4),(0.,0.25,0.5,0.625,0.75,0.8125,0.875,0.9375,0.96875,
1.),.UNSPECIFIED.);
#590=B_SPLINE_CURVE_WITH_KNOTS('',3,(#14391,#14392,#14393,#14394),
 .UNSPECIFIED.,.F.,.F.,(4,4),(0.,0.00120749968240849),.UNSPECIFIED.);
#591=B_SPLINE_CURVE_WITH_KNOTS('',3,(#14396,#14397,#14398,#14399,#14400),
 .UNSPECIFIED.,.F.,.F.,(4,1,4),(0.,0.499999854925025,0.999999709850049),
 .UNSPECIFIED.);
#592=B_SPLINE_CURVE_WITH_KNOTS('',3,(#14404,#14405,#14406,#14407,#14408),
 .UNSPECIFIED.,.F.,.F.,(4,1,4),(2.901447750701E-7,0.500000145072388,1.),
 .UNSPECIFIED.);
#593=B_SPLINE_CURVE_WITH_KNOTS('',3,(#14410,#14411,#14412,#14413),
 .UNSPECIFIED.,.F.,.F.,(4,4),(0.,0.00120725234168436),.UNSPECIFIED.);
#594=B_SPLINE_CURVE_WITH_KNOTS('',3,(#14415,#14416,#14417,#14418,#14419),
 .UNSPECIFIED.,.F.,.F.,(4,1,4),(0.,0.5,1.),.UNSPECIFIED.);
#595=B_SPLINE_CURVE_WITH_KNOTS('',3,(#14421,#14422,#14423,#14424),
 .UNSPECIFIED.,.F.,.F.,(4,4),(-1.1112351980909E-15,1.),.UNSPECIFIED.);
#596=B_SPLINE_CURVE_WITH_KNOTS('',3,(#14428,#14429,#14430,#14431),
 .UNSPECIFIED.,.F.,.F.,(4,4),(0.,1.),.UNSPECIFIED.);
#597=B_SPLINE_CURVE_WITH_KNOTS('',3,(#14433,#14434,#14435,#14436,#14437),
 .UNSPECIFIED.,.F.,.F.,(4,1,4),(0.,0.5,1.),.UNSPECIFIED.);
#598=B_SPLINE_CURVE_WITH_KNOTS('',3,(#14439,#14440,#14441,#14442),
 .UNSPECIFIED.,.F.,.F.,(4,4),(0.,0.00120749968217001),.UNSPECIFIED.);
#599=B_SPLINE_CURVE_WITH_KNOTS('',3,(#14444,#14445,#14446,#14447,#14448),
 .UNSPECIFIED.,.F.,.F.,(4,1,4),(0.,0.49999985492503,0.999999709850059),
 .UNSPECIFIED.);
#600=B_SPLINE_CURVE_WITH_KNOTS('',3,(#14452,#14453,#14454,#14455,#14456),
 .UNSPECIFIED.,.F.,.F.,(4,1,4),(2.9014478282069E-7,0.500000145072391,1.),
 .UNSPECIFIED.);
#601=B_SPLINE_CURVE_WITH_KNOTS('',3,(#14458,#14459,#14460,#14461),
 .UNSPECIFIED.,.F.,.F.,(4,4),(0.,0.00120725234193258),.UNSPECIFIED.);
#602=B_SPLINE_CURVE_WITH_KNOTS('',3,(#14463,#14464,#14465,#14466,#14467),
 .UNSPECIFIED.,.F.,.F.,(4,1,4),(0.,0.5,1.),.UNSPECIFIED.);
#603=B_SPLINE_CURVE_WITH_KNOTS('',3,(#14469,#14470,#14471,#14472),
 .UNSPECIFIED.,.F.,.F.,(4,4),(0.,1.),.UNSPECIFIED.);
#604=B_SPLINE_CURVE_WITH_KNOTS('',3,(#14474,#14475,#14476,#14477,#14478),
 .UNSPECIFIED.,.F.,.F.,(4,1,4),(0.,0.5,1.),.UNSPECIFIED.);
#605=B_SPLINE_CURVE_WITH_KNOTS('',3,(#14480,#14481,#14482,#14483),
 .UNSPECIFIED.,.F.,.F.,(4,4),(0.,0.00120749968043747),.UNSPECIFIED.);
#606=B_SPLINE_CURVE_WITH_KNOTS('',3,(#14485,#14486,#14487,#14488,#14489),
 .UNSPECIFIED.,.F.,.F.,(4,1,4),(0.,0.499999854925027,0.999999709850054),
 .UNSPECIFIED.);
#607=B_SPLINE_CURVE_WITH_KNOTS('',3,(#14493,#14494,#14495,#14496,#14497),
 .UNSPECIFIED.,.F.,.F.,(4,1,4),(2.90144768683264E-7,0.500000145072384,1.),
 .UNSPECIFIED.);
#608=B_SPLINE_CURVE_WITH_KNOTS('',3,(#14499,#14500,#14501,#14502),
 .UNSPECIFIED.,.F.,.F.,(4,4),(0.,0.00120725233951242),.UNSPECIFIED.);
#609=B_SPLINE_CURVE_WITH_KNOTS('',3,(#14504,#14505,#14506,#14507,#14508),
 .UNSPECIFIED.,.F.,.F.,(4,1,4),(0.,0.5,1.),.UNSPECIFIED.);
#610=B_SPLINE_CURVE_WITH_KNOTS('',3,(#14510,#14511,#14512,#14513),
 .UNSPECIFIED.,.F.,.F.,(4,4),(0.,1.),.UNSPECIFIED.);
#611=B_SPLINE_CURVE_WITH_KNOTS('',3,(#14515,#14516,#14517,#14518,#14519),
 .UNSPECIFIED.,.F.,.F.,(4,1,4),(0.,0.5,1.),.UNSPECIFIED.);
#612=B_SPLINE_CURVE_WITH_KNOTS('',3,(#14521,#14522,#14523,#14524),
 .UNSPECIFIED.,.F.,.F.,(4,4),(0.,0.00120749968120778),.UNSPECIFIED.);
#613=B_SPLINE_CURVE_WITH_KNOTS('',3,(#14526,#14527,#14528,#14529,#14530),
 .UNSPECIFIED.,.F.,.F.,(4,1,4),(0.,0.499999854925025,0.999999709850049),
 .UNSPECIFIED.);
#614=B_SPLINE_CURVE_WITH_KNOTS('',3,(#14534,#14535,#14536,#14537,#14538),
 .UNSPECIFIED.,.F.,.F.,(4,1,4),(2.90149859374016E-7,0.50000014507493,1.),
 .UNSPECIFIED.);
#615=B_SPLINE_CURVE_WITH_KNOTS('',3,(#14540,#14541,#14542,#14543),
 .UNSPECIFIED.,.F.,.F.,(4,4),(-0.000265114428389933,0.000941618287195232),
 .UNSPECIFIED.);
#616=B_SPLINE_CURVE_WITH_KNOTS('',3,(#14548,#14549,#14550,#14551),
 .UNSPECIFIED.,.F.,.F.,(4,4),(0.,1.00000004166667),.UNSPECIFIED.);
#617=B_SPLINE_CURVE_WITH_KNOTS('',3,(#14553,#14554,#14555,#14556),
 .UNSPECIFIED.,.F.,.F.,(4,4),(-8.33333471783616E-8,1.),.UNSPECIFIED.);
#618=B_SPLINE_CURVE_WITH_KNOTS('',3,(#14562,#14563,#14564,#14565),
 .UNSPECIFIED.,.F.,.F.,(4,4),(0.,1.),.UNSPECIFIED.);
#619=B_SPLINE_CURVE_WITH_KNOTS('',3,(#14571,#14572,#14573,#14574),
 .UNSPECIFIED.,.F.,.F.,(4,4),(0.,1.),.UNSPECIFIED.);
#620=B_SPLINE_CURVE_WITH_KNOTS('',3,(#14580,#14581,#14582,#14583),
 .UNSPECIFIED.,.F.,.F.,(4,4),(0.,0.99999934647141),.UNSPECIFIED.);
#621=B_SPLINE_CURVE_WITH_KNOTS('',3,(#14591,#14592,#14593,#14594),
 .UNSPECIFIED.,.F.,.F.,(4,4),(0.,1.),.UNSPECIFIED.);
#622=B_SPLINE_CURVE_WITH_KNOTS('',3,(#14599,#14600,#14601,#14602),
 .UNSPECIFIED.,.F.,.F.,(4,4),(0.,0.999999345689277),.UNSPECIFIED.);
#623=B_SPLINE_CURVE_WITH_KNOTS('',3,(#14610,#14611,#14612,#14613),
 .UNSPECIFIED.,.F.,.F.,(4,4),(0.,1.),.UNSPECIFIED.);
#624=B_SPLINE_CURVE_WITH_KNOTS('',3,(#14616,#14617,#14618,#14619),
 .UNSPECIFIED.,.F.,.F.,(4,4),(0.,0.999999342822145),.UNSPECIFIED.);
#625=B_SPLINE_CURVE_WITH_KNOTS('',3,(#14627,#14628,#14629,#14630),
 .UNSPECIFIED.,.F.,.F.,(4,4),(0.,1.),.UNSPECIFIED.);
#626=B_SPLINE_CURVE_WITH_KNOTS('',3,(#14635,#14636,#14637,#14638),
 .UNSPECIFIED.,.F.,.F.,(4,4),(0.,0.999999346375954),.UNSPECIFIED.);
#627=B_SPLINE_CURVE_WITH_KNOTS('',3,(#14646,#14647,#14648,#14649),
 .UNSPECIFIED.,.F.,.F.,(4,4),(0.,1.),.UNSPECIFIED.);
#628=B_SPLINE_CURVE_WITH_KNOTS('',3,(#14654,#14655,#14656,#14657),
 .UNSPECIFIED.,.F.,.F.,(4,4),(0.,0.999999345593822),.UNSPECIFIED.);
#629=B_SPLINE_CURVE_WITH_KNOTS('',3,(#14665,#14666,#14667,#14668),
 .UNSPECIFIED.,.F.,.F.,(4,4),(0.,1.),.UNSPECIFIED.);
#630=B_SPLINE_CURVE_WITH_KNOTS('',3,(#14673,#14674,#14675,#14676),
 .UNSPECIFIED.,.F.,.F.,(4,4),(0.,0.999999342715313),.UNSPECIFIED.);
#631=B_SPLINE_CURVE_WITH_KNOTS('',3,(#14720,#14721,#14722,#14723),
 .UNSPECIFIED.,.F.,.F.,(4,4),(0.,1.),.UNSPECIFIED.);
#632=B_SPLINE_CURVE_WITH_KNOTS('',3,(#14727,#14728,#14729,#14730),
 .UNSPECIFIED.,.F.,.F.,(4,4),(-4.16666747456633E-8,1.),.UNSPECIFIED.);
#633=B_SPLINE_CURVE_WITH_KNOTS('',3,(#14732,#14733,#14734,#14735),
 .UNSPECIFIED.,.F.,.F.,(4,4),(0.,1.00000004166667),.UNSPECIFIED.);
#634=B_SPLINE_CURVE_WITH_KNOTS('',3,(#14741,#14742,#14743,#14744),
 .UNSPECIFIED.,.F.,.F.,(4,4),(0.,1.),.UNSPECIFIED.);
#635=B_SPLINE_CURVE_WITH_KNOTS('',3,(#14746,#14747,#14748,#14749),
 .UNSPECIFIED.,.F.,.F.,(4,4),(0.,1.),.UNSPECIFIED.);
#636=B_SPLINE_CURVE_WITH_KNOTS('',3,(#14753,#14754,#14755,#14756),
 .UNSPECIFIED.,.F.,.F.,(4,4),(-4.16666735891808E-8,1.),.UNSPECIFIED.);
#637=B_SPLINE_CURVE_WITH_KNOTS('',3,(#14760,#14761,#14762,#14763),
 .UNSPECIFIED.,.F.,.F.,(4,4),(0.,1.00000004166667),.UNSPECIFIED.);
#638=B_SPLINE_CURVE_WITH_KNOTS('',3,(#14767,#14768,#14769,#14770),
 .UNSPECIFIED.,.F.,.F.,(4,4),(0.,1.),.UNSPECIFIED.);
#639=B_SPLINE_CURVE_WITH_KNOTS('',3,(#14772,#14773,#14774,#14775),
 .UNSPECIFIED.,.F.,.F.,(4,4),(0.,1.),.UNSPECIFIED.);
#640=B_SPLINE_CURVE_WITH_KNOTS('',3,(#14779,#14780,#14781,#14782),
 .UNSPECIFIED.,.F.,.F.,(4,4),(-4.16666735891808E-8,1.),.UNSPECIFIED.);
#641=B_SPLINE_CURVE_WITH_KNOTS('',3,(#14786,#14787,#14788,#14789),
 .UNSPECIFIED.,.F.,.F.,(4,4),(0.,1.00000004166667),.UNSPECIFIED.);
#642=B_SPLINE_CURVE_WITH_KNOTS('',3,(#14793,#14794,#14795,#14796),
 .UNSPECIFIED.,.F.,.F.,(4,4),(0.,1.),.UNSPECIFIED.);
#643=B_SPLINE_CURVE_WITH_KNOTS('',3,(#14798,#14799,#14800,#14801),
 .UNSPECIFIED.,.F.,.F.,(4,4),(0.,1.),.UNSPECIFIED.);
#644=B_SPLINE_CURVE_WITH_KNOTS('',3,(#14805,#14806,#14807,#14808),
 .UNSPECIFIED.,.F.,.F.,(4,4),(-4.16666747456633E-8,1.),.UNSPECIFIED.);
#645=B_SPLINE_CURVE_WITH_KNOTS('',3,(#14812,#14813,#14814,#14815),
 .UNSPECIFIED.,.F.,.F.,(4,4),(0.,1.00000004166667),.UNSPECIFIED.);
#646=B_SPLINE_CURVE_WITH_KNOTS('',3,(#14819,#14820,#14821,#14822),
 .UNSPECIFIED.,.F.,.F.,(4,4),(0.,1.),.UNSPECIFIED.);
#647=B_SPLINE_CURVE_WITH_KNOTS('',3,(#14824,#14825,#14826,#14827),
 .UNSPECIFIED.,.F.,.F.,(4,4),(0.,1.),.UNSPECIFIED.);
#648=B_SPLINE_CURVE_WITH_KNOTS('',3,(#14831,#14832,#14833,#14834),
 .UNSPECIFIED.,.F.,.F.,(4,4),(-4.16666735891808E-8,1.),.UNSPECIFIED.);
#649=B_SPLINE_CURVE_WITH_KNOTS('',3,(#14836,#14837,#14838,#14839),
 .UNSPECIFIED.,.F.,.F.,(4,4),(0.,1.00000004166667),.UNSPECIFIED.);
#650=B_SPLINE_CURVE_WITH_KNOTS('',3,(#14845,#14846,#14847,#14848),
 .UNSPECIFIED.,.F.,.F.,(4,4),(0.,1.),.UNSPECIFIED.);
#651=B_SPLINE_CURVE_WITH_KNOTS('',3,(#14852,#14853,#14854,#14855),
 .UNSPECIFIED.,.F.,.F.,(4,4),(0.,1.),.UNSPECIFIED.);
#652=B_SPLINE_CURVE_WITH_KNOTS('',3,(#14860,#14861,#14862,#14863,#14864,
#14865,#14866,#14867,#14868,#14869,#14870),.UNSPECIFIED.,.F.,.F.,(4,1,1,
1,1,1,1,1,4),(2.37189194415179E-10,0.125000000203968,0.250000000170747,
0.375000000137525,0.500000000104304,0.625000000071083,0.750000000037861,
0.87500000000464,0.999999999971419),.UNSPECIFIED.);
#653=B_SPLINE_CURVE_WITH_KNOTS('',3,(#14879,#14880,#14881,#14882),
 .UNSPECIFIED.,.F.,.F.,(4,4),(0.,0.999999613428237),.UNSPECIFIED.);
#654=B_SPLINE_CURVE_WITH_KNOTS('',3,(#14883,#14884,#14885,#14886),
 .UNSPECIFIED.,.F.,.F.,(4,4),(0.,1.),.UNSPECIFIED.);
#655=B_SPLINE_CURVE_WITH_KNOTS('',3,(#14891,#14892,#14893,#14894),
 .UNSPECIFIED.,.F.,.F.,(4,4),(0.,1.),.UNSPECIFIED.);
#656=B_SPLINE_CURVE_WITH_KNOTS('',3,(#14902,#14903,#14904,#14905),
 .UNSPECIFIED.,.F.,.F.,(4,4),(0.,1.),.UNSPECIFIED.);
#657=B_SPLINE_CURVE_WITH_KNOTS('',3,(#14906,#14907,#14908,#14909),
 .UNSPECIFIED.,.F.,.F.,(4,4),(0.,1.),.UNSPECIFIED.);
#658=B_SPLINE_CURVE_WITH_KNOTS('',3,(#14917,#14918,#14919,#14920),
 .UNSPECIFIED.,.F.,.F.,(4,4),(0.,1.),.UNSPECIFIED.);
#659=B_SPLINE_CURVE_WITH_KNOTS('',3,(#14921,#14922,#14923,#14924),
 .UNSPECIFIED.,.F.,.F.,(4,4),(0.,1.),.UNSPECIFIED.);
#660=B_SPLINE_CURVE_WITH_KNOTS('',3,(#14932,#14933,#14934,#14935),
 .UNSPECIFIED.,.F.,.F.,(4,4),(0.,1.),.UNSPECIFIED.);
#661=B_SPLINE_CURVE_WITH_KNOTS('',3,(#14936,#14937,#14938,#14939),
 .UNSPECIFIED.,.F.,.F.,(4,4),(0.,1.),.UNSPECIFIED.);
#662=B_SPLINE_CURVE_WITH_KNOTS('',3,(#14947,#14948,#14949,#14950),
 .UNSPECIFIED.,.F.,.F.,(4,4),(0.,1.),.UNSPECIFIED.);
#663=B_SPLINE_CURVE_WITH_KNOTS('',3,(#14954,#14955,#14956,#14957),
 .UNSPECIFIED.,.F.,.F.,(4,4),(0.,1.),.UNSPECIFIED.);
#664=B_SPLINE_CURVE_WITH_KNOTS('',3,(#14958,#14959,#14960,#14961),
 .UNSPECIFIED.,.F.,.F.,(4,4),(0.,1.),.UNSPECIFIED.);
#665=B_SPLINE_CURVE_WITH_KNOTS('',3,(#15003,#15004,#15005,#15006),
 .UNSPECIFIED.,.F.,.F.,(4,4),(4.16666666447352E-8,1.),.UNSPECIFIED.);
#666=B_SPLINE_CURVE_WITH_KNOTS('',3,(#15026,#15027,#15028,#15029),
 .UNSPECIFIED.,.F.,.F.,(4,4),(4.16666666447352E-8,1.),.UNSPECIFIED.);
#667=B_SPLINE_CURVE_WITH_KNOTS('',3,(#15031,#15032,#15033,#15034),
 .UNSPECIFIED.,.F.,.F.,(4,4),(0.,1.),.UNSPECIFIED.);
#668=B_SPLINE_CURVE_WITH_KNOTS('',3,(#15036,#15037,#15038,#15039),
 .UNSPECIFIED.,.F.,.F.,(4,4),(0.,1.),.UNSPECIFIED.);
#669=B_SPLINE_CURVE_WITH_KNOTS('',3,(#15041,#15042,#15043,#15044),
 .UNSPECIFIED.,.F.,.F.,(4,4),(0.,1.),.UNSPECIFIED.);
#670=B_SPLINE_CURVE_WITH_KNOTS('',3,(#15047,#15048,#15049,#15050),
 .UNSPECIFIED.,.F.,.F.,(4,4),(4.16666666447351E-8,1.),.UNSPECIFIED.);
#671=B_SPLINE_CURVE_WITH_KNOTS('',3,(#15052,#15053,#15054,#15055),
 .UNSPECIFIED.,.F.,.F.,(4,4),(0.,1.),.UNSPECIFIED.);
#672=B_SPLINE_CURVE_WITH_KNOTS('',3,(#15057,#15058,#15059,#15060),
 .UNSPECIFIED.,.F.,.F.,(4,4),(0.,1.),.UNSPECIFIED.);
#673=B_SPLINE_CURVE_WITH_KNOTS('',3,(#15062,#15063,#15064,#15065),
 .UNSPECIFIED.,.F.,.F.,(4,4),(0.,1.),.UNSPECIFIED.);
#674=B_SPLINE_CURVE_WITH_KNOTS('',3,(#15068,#15069,#15070,#15071),
 .UNSPECIFIED.,.F.,.F.,(4,4),(0.,1.),.UNSPECIFIED.);
#675=B_SPLINE_CURVE_WITH_KNOTS('',3,(#15073,#15074,#15075,#15076),
 .UNSPECIFIED.,.F.,.F.,(4,4),(0.,1.),.UNSPECIFIED.);
#676=B_SPLINE_CURVE_WITH_KNOTS('',3,(#15078,#15079,#15080,#15081),
 .UNSPECIFIED.,.F.,.F.,(4,4),(0.,1.),.UNSPECIFIED.);
#677=B_SPLINE_CURVE_WITH_KNOTS('',3,(#15084,#15085,#15086,#15087),
 .UNSPECIFIED.,.F.,.F.,(4,4),(4.16666666447352E-8,1.),.UNSPECIFIED.);
#678=B_SPLINE_CURVE_WITH_KNOTS('',3,(#15089,#15090,#15091,#15092),
 .UNSPECIFIED.,.F.,.F.,(4,4),(0.,1.),.UNSPECIFIED.);
#679=B_SPLINE_CURVE_WITH_KNOTS('',3,(#15094,#15095,#15096,#15097),
 .UNSPECIFIED.,.F.,.F.,(4,4),(0.,1.),.UNSPECIFIED.);
#680=B_SPLINE_CURVE_WITH_KNOTS('',3,(#15099,#15100,#15101,#15102),
 .UNSPECIFIED.,.F.,.F.,(4,4),(0.,1.),.UNSPECIFIED.);
#681=B_SPLINE_CURVE_WITH_KNOTS('',3,(#15105,#15106,#15107,#15108),
 .UNSPECIFIED.,.F.,.F.,(4,4),(4.16666666447351E-8,1.),.UNSPECIFIED.);
#682=B_SPLINE_CURVE_WITH_KNOTS('',3,(#15110,#15111,#15112,#15113),
 .UNSPECIFIED.,.F.,.F.,(4,4),(0.,1.),.UNSPECIFIED.);
#683=B_SPLINE_CURVE_WITH_KNOTS('',3,(#15115,#15116,#15117,#15118),
 .UNSPECIFIED.,.F.,.F.,(4,4),(0.,1.),.UNSPECIFIED.);
#684=B_SPLINE_CURVE_WITH_KNOTS('',3,(#15120,#15121,#15122,#15123),
 .UNSPECIFIED.,.F.,.F.,(4,4),(0.,1.),.UNSPECIFIED.);
#685=B_SPLINE_CURVE_WITH_KNOTS('',3,(#15126,#15127,#15128,#15129),
 .UNSPECIFIED.,.F.,.F.,(4,4),(4.16666666447352E-8,1.),.UNSPECIFIED.);
#686=B_SPLINE_CURVE_WITH_KNOTS('',3,(#15131,#15132,#15133,#15134),
 .UNSPECIFIED.,.F.,.F.,(4,4),(0.,1.),.UNSPECIFIED.);
#687=B_SPLINE_CURVE_WITH_KNOTS('',3,(#15136,#15137,#15138,#15139),
 .UNSPECIFIED.,.F.,.F.,(4,4),(0.,1.),.UNSPECIFIED.);
#688=B_SPLINE_CURVE_WITH_KNOTS('',3,(#15141,#15142,#15143,#15144),
 .UNSPECIFIED.,.F.,.F.,(4,4),(0.,1.),.UNSPECIFIED.);
#689=B_SPLINE_CURVE_WITH_KNOTS('',3,(#15150,#15151,#15152,#15153,#15154,
#15155,#15156,#15157,#15158,#15159,#15160),.UNSPECIFIED.,.F.,.F.,(4,1,1,
1,1,1,1,1,4),(1.82133860695804E-10,0.125000000151206,0.250000000120279,
0.375000000089351,0.500000000058424,0.625000000027496,0.749999999996569,
0.874999999965641,0.999999999934714),.UNSPECIFIED.);
#690=B_SPLINE_CURVE_WITH_KNOTS('',3,(#15165,#15166,#15167,#15168,#15169,
#15170,#15171,#15172,#15173,#15174,#15175),.UNSPECIFIED.,.F.,.F.,(4,1,1,
1,1,1,1,1,4),(0.,0.125,0.25,0.375,0.5,0.625,0.75,0.875,1.),
 .UNSPECIFIED.);
#691=B_SPLINE_CURVE_WITH_KNOTS('',3,(#15180,#15181,#15182,#15183,#15184,
#15185,#15186,#15187,#15188,#15189,#15190),.UNSPECIFIED.,.F.,.F.,(4,1,1,
1,1,1,1,1,4),(1.08557388758105E-10,0.125000000084605,0.250000000060653,
0.375000000036701,0.500000000012749,0.624999999988797,0.749999999964844,
0.874999999940892,0.99999999991694),.UNSPECIFIED.);
#692=B_SPLINE_CURVE_WITH_KNOTS('',3,(#15195,#15196,#15197,#15198,#15199,
#15200,#15201,#15202,#15203,#15204,#15205),.UNSPECIFIED.,.F.,.F.,(4,1,1,
1,1,1,1,1,4),(2.37189827595616E-10,0.125000000203968,0.250000000170747,
0.375000000137525,0.500000000104304,0.625000000071082,0.750000000037861,
0.875000000004639,0.999999999971418),.UNSPECIFIED.);
#693=B_SPLINE_CURVE_WITH_KNOTS('',3,(#15214,#15215,#15216,#15217,#15218,
#15219,#15220,#15221,#15222,#15223,#15224),.UNSPECIFIED.,.F.,.F.,(4,1,1,
1,1,1,1,1,4),(0.,0.124999999998599,0.249999999997198,0.374999999995797,
0.499999999994397,0.624999999992996,0.749999999991595,0.874999999990194,
0.999999999988793),.UNSPECIFIED.);
#694=B_SPLINE_CURVE_WITH_KNOTS('',3,(#15229,#15230,#15231,#15232),
 .UNSPECIFIED.,.F.,.F.,(4,4),(0.,1.),.UNSPECIFIED.);
#695=B_SPLINE_CURVE_WITH_KNOTS('',3,(#15236,#15237,#15238,#15239),
 .UNSPECIFIED.,.F.,.F.,(4,4),(0.,1.),.UNSPECIFIED.);
#696=B_SPLINE_CURVE_WITH_KNOTS('',3,(#15243,#15244,#15245,#15246),
 .UNSPECIFIED.,.F.,.F.,(4,4),(0.,0.999999991856635),.UNSPECIFIED.);
#697=B_SPLINE_CURVE_WITH_KNOTS('',3,(#15250,#15251,#15252,#15253),
 .UNSPECIFIED.,.F.,.F.,(4,4),(0.,1.),.UNSPECIFIED.);
#698=B_SPLINE_CURVE_WITH_KNOTS('',3,(#15257,#15258,#15259,#15260),
 .UNSPECIFIED.,.F.,.F.,(4,4),(0.,1.),.UNSPECIFIED.);
#699=B_SPLINE_CURVE_WITH_KNOTS('',3,(#15264,#15265,#15266,#15267),
 .UNSPECIFIED.,.F.,.F.,(4,4),(8.91275946058781E-10,1.),.UNSPECIFIED.);
#700=B_SPLINE_CURVE_WITH_KNOTS('',3,(#15271,#15272,#15273,#15274),
 .UNSPECIFIED.,.F.,.F.,(4,4),(0.,0.999999991166321),.UNSPECIFIED.);
#701=B_SPLINE_CURVE_WITH_KNOTS('',3,(#15278,#15279,#15280,#15281),
 .UNSPECIFIED.,.F.,.F.,(4,4),(0.,1.),.UNSPECIFIED.);
#702=B_SPLINE_CURVE_WITH_KNOTS('',3,(#15285,#15286,#15287,#15288),
 .UNSPECIFIED.,.F.,.F.,(4,4),(0.,0.999999991635845),.UNSPECIFIED.);
#703=B_SPLINE_CURVE_WITH_KNOTS('',3,(#15292,#15293,#15294,#15295),
 .UNSPECIFIED.,.F.,.F.,(4,4),(0.,1.),.UNSPECIFIED.);
#704=B_SPLINE_CURVE_WITH_KNOTS('',3,(#15299,#15300,#15301,#15302),
 .UNSPECIFIED.,.F.,.F.,(4,4),(0.,0.999999990695087),.UNSPECIFIED.);
#705=B_SPLINE_CURVE_WITH_KNOTS('',3,(#15306,#15307,#15308,#15309),
 .UNSPECIFIED.,.F.,.F.,(4,4),(6.70478438173798E-10,1.),.UNSPECIFIED.);
#706=B_SPLINE_CURVE_WITH_KNOTS('',3,(#15329,#15330,#15331,#15332),
 .UNSPECIFIED.,.F.,.F.,(4,4),(0.,1.),.UNSPECIFIED.);
#707=B_SPLINE_CURVE_WITH_KNOTS('',3,(#15334,#15335,#15336,#15337),
 .UNSPECIFIED.,.F.,.F.,(4,4),(3.58215183541293E-10,0.000343052456161631),
 .UNSPECIFIED.);
#708=B_SPLINE_CURVE_WITH_KNOTS('',3,(#15339,#15340,#15341,#15342),
 .UNSPECIFIED.,.F.,.F.,(4,4),(3.65096538768038E-8,0.999999982920268),
 .UNSPECIFIED.);
#709=B_SPLINE_CURVE_WITH_KNOTS('',3,(#15344,#15345,#15346,#15347),
 .UNSPECIFIED.,.F.,.F.,(4,4),(0.,0.000343052524018004),.UNSPECIFIED.);
#710=B_SPLINE_CURVE_WITH_KNOTS('',3,(#15349,#15350,#15351,#15352),
 .UNSPECIFIED.,.F.,.F.,(4,4),(0.,1.),.UNSPECIFIED.);
#711=B_SPLINE_CURVE_WITH_KNOTS('',3,(#15354,#15355,#15356,#15357),
 .UNSPECIFIED.,.F.,.F.,(4,4),(3.26629103003972E-10,0.000343052385686348),
 .UNSPECIFIED.);
#712=B_SPLINE_CURVE_WITH_KNOTS('',3,(#15361,#15362,#15363,#15364),
 .UNSPECIFIED.,.F.,.F.,(4,4),(0.,0.000343052455136989),.UNSPECIFIED.);
#713=B_SPLINE_CURVE_WITH_KNOTS('',3,(#15366,#15367,#15368,#15369),
 .UNSPECIFIED.,.F.,.F.,(4,4),(0.,0.999999999067061),.UNSPECIFIED.);
#714=B_SPLINE_CURVE_WITH_KNOTS('',3,(#15371,#15372,#15373,#15374),
 .UNSPECIFIED.,.F.,.F.,(4,4),(3.60835728632106E-10,0.000343052452422124),
 .UNSPECIFIED.);
#715=B_SPLINE_CURVE_WITH_KNOTS('',3,(#15376,#15377,#15378,#15379),
 .UNSPECIFIED.,.F.,.F.,(4,4),(3.41089703588926E-8,0.999999981759078),
 .UNSPECIFIED.);
#716=B_SPLINE_CURVE_WITH_KNOTS('',3,(#15381,#15382,#15383,#15384),
 .UNSPECIFIED.,.F.,.F.,(4,4),(0.,0.000343052525875007),.UNSPECIFIED.);
#717=B_SPLINE_CURVE_WITH_KNOTS('',3,(#15386,#15387,#15388,#15389),
 .UNSPECIFIED.,.F.,.F.,(4,4),(0.,0.999999997808727),.UNSPECIFIED.);
#718=B_SPLINE_CURVE_WITH_KNOTS('',3,(#15393,#15394,#15395,#15396),
 .UNSPECIFIED.,.F.,.F.,(4,4),(0.,0.000343052525807486),.UNSPECIFIED.);
#719=B_SPLINE_CURVE_WITH_KNOTS('',3,(#15399,#15400,#15401,#15402),
 .UNSPECIFIED.,.F.,.F.,(4,4),(0.,0.999999998658949),.UNSPECIFIED.);
#720=B_SPLINE_CURVE_WITH_KNOTS('',3,(#15403,#15404,#15405,#15406),
 .UNSPECIFIED.,.F.,.F.,(4,4),(0.,0.99999999962777),.UNSPECIFIED.);
#721=B_SPLINE_CURVE_WITH_KNOTS('',3,(#15408,#15409,#15410,#15411),
 .UNSPECIFIED.,.F.,.F.,(4,4),(3.57901911661657E-10,0.000343052455535201),
 .UNSPECIFIED.);
#722=B_SPLINE_CURVE_WITH_KNOTS('',3,(#15413,#15414,#15415,#15416),
 .UNSPECIFIED.,.F.,.F.,(4,4),(3.64646145125801E-8,0.999999982935945),
 .UNSPECIFIED.);
#723=B_SPLINE_CURVE_WITH_KNOTS('',3,(#15418,#15419,#15420,#15421),
 .UNSPECIFIED.,.F.,.F.,(4,4),(0.,0.000343052484606286),.UNSPECIFIED.);
#724=B_SPLINE_CURVE_WITH_KNOTS('',3,(#15423,#15424,#15425,#15426),
 .UNSPECIFIED.,.F.,.F.,(4,4),(0.,0.999999999941115),.UNSPECIFIED.);
#725=B_SPLINE_CURVE_WITH_KNOTS('',3,(#15428,#15429,#15430,#15431),
 .UNSPECIFIED.,.F.,.F.,(4,4),(3.61573077407582E-10,0.000343052449740987),
 .UNSPECIFIED.);
#726=B_SPLINE_CURVE_WITH_KNOTS('',3,(#15433,#15434,#15435,#15436),
 .UNSPECIFIED.,.F.,.F.,(4,4),(3.74094535835276E-8,0.999999981302811),
 .UNSPECIFIED.);
#727=B_SPLINE_CURVE_WITH_KNOTS('',3,(#15438,#15439,#15440,#15441),
 .UNSPECIFIED.,.F.,.F.,(4,4),(0.,0.000343052521102341),.UNSPECIFIED.);
#728=B_SPLINE_CURVE_WITH_KNOTS('',3,(#15443,#15444,#15445,#15446),
 .UNSPECIFIED.,.F.,.F.,(4,4),(0.,0.999999999492176),.UNSPECIFIED.);
#729=B_SPLINE_CURVE_WITH_KNOTS('',3,(#15448,#15449,#15450,#15451),
 .UNSPECIFIED.,.F.,.F.,(4,4),(3.60479596378399E-10,0.000343052451752998),
 .UNSPECIFIED.);
#730=B_SPLINE_CURVE_WITH_KNOTS('',3,(#15453,#15454,#15455,#15456),
 .UNSPECIFIED.,.F.,.F.,(4,4),(3.41403005359674E-8,0.999999981774713),
 .UNSPECIFIED.);
#731=B_SPLINE_CURVE_WITH_KNOTS('',3,(#15461,#15462,#15463,#15464,#15465),
 .UNSPECIFIED.,.F.,.F.,(4,1,4),(0.,0.5,1.),.UNSPECIFIED.);
#732=B_SPLINE_CURVE_WITH_KNOTS('',3,(#15470,#15471,#15472,#15473),
 .UNSPECIFIED.,.F.,.F.,(4,4),(0.,1.),.UNSPECIFIED.);
#733=B_SPLINE_CURVE_WITH_KNOTS('',3,(#15474,#15475,#15476,#15477),
 .UNSPECIFIED.,.F.,.F.,(4,4),(0.,1.),.UNSPECIFIED.);
#734=B_SPLINE_CURVE_WITH_KNOTS('',3,(#15479,#15480,#15481,#15482,#15483,
#15484,#15485),.UNSPECIFIED.,.F.,.F.,(4,1,1,1,4),(-2.56869318007201E-15,
0.249999999983678,0.499999999967359,0.749999999951039,0.99999999993472),
 .UNSPECIFIED.);
#735=B_SPLINE_CURVE_WITH_KNOTS('',3,(#15487,#15488,#15489,#15490),
 .UNSPECIFIED.,.F.,.F.,(4,4),(0.,0.999999999325284),.UNSPECIFIED.);
#736=B_SPLINE_CURVE_WITH_KNOTS('',3,(#15497,#15498,#15499,#15500,#15501),
 .UNSPECIFIED.,.F.,.F.,(4,1,4),(0.,0.5,1.),.UNSPECIFIED.);
#737=B_SPLINE_CURVE_WITH_KNOTS('',3,(#15511,#15512,#15513,#15514),
 .UNSPECIFIED.,.F.,.F.,(4,4),(0.,1.),.UNSPECIFIED.);
#738=B_SPLINE_CURVE_WITH_KNOTS('',3,(#15515,#15516,#15517,#15518),
 .UNSPECIFIED.,.F.,.F.,(4,4),(0.,1.),.UNSPECIFIED.);
#739=B_SPLINE_CURVE_WITH_KNOTS('',3,(#15522,#15523,#15524,#15525,#15526),
 .UNSPECIFIED.,.F.,.F.,(4,1,4),(0.,0.5,1.),.UNSPECIFIED.);
#740=B_SPLINE_CURVE_WITH_KNOTS('',3,(#15531,#15532,#15533,#15534),
 .UNSPECIFIED.,.F.,.F.,(4,4),(2.19687401555071E-9,0.00876797316768544),
 .UNSPECIFIED.);
#741=B_SPLINE_CURVE_WITH_KNOTS('',3,(#15536,#15537,#15538,#15539),
 .UNSPECIFIED.,.F.,.F.,(4,4),(0.,0.999999810914528),.UNSPECIFIED.);
#742=B_SPLINE_CURVE_WITH_KNOTS('',3,(#15541,#15542,#15543,#15544),
 .UNSPECIFIED.,.F.,.F.,(4,4),(1.5598153650561E-11,0.000115526634783486),
 .UNSPECIFIED.);
#743=B_SPLINE_CURVE_WITH_KNOTS('',3,(#15545,#15546,#15547,#15548),
 .UNSPECIFIED.,.F.,.F.,(4,4),(2.45933409031924E-8,1.),.UNSPECIFIED.);
#744=B_SPLINE_CURVE_WITH_KNOTS('',3,(#15550,#15551,#15552,#15553),
 .UNSPECIFIED.,.F.,.F.,(4,4),(0.,0.000461780122359631),.UNSPECIFIED.);
#745=B_SPLINE_CURVE_WITH_KNOTS('',3,(#15555,#15556,#15557,#15558),
 .UNSPECIFIED.,.F.,.F.,(4,4),(1.86650584960977E-10,0.999999999799147),
 .UNSPECIFIED.);
#746=B_SPLINE_CURVE_WITH_KNOTS('',3,(#15560,#15561,#15562,#15563),
 .UNSPECIFIED.,.F.,.F.,(4,4),(-0.000178154369988799,0.000282469411184293),
 .UNSPECIFIED.);
#747=B_SPLINE_CURVE_WITH_KNOTS('',3,(#15565,#15566,#15567,#15568),
 .UNSPECIFIED.,.F.,.F.,(4,4),(0.,0.000115526639299657),.UNSPECIFIED.);
#748=B_SPLINE_CURVE_WITH_KNOTS('',3,(#15570,#15571,#15572,#15573),
 .UNSPECIFIED.,.F.,.F.,(4,4),(3.53200758195611E-7,1.),.UNSPECIFIED.);
#749=B_SPLINE_CURVE_WITH_KNOTS('',3,(#15575,#15576,#15577,#15578),
 .UNSPECIFIED.,.F.,.F.,(4,4),(0.,0.00876797281533553),.UNSPECIFIED.);
#750=B_SPLINE_CURVE_WITH_KNOTS('',3,(#15579,#15580,#15581,#15582),
 .UNSPECIFIED.,.F.,.F.,(4,4),(1.21975118277068E-8,0.999999969283181),
 .UNSPECIFIED.);
#751=B_SPLINE_CURVE_WITH_KNOTS('',3,(#15584,#15585,#15586,#15587),
 .UNSPECIFIED.,.F.,.F.,(4,4),(0.,1.),.UNSPECIFIED.);
#752=B_SPLINE_CURVE_WITH_KNOTS('',3,(#15589,#15590,#15591,#15592),
 .UNSPECIFIED.,.F.,.F.,(4,4),(2.19679543549726E-9,0.00876797316357997),
 .UNSPECIFIED.);
#753=B_SPLINE_CURVE_WITH_KNOTS('',3,(#15594,#15595,#15596,#15597),
 .UNSPECIFIED.,.F.,.F.,(4,4),(0.,0.99999981091663),.UNSPECIFIED.);
#754=B_SPLINE_CURVE_WITH_KNOTS('',3,(#15599,#15600,#15601,#15602),
 .UNSPECIFIED.,.F.,.F.,(4,4),(1.36153440382503E-11,0.000115526633265117),
 .UNSPECIFIED.);
#755=B_SPLINE_CURVE_WITH_KNOTS('',3,(#15604,#15605,#15606,#15607),
 .UNSPECIFIED.,.F.,.F.,(4,4),(0.,0.000461390340959227),.UNSPECIFIED.);
#756=B_SPLINE_CURVE_WITH_KNOTS('',3,(#15609,#15610,#15611,#15612),
 .UNSPECIFIED.,.F.,.F.,(4,4),(6.51238540302813E-9,0.999999991006167),
 .UNSPECIFIED.);
#757=B_SPLINE_CURVE_WITH_KNOTS('',3,(#15614,#15615,#15616,#15617),
 .UNSPECIFIED.,.F.,.F.,(4,4),(4.44834970861248E-11,0.000461780122269224),
 .UNSPECIFIED.);
#758=B_SPLINE_CURVE_WITH_KNOTS('',3,(#15619,#15620,#15621,#15622),
 .UNSPECIFIED.,.F.,.F.,(4,4),(0.,0.000115526639624777),.UNSPECIFIED.);
#759=B_SPLINE_CURVE_WITH_KNOTS('',3,(#15624,#15625,#15626,#15627),
 .UNSPECIFIED.,.F.,.F.,(4,4),(3.53210884617722E-7,1.),.UNSPECIFIED.);
#760=B_SPLINE_CURVE_WITH_KNOTS('',3,(#15629,#15630,#15631,#15632),
 .UNSPECIFIED.,.F.,.F.,(4,4),(0.,0.00876797281938125),.UNSPECIFIED.);
#761=B_SPLINE_CURVE_WITH_KNOTS('',3,(#15633,#15634,#15635,#15636),
 .UNSPECIFIED.,.F.,.F.,(4,4),(0.,0.999999969357093),.UNSPECIFIED.);
#762=B_SPLINE_CURVE_WITH_KNOTS('',3,(#15638,#15639,#15640,#15641),
 .UNSPECIFIED.,.F.,.F.,(4,4),(0.,1.),.UNSPECIFIED.);
#763=B_SPLINE_CURVE_WITH_KNOTS('',3,(#15643,#15644,#15645,#15646),
 .UNSPECIFIED.,.F.,.F.,(4,4),(7.85920675138078E-11,0.000507167122736054),
 .UNSPECIFIED.);
#764=B_SPLINE_CURVE_WITH_KNOTS('',3,(#15648,#15649,#15650,#15651),
 .UNSPECIFIED.,.F.,.F.,(4,4),(0.,1.),.UNSPECIFIED.);
#765=B_SPLINE_CURVE_WITH_KNOTS('',3,(#15659,#15660,#15661,#15662),
 .UNSPECIFIED.,.F.,.F.,(4,4),(4.44935875990053E-11,0.000461780122658492),
 .UNSPECIFIED.);
#766=B_SPLINE_CURVE_WITH_KNOTS('',3,(#15664,#15665,#15666,#15667),
 .UNSPECIFIED.,.F.,.F.,(4,4),(0.,0.000115526643526207),.UNSPECIFIED.);
#767=B_SPLINE_CURVE_WITH_KNOTS('',3,(#15669,#15670,#15671,#15672),
 .UNSPECIFIED.,.F.,.F.,(4,4),(1.21975111506088E-8,0.999999969326361),
 .UNSPECIFIED.);
#768=B_SPLINE_CURVE_WITH_KNOTS('',3,(#15673,#15674,#15675,#15676),
 .UNSPECIFIED.,.F.,.F.,(4,4),(3.53216997744741E-7,1.),.UNSPECIFIED.);
#769=B_SPLINE_CURVE_WITH_KNOTS('',3,(#15678,#15679,#15680,#15681),
 .UNSPECIFIED.,.F.,.F.,(4,4),(0.,0.00876797288604423),.UNSPECIFIED.);
#770=B_SPLINE_CURVE_WITH_KNOTS('',3,(#15683,#15684,#15685,#15686),
 .UNSPECIFIED.,.F.,.F.,(4,4),(0.,1.),.UNSPECIFIED.);
#771=B_SPLINE_CURVE_WITH_KNOTS('',3,(#15688,#15689,#15690,#15691),
 .UNSPECIFIED.,.F.,.F.,(4,4),(2.19806870576548E-9,0.00876797316802286),
 .UNSPECIFIED.);
#772=B_SPLINE_CURVE_WITH_KNOTS('',3,(#15693,#15694,#15695,#15696),
 .UNSPECIFIED.,.F.,.F.,(4,4),(0.,0.999999810910841),.UNSPECIFIED.);
#773=B_SPLINE_CURVE_WITH_KNOTS('',3,(#15698,#15699,#15700,#15701),
 .UNSPECIFIED.,.F.,.F.,(4,4),(1.55981466010636E-11,0.000115526634759396),
 .UNSPECIFIED.);
#774=B_SPLINE_CURVE_WITH_KNOTS('',3,(#15703,#15704,#15705,#15706),
 .UNSPECIFIED.,.F.,.F.,(4,4),(0.,0.000461780122378384),.UNSPECIFIED.);
#775=B_SPLINE_CURVE_WITH_KNOTS('',3,(#15708,#15709,#15710,#15711),
 .UNSPECIFIED.,.F.,.F.,(4,4),(2.06223918325493E-10,0.999999990931219),
 .UNSPECIFIED.);
#776=B_SPLINE_CURVE_WITH_KNOTS('',3,(#15713,#15714,#15715,#15716),
 .UNSPECIFIED.,.F.,.F.,(4,4),(4.45944620771068E-11,0.000461780122150718),
 .UNSPECIFIED.);
#777=B_SPLINE_CURVE_WITH_KNOTS('',3,(#15718,#15719,#15720,#15721),
 .UNSPECIFIED.,.F.,.F.,(4,4),(0.,0.000115526634772737),.UNSPECIFIED.);
#778=B_SPLINE_CURVE_WITH_KNOTS('',3,(#15723,#15724,#15725,#15726),
 .UNSPECIFIED.,.F.,.F.,(4,4),(3.53260322116059E-7,1.),.UNSPECIFIED.);
#779=B_SPLINE_CURVE_WITH_KNOTS('',3,(#15728,#15729,#15730,#15731),
 .UNSPECIFIED.,.F.,.F.,(4,4),(0.,0.0087679728154019),.UNSPECIFIED.);
#780=B_SPLINE_CURVE_WITH_KNOTS('',3,(#15732,#15733,#15734,#15735),
 .UNSPECIFIED.,.F.,.F.,(4,4),(1.21975118277068E-8,0.999999969283181),
 .UNSPECIFIED.);
#781=B_SPLINE_CURVE_WITH_KNOTS('',3,(#15737,#15738,#15739,#15740),
 .UNSPECIFIED.,.F.,.F.,(4,4),(0.,1.),.UNSPECIFIED.);
#782=B_SPLINE_CURVE_WITH_KNOTS('',3,(#15742,#15743,#15744,#15745),
 .UNSPECIFIED.,.F.,.F.,(4,4),(2.19700664975534E-9,0.00876797316368185),
 .UNSPECIFIED.);
#783=B_SPLINE_CURVE_WITH_KNOTS('',3,(#15747,#15748,#15749,#15750),
 .UNSPECIFIED.,.F.,.F.,(4,4),(0.,0.999999810875566),.UNSPECIFIED.);
#784=B_SPLINE_CURVE_WITH_KNOTS('',3,(#15752,#15753,#15754,#15755),
 .UNSPECIFIED.,.F.,.F.,(4,4),(1.36153488748495E-11,0.000115526628722257),
 .UNSPECIFIED.);
#785=B_SPLINE_CURVE_WITH_KNOTS('',3,(#15757,#15758,#15759,#15760),
 .UNSPECIFIED.,.F.,.F.,(4,4),(0.,0.000461780122286861),.UNSPECIFIED.);
#786=B_SPLINE_CURVE_WITH_KNOTS('',3,(#15762,#15763,#15764,#15765),
 .UNSPECIFIED.,.F.,.F.,(4,4),(2.36216418598326E-10,0.999999991023223),
 .UNSPECIFIED.);
#787=B_SPLINE_CURVE_WITH_KNOTS('',3,(#15767,#15768,#15769,#15770),
 .UNSPECIFIED.,.F.,.F.,(4,4),(4.44686267605015E-11,0.000461780122242359),
 .UNSPECIFIED.);
#788=B_SPLINE_CURVE_WITH_KNOTS('',3,(#15772,#15773,#15774,#15775),
 .UNSPECIFIED.,.F.,.F.,(4,4),(0.,0.000115526639658502),.UNSPECIFIED.);
#789=B_SPLINE_CURVE_WITH_KNOTS('',3,(#15777,#15778,#15779,#15780),
 .UNSPECIFIED.,.F.,.F.,(4,4),(3.53305356218227E-7,1.),.UNSPECIFIED.);
#790=B_SPLINE_CURVE_WITH_KNOTS('',3,(#15782,#15783,#15784,#15785),
 .UNSPECIFIED.,.F.,.F.,(4,4),(0.,0.0087679728211208),.UNSPECIFIED.);
#791=B_SPLINE_CURVE_WITH_KNOTS('',3,(#15786,#15787,#15788,#15789),
 .UNSPECIFIED.,.F.,.F.,(4,4),(1.21975111506088E-8,0.999999969357093),
 .UNSPECIFIED.);
#792=B_SPLINE_CURVE_WITH_KNOTS('',3,(#15791,#15792,#15793,#15794),
 .UNSPECIFIED.,.F.,.F.,(4,4),(0.,1.),.UNSPECIFIED.);
#793=B_SPLINE_CURVE_WITH_KNOTS('',3,(#15796,#15797,#15798,#15799),
 .UNSPECIFIED.,.F.,.F.,(4,4),(2.19702460833624E-9,0.00876797316930945),
 .UNSPECIFIED.);
#794=B_SPLINE_CURVE_WITH_KNOTS('',3,(#15801,#15802,#15803,#15804),
 .UNSPECIFIED.,.F.,.F.,(4,4),(0.,0.999999810901908),.UNSPECIFIED.);
#795=B_SPLINE_CURVE_WITH_KNOTS('',3,(#15806,#15807,#15808,#15809),
 .UNSPECIFIED.,.F.,.F.,(4,4),(1.79267076322998E-11,0.00011552663817591),
 .UNSPECIFIED.);
#796=B_SPLINE_CURVE_WITH_KNOTS('',3,(#15811,#15812,#15813,#15814),
 .UNSPECIFIED.,.F.,.F.,(4,4),(0.,0.000461780123066742),.UNSPECIFIED.);
#797=B_SPLINE_CURVE_WITH_KNOTS('',3,(#15816,#15817,#15818,#15819),
 .UNSPECIFIED.,.F.,.F.,(4,4),(2.5020233577996E-10,0.99999999095112),
 .UNSPECIFIED.);
#798=B_SPLINE_CURVE_WITH_KNOTS('',3,(#15821,#15822,#15823,#15824),
 .UNSPECIFIED.,.F.,.F.,(4,4),(4.44328322544207E-11,0.000461780122903715),
 .UNSPECIFIED.);
#799=B_SPLINE_CURVE_WITH_KNOTS('',3,(#15826,#15827,#15828,#15829),
 .UNSPECIFIED.,.F.,.F.,(4,4),(0.,0.000115526643559045),.UNSPECIFIED.);
#800=B_SPLINE_CURVE_WITH_KNOTS('',3,(#15831,#15832,#15833,#15834),
 .UNSPECIFIED.,.F.,.F.,(4,4),(3.53157909585551E-7,1.),.UNSPECIFIED.);
#801=B_SPLINE_CURVE_WITH_KNOTS('',3,(#15836,#15837,#15838,#15839),
 .UNSPECIFIED.,.F.,.F.,(4,4),(0.,0.00876797282088719),.UNSPECIFIED.);
#802=B_SPLINE_CURVE_WITH_KNOTS('',3,(#15840,#15841,#15842,#15843),
 .UNSPECIFIED.,.F.,.F.,(4,4),(1.21975111506088E-8,0.999999969326361),
 .UNSPECIFIED.);
#803=B_SPLINE_CURVE_WITH_KNOTS('',3,(#15846,#15847,#15848,#15849),
 .UNSPECIFIED.,.F.,.F.,(4,4),(0.,5.47511884554027E-5),.UNSPECIFIED.);
#804=B_SPLINE_CURVE_WITH_KNOTS('',3,(#15851,#15852,#15853,#15854),
 .UNSPECIFIED.,.F.,.F.,(4,4),(0.,1.),.UNSPECIFIED.);
#805=B_SPLINE_CURVE_WITH_KNOTS('',3,(#15856,#15857,#15858,#15859),
 .UNSPECIFIED.,.F.,.F.,(4,4),(2.6662045205095E-15,5.47511885493758E-5),
 .UNSPECIFIED.);
#806=B_SPLINE_CURVE_WITH_KNOTS('',3,(#15860,#15861,#15862,#15863,#15864,
#15865,#15866,#15867,#15868),.UNSPECIFIED.,.F.,.F.,(4,1,1,1,1,1,4),(0.,
0.25,0.375,0.5,0.625,0.75,1.),.UNSPECIFIED.);
#807=B_SPLINE_CURVE_WITH_KNOTS('',3,(#15871,#15872,#15873,#15874,#15875,
#15876,#15877,#15878,#15879,#15880),.UNSPECIFIED.,.F.,.F.,(4,1,1,1,1,1,
1,4),(0.,0.25,0.375,0.5,0.625,0.75,0.875,1.),.UNSPECIFIED.);
#808=B_SPLINE_CURVE_WITH_KNOTS('',3,(#15882,#15883,#15884,#15885),
 .UNSPECIFIED.,.F.,.F.,(4,4),(0.,5.47504762023892E-5),.UNSPECIFIED.);
#809=B_SPLINE_CURVE_WITH_KNOTS('',3,(#15889,#15890,#15891,#15892),
 .UNSPECIFIED.,.F.,.F.,(4,4),(5.41713412566433E-5,0.999997965428435),
 .UNSPECIFIED.);
#810=B_SPLINE_CURVE_WITH_KNOTS('',3,(#15894,#15895,#15896,#15897),
 .UNSPECIFIED.,.F.,.F.,(4,4),(4.31187151013716E-9,0.00876797323705365),
 .UNSPECIFIED.);
#811=B_SPLINE_CURVE_WITH_KNOTS('',3,(#15898,#15899,#15900,#15901,#15902,
#15903,#15904,#15905,#15906),.UNSPECIFIED.,.F.,.F.,(4,1,1,1,1,1,4),(0.,
0.25,0.375,0.5,0.625,0.75,1.),.UNSPECIFIED.);
#812=B_SPLINE_CURVE_WITH_KNOTS('',3,(#15909,#15910,#15911,#15912,#15913,
#15914,#15915,#15916,#15917,#15918),.UNSPECIFIED.,.F.,.F.,(4,1,1,1,1,1,
1,4),(0.,0.25,0.375,0.5,0.625,0.75,0.875,1.),.UNSPECIFIED.);
#813=B_SPLINE_CURVE_WITH_KNOTS('',3,(#15920,#15921,#15922,#15923),
 .UNSPECIFIED.,.F.,.F.,(4,4),(0.,0.999999976739494),.UNSPECIFIED.);
#814=B_SPLINE_CURVE_WITH_KNOTS('',3,(#15925,#15926,#15927,#15928),
 .UNSPECIFIED.,.F.,.F.,(4,4),(0.,5.47511871644386E-5),.UNSPECIFIED.);
#815=B_SPLINE_CURVE_WITH_KNOTS('',3,(#15930,#15931,#15932,#15933),
 .UNSPECIFIED.,.F.,.F.,(4,4),(0.,1.),.UNSPECIFIED.);
#816=B_SPLINE_CURVE_WITH_KNOTS('',3,(#15935,#15936,#15937,#15938),
 .UNSPECIFIED.,.F.,.F.,(4,4),(0.,5.47485615078587E-5),.UNSPECIFIED.);
#817=B_SPLINE_CURVE_WITH_KNOTS('',3,(#15939,#15940,#15941,#15942,#15943,
#15944,#15945,#15946,#15947),.UNSPECIFIED.,.F.,.F.,(4,1,1,1,1,1,4),(0.,
0.25,0.375,0.5,0.625,0.75,1.),.UNSPECIFIED.);
#818=B_SPLINE_CURVE_WITH_KNOTS('',3,(#15950,#15951,#15952,#15953,#15954,
#15955,#15956,#15957,#15958,#15959),.UNSPECIFIED.,.F.,.F.,(4,1,1,1,1,1,
1,4),(0.,0.25,0.375,0.5,0.625,0.75,0.875,1.),.UNSPECIFIED.);
#819=B_SPLINE_CURVE_WITH_KNOTS('',3,(#15961,#15962,#15963,#15964),
 .UNSPECIFIED.,.F.,.F.,(4,4),(0.,5.47504681501983E-5),.UNSPECIFIED.);
#820=B_SPLINE_CURVE_WITH_KNOTS('',3,(#15966,#15967,#15968,#15969),
 .UNSPECIFIED.,.F.,.F.,(4,4),(0.,1.),.UNSPECIFIED.);
#821=B_SPLINE_CURVE_WITH_KNOTS('',3,(#15971,#15972,#15973,#15974),
 .UNSPECIFIED.,.F.,.F.,(4,4),(1.73372280702655E-14,5.47511861723444E-5),
 .UNSPECIFIED.);
#822=B_SPLINE_CURVE_WITH_KNOTS('',3,(#15975,#15976,#15977,#15978,#15979,
#15980,#15981,#15982,#15983),.UNSPECIFIED.,.F.,.F.,(4,1,1,1,1,1,4),(0.,
0.25,0.375,0.5,0.625,0.75,1.),.UNSPECIFIED.);
#823=B_SPLINE_CURVE_WITH_KNOTS('',3,(#15986,#15987,#15988,#15989,#15990,
#15991,#15992,#15993,#15994,#15995),.UNSPECIFIED.,.F.,.F.,(4,1,1,1,1,1,
1,4),(0.,0.25,0.375,0.5,0.625,0.75,0.875,1.),.UNSPECIFIED.);
#824=B_SPLINE_CURVE_WITH_KNOTS('',3,(#15997,#15998,#15999,#16000),
 .UNSPECIFIED.,.F.,.F.,(4,4),(0.,5.4751186768266E-5),.UNSPECIFIED.);
#825=B_SPLINE_CURVE_WITH_KNOTS('',3,(#16002,#16003,#16004,#16005),
 .UNSPECIFIED.,.F.,.F.,(4,4),(0.,1.),.UNSPECIFIED.);
#826=B_SPLINE_CURVE_WITH_KNOTS('',3,(#16007,#16008,#16009,#16010),
 .UNSPECIFIED.,.F.,.F.,(4,4),(2.81166365578815E-14,5.47511864643206E-5),
 .UNSPECIFIED.);
#827=B_SPLINE_CURVE_WITH_KNOTS('',3,(#16011,#16012,#16013,#16014,#16015,
#16016,#16017,#16018,#16019),.UNSPECIFIED.,.F.,.F.,(4,1,1,1,1,1,4),(0.,
0.25,0.375,0.5,0.625,0.75,1.),.UNSPECIFIED.);
#828=B_SPLINE_CURVE_WITH_KNOTS('',3,(#16022,#16023,#16024,#16025,#16026,
#16027,#16028,#16029,#16030,#16031),.UNSPECIFIED.,.F.,.F.,(4,1,1,1,1,1,
1,4),(0.,0.25,0.375,0.5,0.625,0.75,0.875,1.),.UNSPECIFIED.);
#829=B_SPLINE_CURVE_WITH_KNOTS('',3,(#16033,#16034,#16035,#16036),
 .UNSPECIFIED.,.F.,.F.,(4,4),(0.,5.47511848914998E-5),.UNSPECIFIED.);
#830=B_SPLINE_CURVE_WITH_KNOTS('',3,(#16038,#16039,#16040,#16041),
 .UNSPECIFIED.,.F.,.F.,(4,4),(0.,1.),.UNSPECIFIED.);
#831=B_SPLINE_CURVE_WITH_KNOTS('',3,(#16043,#16044,#16045,#16046),
 .UNSPECIFIED.,.F.,.F.,(4,4),(3.54203178136851E-15,5.47511866309463E-5),
 .UNSPECIFIED.);
#832=B_SPLINE_CURVE_WITH_KNOTS('',3,(#16047,#16048,#16049,#16050,#16051,
#16052,#16053,#16054,#16055),.UNSPECIFIED.,.F.,.F.,(4,1,1,1,1,1,4),(0.,
0.25,0.375,0.5,0.625,0.75,1.),.UNSPECIFIED.);
#833=B_SPLINE_CURVE_WITH_KNOTS('',3,(#16058,#16059,#16060,#16061,#16062,
#16063,#16064,#16065,#16066,#16067),.UNSPECIFIED.,.F.,.F.,(4,1,1,1,1,1,
1,4),(0.,0.25,0.375,0.5,0.625,0.75,0.875,1.),.UNSPECIFIED.);
#834=B_SPLINE_CURVE_WITH_KNOTS('',3,(#16069,#16070,#16071,#16072),
 .UNSPECIFIED.,.F.,.F.,(4,4),(0.,0.999999786485093),.UNSPECIFIED.);
#835=B_SPLINE_CURVE_WITH_KNOTS('',3,(#16075,#16076,#16077,#16078,#16079,
#16080,#16081,#16082,#16083,#16084,#16085,#16086,#16087,#16088,#16089,#16090,
#16091,#16092,#16093,#16094,#16095,#16096,#16097,#16098,#16099),
 .UNSPECIFIED.,.F.,.F.,(4,1,1,1,1,1,1,1,1,1,1,1,1,1,1,1,1,1,1,1,1,1,4),
(0.,0.03125,0.046875,0.0625,0.09375,0.125,0.15625,0.1875,0.21875,0.25,0.3125,
0.375,0.4375,0.5,0.625,0.6875,0.75,0.8125,0.875,0.90625,0.9375,0.96875,
1.),.UNSPECIFIED.);
#836=B_SPLINE_CURVE_WITH_KNOTS('',3,(#16101,#16102,#16103,#16104),
 .UNSPECIFIED.,.F.,.F.,(4,4),(0.,1.),.UNSPECIFIED.);
#837=B_SPLINE_CURVE_WITH_KNOTS('',3,(#16106,#16107,#16108,#16109,#16110,
#16111,#16112,#16113,#16114,#16115,#16116,#16117,#16118,#16119,#16120,#16121,
#16122,#16123,#16124),.UNSPECIFIED.,.F.,.F.,(4,1,1,1,1,1,1,1,1,1,1,1,1,
1,1,1,4),(1.7738102471483E-8,0.0625000166294711,0.0937500160751554,0.12500001552084,
0.187500014412208,0.250000013303577,0.312500012194945,0.375000011086314,
0.437500009977683,0.500000008869051,0.625000006651788,0.687500005543157,
0.750000004434526,0.812500003325894,0.875000002217263,0.937500001108631,
1.),.UNSPECIFIED.);
#838=B_SPLINE_CURVE_WITH_KNOTS('',3,(#16126,#16127,#16128,#16129),
 .UNSPECIFIED.,.F.,.F.,(4,4),(0.,0.999999711518337),.UNSPECIFIED.);
#839=B_SPLINE_CURVE_WITH_KNOTS('',3,(#16132,#16133,#16134,#16135,#16136,
#16137,#16138,#16139,#16140,#16141,#16142,#16143,#16144,#16145,#16146,#16147,
#16148,#16149,#16150,#16151,#16152,#16153,#16154,#16155,#16156),
 .UNSPECIFIED.,.F.,.F.,(4,1,1,1,1,1,1,1,1,1,1,1,1,1,1,1,1,1,1,1,1,1,4),
(0.,0.03125,0.046875,0.0625,0.09375,0.125,0.15625,0.1875,0.21875,0.25,0.3125,
0.375,0.4375,0.5,0.625,0.6875,0.75,0.8125,0.875,0.90625,0.9375,0.96875,
1.),.UNSPECIFIED.);
#840=B_SPLINE_CURVE_WITH_KNOTS('',3,(#16158,#16159,#16160,#16161),
 .UNSPECIFIED.,.F.,.F.,(4,4),(0.,1.),.UNSPECIFIED.);
#841=B_SPLINE_CURVE_WITH_KNOTS('',3,(#16163,#16164,#16165,#16166,#16167,
#16168,#16169,#16170,#16171,#16172,#16173,#16174,#16175,#16176,#16177,#16178,
#16179,#16180,#16181),.UNSPECIFIED.,.F.,.F.,(4,1,1,1,1,1,1,1,1,1,1,1,1,
1,1,1,4),(1.77381032905796E-8,0.0625000166294718,0.0937500160751561,0.12500001552084,
0.187500014412209,0.250000013303577,0.312500012194946,0.375000011086315,
0.437500009977683,0.500000008869052,0.625000006651789,0.687500005543157,
0.750000004434526,0.812500003325894,0.875000002217263,0.937500001108631,
1.),.UNSPECIFIED.);
#842=B_SPLINE_CURVE_WITH_KNOTS('',3,(#16183,#16184,#16185,#16186,#16187,
#16188,#16189,#16190,#16191,#16192,#16193,#16194,#16195,#16196,#16197,#16198,
#16199,#16200,#16201,#16202,#16203,#16204,#16205,#16206,#16207),
 .UNSPECIFIED.,.F.,.F.,(4,1,1,1,1,1,1,1,1,1,1,1,1,1,1,1,1,1,1,1,1,1,4),
(0.,0.03125,0.046875,0.0625,0.09375,0.125,0.15625,0.1875,0.21875,0.25,0.3125,
0.375,0.4375,0.5,0.625,0.6875,0.75,0.8125,0.875,0.90625,0.9375,0.96875,
1.),.UNSPECIFIED.);
#843=B_SPLINE_CURVE_WITH_KNOTS('',3,(#16210,#16211,#16212,#16213),
 .UNSPECIFIED.,.F.,.F.,(4,4),(0.,1.),.UNSPECIFIED.);
#844=B_SPLINE_CURVE_WITH_KNOTS('',3,(#16215,#16216,#16217,#16218,#16219,
#16220,#16221,#16222,#16223,#16224,#16225,#16226,#16227,#16228,#16229,#16230,
#16231),.UNSPECIFIED.,.F.,.F.,(4,1,1,1,1,1,1,1,1,1,1,1,1,1,4),(1.7738103310695E-8,
0.0625000166294719,0.0937500160751561,0.12500001552084,0.187500014412209,
0.250000013303577,0.312500012194946,0.375000011086315,0.437500009977683,
0.500000008869052,0.625000006651789,0.750000004434526,0.812500003325894,
0.875000002217263,1.),.UNSPECIFIED.);
#845=B_SPLINE_CURVE_WITH_KNOTS('',3,(#16233,#16234,#16235,#16236),
 .UNSPECIFIED.,.F.,.F.,(4,4),(0.,0.999999786485099),.UNSPECIFIED.);
#846=B_SPLINE_CURVE_WITH_KNOTS('',3,(#16238,#16239,#16240,#16241,#16242,
#16243,#16244,#16245,#16246,#16247,#16248,#16249,#16250,#16251,#16252,#16253,
#16254,#16255,#16256,#16257,#16258,#16259,#16260,#16261,#16262),
 .UNSPECIFIED.,.F.,.F.,(4,1,1,1,1,1,1,1,1,1,1,1,1,1,1,1,1,1,1,1,1,1,4),
(0.,0.03125,0.046875,0.0625,0.09375,0.125,0.15625,0.1875,0.21875,0.25,0.3125,
0.375,0.4375,0.5,0.625,0.6875,0.75,0.8125,0.875,0.90625,0.9375,0.96875,
1.),.UNSPECIFIED.);
#847=B_SPLINE_CURVE_WITH_KNOTS('',3,(#16265,#16266,#16267,#16268),
 .UNSPECIFIED.,.F.,.F.,(4,4),(0.,1.),.UNSPECIFIED.);
#848=B_SPLINE_CURVE_WITH_KNOTS('',3,(#16270,#16271,#16272,#16273,#16274,
#16275,#16276,#16277,#16278,#16279,#16280,#16281,#16282,#16283,#16284,#16285,
#16286,#16287,#16288),.UNSPECIFIED.,.F.,.F.,(4,1,1,1,1,1,1,1,1,1,1,1,1,
1,1,1,4),(1.77381030488726E-8,0.0625000166294716,0.0937500160751559,0.12500001552084,
0.187500014412209,0.250000013303577,0.312500012194946,0.375000011086314,
0.437500009977683,0.500000008869051,0.625000006651789,0.687500005543157,
0.750000004434526,0.812500003325894,0.875000002217263,0.937500001108631,
1.),.UNSPECIFIED.);
#849=B_SPLINE_CURVE_WITH_KNOTS('',3,(#16290,#16291,#16292,#16293),
 .UNSPECIFIED.,.F.,.F.,(4,4),(0.,0.999999786485093),.UNSPECIFIED.);
#850=B_SPLINE_CURVE_WITH_KNOTS('',3,(#16295,#16296,#16297,#16298,#16299,
#16300,#16301,#16302,#16303,#16304,#16305,#16306,#16307,#16308,#16309,#16310,
#16311,#16312,#16313,#16314,#16315,#16316,#16317,#16318,#16319),
 .UNSPECIFIED.,.F.,.F.,(4,1,1,1,1,1,1,1,1,1,1,1,1,1,1,1,1,1,1,1,1,1,4),
(0.,0.03125,0.046875,0.0625,0.09375,0.125,0.15625,0.1875,0.21875,0.25,0.3125,
0.375,0.4375,0.5,0.625,0.6875,0.75,0.8125,0.875,0.90625,0.9375,0.96875,
1.),.UNSPECIFIED.);
#851=B_SPLINE_CURVE_WITH_KNOTS('',3,(#16322,#16323,#16324,#16325),
 .UNSPECIFIED.,.F.,.F.,(4,4),(0.,1.),.UNSPECIFIED.);
#852=B_SPLINE_CURVE_WITH_KNOTS('',3,(#16327,#16328,#16329,#16330,#16331,
#16332,#16333,#16334,#16335,#16336,#16337,#16338,#16339,#16340,#16341,#16342,
#16343,#16344,#16345),.UNSPECIFIED.,.F.,.F.,(4,1,1,1,1,1,1,1,1,1,1,1,1,
1,1,1,4),(2.39185157367047E-8,0.0625000224236085,0.0937500216761549,0.125000020928701,
0.187500019433794,0.250000017938887,0.31250001644398,0.375000014949072,
0.437500013454165,0.500000011959258,0.625000008969443,0.687500007474536,
0.750000005979629,0.812500004484722,0.875000002989815,0.937500001494907,
1.),.UNSPECIFIED.);
#853=B_SPLINE_CURVE_WITH_KNOTS('',3,(#16347,#16348,#16349,#16350),
 .UNSPECIFIED.,.F.,.F.,(4,4),(0.,0.999999786485096),.UNSPECIFIED.);
#854=B_SPLINE_CURVE_WITH_KNOTS('',3,(#16352,#16353,#16354,#16355),
 .UNSPECIFIED.,.F.,.F.,(4,4),(0.,0.999999786485099),.UNSPECIFIED.);
#855=B_SPLINE_CURVE_WITH_KNOTS('',3,(#16358,#16359,#16360,#16361,#16362,
#16363,#16364,#16365,#16366,#16367,#16368,#16369,#16370,#16371,#16372,#16373,
#16374,#16375,#16376,#16377,#16378,#16379,#16380),.UNSPECIFIED.,.F.,.F.,
(4,1,1,1,1,1,1,1,1,1,1,1,1,1,1,1,1,1,1,1,4),(0.,0.03125,0.046875,0.0625,
0.09375,0.125,0.15625,0.1875,0.21875,0.25,0.3125,0.375,0.4375,0.5,0.625,
0.6875,0.75,0.8125,0.875,0.9375,1.),.UNSPECIFIED.);
#856=B_SPLINE_CURVE_WITH_KNOTS('',3,(#16382,#16383,#16384,#16385),
 .UNSPECIFIED.,.F.,.F.,(4,4),(0.,1.),.UNSPECIFIED.);
#857=B_SPLINE_CURVE_WITH_KNOTS('',3,(#16387,#16388,#16389,#16390,#16391,
#16392,#16393,#16394,#16395,#16396,#16397,#16398,#16399,#16400,#16401,#16402,
#16403,#16404,#16405),.UNSPECIFIED.,.F.,.F.,(4,1,1,1,1,1,1,1,1,1,1,1,1,
1,1,1,4),(1.77381032197E-8,0.0625000166294718,0.093750016075156,0.12500001552084,
0.187500014412209,0.250000013303577,0.312500012194946,0.375000011086315,
0.437500009977683,0.500000008869052,0.625000006651789,0.687500005543157,
0.750000004434526,0.812500003325894,0.875000002217263,0.937500001108631,
1.),.UNSPECIFIED.);
#858=B_SPLINE_CURVE_WITH_KNOTS('',3,(#16407,#16408,#16409,#16410),
 .UNSPECIFIED.,.F.,.F.,(4,4),(9.76476175762548E-14,0.000408584948842628),
 .UNSPECIFIED.);
#859=B_SPLINE_CURVE_WITH_KNOTS('',3,(#16412,#16413,#16414,#16415),
 .UNSPECIFIED.,.F.,.F.,(4,4),(0.,1.),.UNSPECIFIED.);
#860=B_SPLINE_CURVE_WITH_KNOTS('',3,(#16417,#16418,#16419,#16420),
 .UNSPECIFIED.,.F.,.F.,(4,4),(0.,0.999999971246998),.UNSPECIFIED.);
#861=B_SPLINE_CURVE_WITH_KNOTS('',3,(#16422,#16423,#16424,#16425),
 .UNSPECIFIED.,.F.,.F.,(4,4),(-0.000178154180456897,0.000230031247706017),
 .UNSPECIFIED.);
#862=B_SPLINE_CURVE_WITH_KNOTS('',3,(#16427,#16428,#16429,#16430),
 .UNSPECIFIED.,.F.,.F.,(4,4),(5.83500099566355E-9,0.999999999974686),
 .UNSPECIFIED.);
#863=B_SPLINE_CURVE_WITH_KNOTS('',3,(#16432,#16433,#16434,#16435),
 .UNSPECIFIED.,.F.,.F.,(4,4),(8.66730814626801E-10,0.00040832854943033),
 .UNSPECIFIED.);
#864=B_SPLINE_CURVE_WITH_KNOTS('',3,(#16437,#16438,#16439,#16440),
 .UNSPECIFIED.,.F.,.F.,(4,4),(0.,1.),.UNSPECIFIED.);
#865=B_SPLINE_CURVE_WITH_KNOTS('',3,(#16442,#16443,#16444,#16445),
 .UNSPECIFIED.,.F.,.F.,(4,4),(8.74189910716064E-10,0.000408584947659101),
 .UNSPECIFIED.);
#866=B_SPLINE_CURVE_WITH_KNOTS('',3,(#16447,#16448,#16449,#16450),
 .UNSPECIFIED.,.F.,.F.,(4,4),(0.,1.),.UNSPECIFIED.);
#867=B_SPLINE_CURVE_WITH_KNOTS('',3,(#16452,#16453,#16454,#16455),
 .UNSPECIFIED.,.F.,.F.,(4,4),(0.,1.),.UNSPECIFIED.);
#868=B_SPLINE_CURVE_WITH_KNOTS('',3,(#16457,#16458,#16459,#16460),
 .UNSPECIFIED.,.F.,.F.,(4,4),(1.74701212203631E-8,1.),.UNSPECIFIED.);
#869=B_SPLINE_CURVE_WITH_KNOTS('',3,(#16462,#16463,#16464,#16465),
 .UNSPECIFIED.,.F.,.F.,(4,4),(0.,1.),.UNSPECIFIED.);
#870=B_SPLINE_CURVE_WITH_KNOTS('',3,(#16467,#16468,#16469,#16470),
 .UNSPECIFIED.,.F.,.F.,(4,4),(1.22431959981855E-9,0.000408585660822127),
 .UNSPECIFIED.);
#871=B_SPLINE_CURVE_WITH_KNOTS('',3,(#16472,#16473,#16474,#16475),
 .UNSPECIFIED.,.F.,.F.,(4,4),(0.,1.),.UNSPECIFIED.);
#872=B_SPLINE_CURVE_WITH_KNOTS('',3,(#16479,#16480,#16481,#16482),
 .UNSPECIFIED.,.F.,.F.,(4,4),(1.622093506599E-14,0.000408584946011366),
 .UNSPECIFIED.);
#873=B_SPLINE_CURVE_WITH_KNOTS('',3,(#16484,#16485,#16486,#16487),
 .UNSPECIFIED.,.F.,.F.,(4,4),(0.,1.),.UNSPECIFIED.);
#874=B_SPLINE_CURVE_WITH_KNOTS('',3,(#16489,#16490,#16491,#16492),
 .UNSPECIFIED.,.F.,.F.,(4,4),(8.75998893489131E-10,0.000408584945827489),
 .UNSPECIFIED.);
#875=B_SPLINE_CURVE_WITH_KNOTS('',3,(#16494,#16495,#16496,#16497),
 .UNSPECIFIED.,.F.,.F.,(4,4),(0.,1.),.UNSPECIFIED.);
#876=B_SPLINE_CURVE_WITH_KNOTS('',3,(#16499,#16500,#16501,#16502),
 .UNSPECIFIED.,.F.,.F.,(4,4),(0.,1.),.UNSPECIFIED.);
#877=B_SPLINE_CURVE_WITH_KNOTS('',3,(#16504,#16505,#16506,#16507),
 .UNSPECIFIED.,.F.,.F.,(4,4),(2.1214408803583E-14,0.000408584946680086),
 .UNSPECIFIED.);
#878=B_SPLINE_CURVE_WITH_KNOTS('',3,(#16509,#16510,#16511,#16512),
 .UNSPECIFIED.,.F.,.F.,(4,4),(0.,1.),.UNSPECIFIED.);
#879=B_SPLINE_CURVE_WITH_KNOTS('',3,(#16514,#16515,#16516,#16517),
 .UNSPECIFIED.,.F.,.F.,(4,4),(8.72748227154931E-10,0.000408584950442943),
 .UNSPECIFIED.);
#880=B_SPLINE_CURVE_WITH_KNOTS('',3,(#16519,#16520,#16521,#16522),
 .UNSPECIFIED.,.F.,.F.,(4,4),(0.,1.),.UNSPECIFIED.);
#881=B_SPLINE_CURVE_WITH_KNOTS('',3,(#16524,#16525,#16526,#16527),
 .UNSPECIFIED.,.F.,.F.,(4,4),(0.,1.),.UNSPECIFIED.);
#882=B_SPLINE_CURVE_WITH_KNOTS('',3,(#16529,#16530,#16531,#16532),
 .UNSPECIFIED.,.F.,.F.,(4,4),(6.86945077261581E-14,0.000408584947563837),
 .UNSPECIFIED.);
#883=B_SPLINE_CURVE_WITH_KNOTS('',3,(#16534,#16535,#16536,#16537),
 .UNSPECIFIED.,.F.,.F.,(4,4),(5.9410360424763E-7,1.),.UNSPECIFIED.);
#884=B_SPLINE_CURVE_WITH_KNOTS('',3,(#16539,#16540,#16541,#16542),
 .UNSPECIFIED.,.F.,.F.,(4,4),(8.73453709605601E-10,0.000408584949164257),
 .UNSPECIFIED.);
#885=B_SPLINE_CURVE_WITH_KNOTS('',3,(#16544,#16545,#16546,#16547),
 .UNSPECIFIED.,.F.,.F.,(4,4),(0.,0.999999400915229),.UNSPECIFIED.);
#886=B_SPLINE_CURVE_WITH_KNOTS('',3,(#16549,#16550,#16551,#16552),
 .UNSPECIFIED.,.F.,.F.,(4,4),(0.,1.),.UNSPECIFIED.);
#887=B_SPLINE_CURVE_WITH_KNOTS('',3,(#17303,#17304,#17305,#17306),
 .UNSPECIFIED.,.F.,.F.,(4,4),(0.,0.000408585662909977),.UNSPECIFIED.);
#1047=PLANE('',#8695);
#1048=PLANE('',#8697);
#1049=PLANE('',#8703);
#1050=PLANE('',#8705);
#1051=PLANE('',#8711);
#1052=PLANE('',#8713);
#1053=PLANE('',#8719);
#1054=PLANE('',#8721);
#1055=PLANE('',#8727);
#1056=PLANE('',#8729);
#1057=PLANE('',#8735);
#1058=PLANE('',#8737);
#1059=PLANE('',#8743);
#1060=PLANE('',#8745);
#1061=PLANE('',#8751);
#1062=PLANE('',#8753);
#1063=PLANE('',#8759);
#1064=PLANE('',#8821);
#1065=PLANE('',#8834);
#1066=PLANE('',#8879);
#1067=PLANE('',#8886);
#1068=PLANE('',#8969);
#1069=PLANE('',#9008);
#1070=PLANE('',#9027);
#1071=PLANE('',#9031);
#1072=PLANE('',#9032);
#1073=PLANE('',#9036);
#1074=PLANE('',#9040);
#1075=PLANE('',#9041);
#1076=PLANE('',#9045);
#1077=PLANE('',#9046);
#1078=PLANE('',#9050);
#1079=PLANE('',#9051);
#1080=PLANE('',#9055);
#1081=PLANE('',#9069);
#1082=PLANE('',#9112);
#1083=PLANE('',#9114);
#1084=PLANE('',#9116);
#1085=PLANE('',#9118);
#1086=PLANE('',#9125);
#1087=PLANE('',#9127);
#1088=PLANE('',#9129);
#1089=PLANE('',#9131);
#1090=PLANE('',#9133);
#1091=PLANE('',#9135);
#1092=PLANE('',#9137);
#1093=PLANE('',#9142);
#2258=ORIENTED_EDGE('',*,*,#4050,.F.);
#2259=ORIENTED_EDGE('',*,*,#4051,.F.);
#2260=ORIENTED_EDGE('',*,*,#4052,.T.);
#2261=ORIENTED_EDGE('',*,*,#4050,.T.);
#2262=ORIENTED_EDGE('',*,*,#4053,.T.);
#2263=ORIENTED_EDGE('',*,*,#4051,.T.);
#2264=ORIENTED_EDGE('',*,*,#4052,.F.);
#2265=ORIENTED_EDGE('',*,*,#4054,.F.);
#2266=ORIENTED_EDGE('',*,*,#4055,.F.);
#2267=ORIENTED_EDGE('',*,*,#4053,.F.);
#2268=ORIENTED_EDGE('',*,*,#4054,.T.);
#2269=ORIENTED_EDGE('',*,*,#4056,.T.);
#2270=ORIENTED_EDGE('',*,*,#4055,.T.);
#2271=ORIENTED_EDGE('',*,*,#4057,.T.);
#2272=ORIENTED_EDGE('',*,*,#4056,.F.);
#2273=ORIENTED_EDGE('',*,*,#4058,.F.);
#2274=ORIENTED_EDGE('',*,*,#4059,.F.);
#2275=ORIENTED_EDGE('',*,*,#4057,.F.);
#2276=ORIENTED_EDGE('',*,*,#4060,.T.);
#2277=ORIENTED_EDGE('',*,*,#4058,.T.);
#2278=ORIENTED_EDGE('',*,*,#4061,.T.);
#2279=ORIENTED_EDGE('',*,*,#4059,.T.);
#2280=ORIENTED_EDGE('',*,*,#4060,.F.);
#2281=ORIENTED_EDGE('',*,*,#4062,.F.);
#2282=ORIENTED_EDGE('',*,*,#4063,.F.);
#2283=ORIENTED_EDGE('',*,*,#4061,.F.);
#2284=ORIENTED_EDGE('',*,*,#4062,.T.);
#2285=ORIENTED_EDGE('',*,*,#4064,.T.);
#2286=ORIENTED_EDGE('',*,*,#4063,.T.);
#2287=ORIENTED_EDGE('',*,*,#4065,.T.);
#2288=ORIENTED_EDGE('',*,*,#4066,.F.);
#2289=ORIENTED_EDGE('',*,*,#4064,.F.);
#2290=ORIENTED_EDGE('',*,*,#4067,.F.);
#2291=ORIENTED_EDGE('',*,*,#4065,.F.);
#2292=ORIENTED_EDGE('',*,*,#4068,.T.);
#2293=ORIENTED_EDGE('',*,*,#4066,.T.);
#2294=ORIENTED_EDGE('',*,*,#4069,.T.);
#2295=ORIENTED_EDGE('',*,*,#4067,.T.);
#2296=ORIENTED_EDGE('',*,*,#4068,.F.);
#2297=ORIENTED_EDGE('',*,*,#4070,.F.);
#2298=ORIENTED_EDGE('',*,*,#4069,.F.);
#2299=ORIENTED_EDGE('',*,*,#4071,.F.);
#2300=ORIENTED_EDGE('',*,*,#4070,.T.);
#2301=ORIENTED_EDGE('',*,*,#4072,.T.);
#2302=ORIENTED_EDGE('',*,*,#4071,.T.);
#2303=ORIENTED_EDGE('',*,*,#4073,.T.);
#2304=ORIENTED_EDGE('',*,*,#4074,.F.);
#2305=ORIENTED_EDGE('',*,*,#4072,.F.);
#2306=ORIENTED_EDGE('',*,*,#4075,.F.);
#2307=ORIENTED_EDGE('',*,*,#4073,.F.);
#2308=ORIENTED_EDGE('',*,*,#4076,.T.);
#2309=ORIENTED_EDGE('',*,*,#4074,.T.);
#2310=ORIENTED_EDGE('',*,*,#4075,.T.);
#2311=ORIENTED_EDGE('',*,*,#4077,.T.);
#2312=ORIENTED_EDGE('',*,*,#4078,.F.);
#2313=ORIENTED_EDGE('',*,*,#4076,.F.);
#2314=ORIENTED_EDGE('',*,*,#4077,.F.);
#2315=ORIENTED_EDGE('',*,*,#4079,.F.);
#2316=ORIENTED_EDGE('',*,*,#4080,.F.);
#2317=ORIENTED_EDGE('',*,*,#4078,.T.);
#2318=ORIENTED_EDGE('',*,*,#4079,.T.);
#2319=ORIENTED_EDGE('',*,*,#4081,.T.);
#2320=ORIENTED_EDGE('',*,*,#4080,.T.);
#2321=ORIENTED_EDGE('',*,*,#4082,.T.);
#2322=ORIENTED_EDGE('',*,*,#4081,.F.);
#2323=ORIENTED_EDGE('',*,*,#4083,.F.);
#2324=ORIENTED_EDGE('',*,*,#4084,.F.);
#2325=ORIENTED_EDGE('',*,*,#4085,.F.);
#2326=ORIENTED_EDGE('',*,*,#4086,.F.);
#2327=ORIENTED_EDGE('',*,*,#4087,.F.);
#2328=ORIENTED_EDGE('',*,*,#4088,.F.);
#2329=ORIENTED_EDGE('',*,*,#4089,.F.);
#2330=ORIENTED_EDGE('',*,*,#4090,.F.);
#2331=ORIENTED_EDGE('',*,*,#4091,.F.);
#2332=ORIENTED_EDGE('',*,*,#4092,.F.);
#2333=ORIENTED_EDGE('',*,*,#4093,.F.);
#2334=ORIENTED_EDGE('',*,*,#4094,.F.);
#2335=ORIENTED_EDGE('',*,*,#4095,.F.);
#2336=ORIENTED_EDGE('',*,*,#4096,.F.);
#2337=ORIENTED_EDGE('',*,*,#4097,.F.);
#2338=ORIENTED_EDGE('',*,*,#4098,.F.);
#2339=ORIENTED_EDGE('',*,*,#4099,.F.);
#2340=ORIENTED_EDGE('',*,*,#4100,.F.);
#2341=ORIENTED_EDGE('',*,*,#4101,.F.);
#2342=ORIENTED_EDGE('',*,*,#4102,.F.);
#2343=ORIENTED_EDGE('',*,*,#4082,.F.);
#2344=ORIENTED_EDGE('',*,*,#4103,.F.);
#2345=ORIENTED_EDGE('',*,*,#4083,.T.);
#2346=ORIENTED_EDGE('',*,*,#4104,.F.);
#2347=ORIENTED_EDGE('',*,*,#4102,.T.);
#2348=ORIENTED_EDGE('',*,*,#4101,.T.);
#2349=ORIENTED_EDGE('',*,*,#4105,.F.);
#2350=ORIENTED_EDGE('',*,*,#4106,.F.);
#2351=ORIENTED_EDGE('',*,*,#4100,.T.);
#2352=ORIENTED_EDGE('',*,*,#4107,.F.);
#2353=ORIENTED_EDGE('',*,*,#4099,.T.);
#2354=ORIENTED_EDGE('',*,*,#4108,.F.);
#2355=ORIENTED_EDGE('',*,*,#4098,.T.);
#2356=ORIENTED_EDGE('',*,*,#4109,.F.);
#2357=ORIENTED_EDGE('',*,*,#4097,.T.);
#2358=ORIENTED_EDGE('',*,*,#4110,.F.);
#2359=ORIENTED_EDGE('',*,*,#4096,.T.);
#2360=ORIENTED_EDGE('',*,*,#4111,.F.);
#2361=ORIENTED_EDGE('',*,*,#4095,.T.);
#2362=ORIENTED_EDGE('',*,*,#4112,.F.);
#2363=ORIENTED_EDGE('',*,*,#4094,.T.);
#2364=ORIENTED_EDGE('',*,*,#4113,.F.);
#2365=ORIENTED_EDGE('',*,*,#4093,.T.);
#2366=ORIENTED_EDGE('',*,*,#4114,.F.);
#2367=ORIENTED_EDGE('',*,*,#4092,.T.);
#2368=ORIENTED_EDGE('',*,*,#4115,.F.);
#2369=ORIENTED_EDGE('',*,*,#4091,.T.);
#2370=ORIENTED_EDGE('',*,*,#4116,.F.);
#2371=ORIENTED_EDGE('',*,*,#4090,.T.);
#2372=ORIENTED_EDGE('',*,*,#4117,.F.);
#2373=ORIENTED_EDGE('',*,*,#4089,.T.);
#2374=ORIENTED_EDGE('',*,*,#4118,.F.);
#2375=ORIENTED_EDGE('',*,*,#4088,.T.);
#2376=ORIENTED_EDGE('',*,*,#4119,.F.);
#2377=ORIENTED_EDGE('',*,*,#4087,.T.);
#2378=ORIENTED_EDGE('',*,*,#4120,.F.);
#2379=ORIENTED_EDGE('',*,*,#4086,.T.);
#2380=ORIENTED_EDGE('',*,*,#4121,.F.);
#2381=ORIENTED_EDGE('',*,*,#4085,.T.);
#2382=ORIENTED_EDGE('',*,*,#4122,.T.);
#2383=ORIENTED_EDGE('',*,*,#4123,.T.);
#2384=ORIENTED_EDGE('',*,*,#4084,.T.);
#2385=ORIENTED_EDGE('',*,*,#4103,.T.);
#2386=ORIENTED_EDGE('',*,*,#4124,.F.);
#2387=ORIENTED_EDGE('',*,*,#4125,.F.);
#2388=ORIENTED_EDGE('',*,*,#4126,.F.);
#2389=ORIENTED_EDGE('',*,*,#4121,.T.);
#2390=ORIENTED_EDGE('',*,*,#4120,.T.);
#2391=ORIENTED_EDGE('',*,*,#4119,.T.);
#2392=ORIENTED_EDGE('',*,*,#4118,.T.);
#2393=ORIENTED_EDGE('',*,*,#4117,.T.);
#2394=ORIENTED_EDGE('',*,*,#4116,.T.);
#2395=ORIENTED_EDGE('',*,*,#4115,.T.);
#2396=ORIENTED_EDGE('',*,*,#4114,.T.);
#2397=ORIENTED_EDGE('',*,*,#4113,.T.);
#2398=ORIENTED_EDGE('',*,*,#4112,.T.);
#2399=ORIENTED_EDGE('',*,*,#4111,.T.);
#2400=ORIENTED_EDGE('',*,*,#4110,.T.);
#2401=ORIENTED_EDGE('',*,*,#4109,.T.);
#2402=ORIENTED_EDGE('',*,*,#4108,.T.);
#2403=ORIENTED_EDGE('',*,*,#4107,.T.);
#2404=ORIENTED_EDGE('',*,*,#4106,.T.);
#2405=ORIENTED_EDGE('',*,*,#4105,.T.);
#2406=ORIENTED_EDGE('',*,*,#4104,.T.);
#2407=ORIENTED_EDGE('',*,*,#4127,.F.);
#2408=ORIENTED_EDGE('',*,*,#4122,.F.);
#2409=ORIENTED_EDGE('',*,*,#4123,.F.);
#2410=ORIENTED_EDGE('',*,*,#4128,.T.);
#2411=ORIENTED_EDGE('',*,*,#4129,.T.);
#2412=ORIENTED_EDGE('',*,*,#4124,.T.);
#2413=ORIENTED_EDGE('',*,*,#4125,.T.);
#2414=ORIENTED_EDGE('',*,*,#4130,.F.);
#2415=ORIENTED_EDGE('',*,*,#4131,.F.);
#2416=ORIENTED_EDGE('',*,*,#4127,.T.);
#2417=ORIENTED_EDGE('',*,*,#4132,.T.);
#2418=ORIENTED_EDGE('',*,*,#4133,.T.);
#2419=ORIENTED_EDGE('',*,*,#4129,.F.);
#2420=ORIENTED_EDGE('',*,*,#4128,.F.);
#2421=ORIENTED_EDGE('',*,*,#4126,.T.);
#2422=ORIENTED_EDGE('',*,*,#4130,.T.);
#2423=ORIENTED_EDGE('',*,*,#4131,.T.);
#2424=ORIENTED_EDGE('',*,*,#4134,.F.);
#2425=ORIENTED_EDGE('',*,*,#4135,.T.);
#2426=ORIENTED_EDGE('',*,*,#4136,.T.);
#2427=ORIENTED_EDGE('',*,*,#4132,.F.);
#2428=ORIENTED_EDGE('',*,*,#4133,.F.);
#2429=ORIENTED_EDGE('',*,*,#4137,.T.);
#2430=ORIENTED_EDGE('',*,*,#4134,.T.);
#2431=ORIENTED_EDGE('',*,*,#4136,.F.);
#2432=ORIENTED_EDGE('',*,*,#4138,.F.);
#2433=ORIENTED_EDGE('',*,*,#4139,.F.);
#2434=ORIENTED_EDGE('',*,*,#4140,.F.);
#2435=ORIENTED_EDGE('',*,*,#4140,.T.);
#2436=ORIENTED_EDGE('',*,*,#4141,.F.);
#2437=ORIENTED_EDGE('',*,*,#4138,.T.);
#2438=ORIENTED_EDGE('',*,*,#4135,.F.);
#2439=ORIENTED_EDGE('',*,*,#4142,.F.);
#2440=ORIENTED_EDGE('',*,*,#4143,.F.);
#2441=ORIENTED_EDGE('',*,*,#4137,.F.);
#2442=ORIENTED_EDGE('',*,*,#4141,.T.);
#2443=ORIENTED_EDGE('',*,*,#4139,.T.);
#2444=ORIENTED_EDGE('',*,*,#4144,.T.);
#2445=ORIENTED_EDGE('',*,*,#4145,.T.);
#2446=ORIENTED_EDGE('',*,*,#4146,.T.);
#2447=ORIENTED_EDGE('',*,*,#4147,.T.);
#2448=ORIENTED_EDGE('',*,*,#4148,.T.);
#2449=ORIENTED_EDGE('',*,*,#4149,.T.);
#2450=ORIENTED_EDGE('',*,*,#4150,.T.);
#2451=ORIENTED_EDGE('',*,*,#4151,.T.);
#2452=ORIENTED_EDGE('',*,*,#4152,.T.);
#2453=ORIENTED_EDGE('',*,*,#4153,.T.);
#2454=ORIENTED_EDGE('',*,*,#4154,.T.);
#2455=ORIENTED_EDGE('',*,*,#4155,.T.);
#2456=ORIENTED_EDGE('',*,*,#4156,.T.);
#2457=ORIENTED_EDGE('',*,*,#4157,.T.);
#2458=ORIENTED_EDGE('',*,*,#4158,.T.);
#2459=ORIENTED_EDGE('',*,*,#4159,.T.);
#2460=ORIENTED_EDGE('',*,*,#4160,.T.);
#2461=ORIENTED_EDGE('',*,*,#4161,.T.);
#2462=ORIENTED_EDGE('',*,*,#4162,.T.);
#2463=ORIENTED_EDGE('',*,*,#4163,.T.);
#2464=ORIENTED_EDGE('',*,*,#4164,.T.);
#2465=ORIENTED_EDGE('',*,*,#4165,.T.);
#2466=ORIENTED_EDGE('',*,*,#4166,.T.);
#2467=ORIENTED_EDGE('',*,*,#4167,.T.);
#2468=ORIENTED_EDGE('',*,*,#4168,.T.);
#2469=ORIENTED_EDGE('',*,*,#4169,.T.);
#2470=ORIENTED_EDGE('',*,*,#4143,.T.);
#2471=ORIENTED_EDGE('',*,*,#4142,.T.);
#2472=ORIENTED_EDGE('',*,*,#4170,.T.);
#2473=ORIENTED_EDGE('',*,*,#4171,.F.);
#2474=ORIENTED_EDGE('',*,*,#4172,.F.);
#2475=ORIENTED_EDGE('',*,*,#4158,.F.);
#2476=ORIENTED_EDGE('',*,*,#4157,.F.);
#2477=ORIENTED_EDGE('',*,*,#4173,.F.);
#2478=ORIENTED_EDGE('',*,*,#4174,.F.);
#2479=ORIENTED_EDGE('',*,*,#4175,.F.);
#2480=ORIENTED_EDGE('',*,*,#4159,.F.);
#2481=ORIENTED_EDGE('',*,*,#4172,.T.);
#2482=ORIENTED_EDGE('',*,*,#4160,.F.);
#2483=ORIENTED_EDGE('',*,*,#4175,.T.);
#2484=ORIENTED_EDGE('',*,*,#4176,.F.);
#2485=ORIENTED_EDGE('',*,*,#4177,.F.);
#2486=ORIENTED_EDGE('',*,*,#4161,.F.);
#2487=ORIENTED_EDGE('',*,*,#4177,.T.);
#2488=ORIENTED_EDGE('',*,*,#4178,.F.);
#2489=ORIENTED_EDGE('',*,*,#4179,.F.);
#2490=ORIENTED_EDGE('',*,*,#4162,.F.);
#2491=ORIENTED_EDGE('',*,*,#4179,.T.);
#2492=ORIENTED_EDGE('',*,*,#4180,.F.);
#2493=ORIENTED_EDGE('',*,*,#4181,.F.);
#2494=ORIENTED_EDGE('',*,*,#4163,.F.);
#2495=ORIENTED_EDGE('',*,*,#4181,.T.);
#2496=ORIENTED_EDGE('',*,*,#4182,.F.);
#2497=ORIENTED_EDGE('',*,*,#4183,.F.);
#2498=ORIENTED_EDGE('',*,*,#4164,.F.);
#2499=ORIENTED_EDGE('',*,*,#4183,.T.);
#2500=ORIENTED_EDGE('',*,*,#4184,.F.);
#2501=ORIENTED_EDGE('',*,*,#4185,.F.);
#2502=ORIENTED_EDGE('',*,*,#4165,.F.);
#2503=ORIENTED_EDGE('',*,*,#4185,.T.);
#2504=ORIENTED_EDGE('',*,*,#4186,.F.);
#2505=ORIENTED_EDGE('',*,*,#4187,.F.);
#2506=ORIENTED_EDGE('',*,*,#4166,.F.);
#2507=ORIENTED_EDGE('',*,*,#4187,.T.);
#2508=ORIENTED_EDGE('',*,*,#4188,.F.);
#2509=ORIENTED_EDGE('',*,*,#4189,.F.);
#2510=ORIENTED_EDGE('',*,*,#4167,.F.);
#2511=ORIENTED_EDGE('',*,*,#4189,.T.);
#2512=ORIENTED_EDGE('',*,*,#4190,.F.);
#2513=ORIENTED_EDGE('',*,*,#4191,.F.);
#2514=ORIENTED_EDGE('',*,*,#4168,.F.);
#2515=ORIENTED_EDGE('',*,*,#4191,.T.);
#2516=ORIENTED_EDGE('',*,*,#4192,.F.);
#2517=ORIENTED_EDGE('',*,*,#4193,.F.);
#2518=ORIENTED_EDGE('',*,*,#4169,.F.);
#2519=ORIENTED_EDGE('',*,*,#4193,.T.);
#2520=ORIENTED_EDGE('',*,*,#4194,.F.);
#2521=ORIENTED_EDGE('',*,*,#4195,.F.);
#2522=ORIENTED_EDGE('',*,*,#4195,.T.);
#2523=ORIENTED_EDGE('',*,*,#4196,.F.);
#2524=ORIENTED_EDGE('',*,*,#4197,.F.);
#2525=ORIENTED_EDGE('',*,*,#4144,.F.);
#2526=ORIENTED_EDGE('',*,*,#4145,.F.);
#2527=ORIENTED_EDGE('',*,*,#4197,.T.);
#2528=ORIENTED_EDGE('',*,*,#4198,.F.);
#2529=ORIENTED_EDGE('',*,*,#4199,.F.);
#2530=ORIENTED_EDGE('',*,*,#4200,.F.);
#2531=ORIENTED_EDGE('',*,*,#4201,.F.);
#2532=ORIENTED_EDGE('',*,*,#4146,.F.);
#2533=ORIENTED_EDGE('',*,*,#4199,.T.);
#2534=ORIENTED_EDGE('',*,*,#4202,.F.);
#2535=ORIENTED_EDGE('',*,*,#4203,.F.);
#2536=ORIENTED_EDGE('',*,*,#4147,.F.);
#2537=ORIENTED_EDGE('',*,*,#4201,.T.);
#2538=ORIENTED_EDGE('',*,*,#4204,.F.);
#2539=ORIENTED_EDGE('',*,*,#4205,.F.);
#2540=ORIENTED_EDGE('',*,*,#4148,.F.);
#2541=ORIENTED_EDGE('',*,*,#4203,.T.);
#2542=ORIENTED_EDGE('',*,*,#4206,.F.);
#2543=ORIENTED_EDGE('',*,*,#4207,.F.);
#2544=ORIENTED_EDGE('',*,*,#4149,.F.);
#2545=ORIENTED_EDGE('',*,*,#4205,.T.);
#2546=ORIENTED_EDGE('',*,*,#4208,.F.);
#2547=ORIENTED_EDGE('',*,*,#4209,.F.);
#2548=ORIENTED_EDGE('',*,*,#4150,.F.);
#2549=ORIENTED_EDGE('',*,*,#4207,.T.);
#2550=ORIENTED_EDGE('',*,*,#4210,.F.);
#2551=ORIENTED_EDGE('',*,*,#4211,.F.);
#2552=ORIENTED_EDGE('',*,*,#4151,.F.);
#2553=ORIENTED_EDGE('',*,*,#4209,.T.);
#2554=ORIENTED_EDGE('',*,*,#4212,.F.);
#2555=ORIENTED_EDGE('',*,*,#4213,.F.);
#2556=ORIENTED_EDGE('',*,*,#4152,.F.);
#2557=ORIENTED_EDGE('',*,*,#4211,.T.);
#2558=ORIENTED_EDGE('',*,*,#4214,.F.);
#2559=ORIENTED_EDGE('',*,*,#4215,.F.);
#2560=ORIENTED_EDGE('',*,*,#4153,.F.);
#2561=ORIENTED_EDGE('',*,*,#4213,.T.);
#2562=ORIENTED_EDGE('',*,*,#4216,.F.);
#2563=ORIENTED_EDGE('',*,*,#4217,.F.);
#2564=ORIENTED_EDGE('',*,*,#4154,.F.);
#2565=ORIENTED_EDGE('',*,*,#4215,.T.);
#2566=ORIENTED_EDGE('',*,*,#4218,.F.);
#2567=ORIENTED_EDGE('',*,*,#4219,.F.);
#2568=ORIENTED_EDGE('',*,*,#4155,.F.);
#2569=ORIENTED_EDGE('',*,*,#4217,.T.);
#2570=ORIENTED_EDGE('',*,*,#4220,.F.);
#2571=ORIENTED_EDGE('',*,*,#4173,.T.);
#2572=ORIENTED_EDGE('',*,*,#4156,.F.);
#2573=ORIENTED_EDGE('',*,*,#4219,.T.);
#2574=ORIENTED_EDGE('',*,*,#4221,.F.);
#2575=ORIENTED_EDGE('',*,*,#4170,.F.);
#2576=ORIENTED_EDGE('',*,*,#4222,.T.);
#2577=ORIENTED_EDGE('',*,*,#4171,.T.);
#2578=ORIENTED_EDGE('',*,*,#4223,.T.);
#2579=ORIENTED_EDGE('',*,*,#4224,.T.);
#2580=ORIENTED_EDGE('',*,*,#4225,.F.);
#2581=ORIENTED_EDGE('',*,*,#4226,.F.);
#2582=ORIENTED_EDGE('',*,*,#4227,.F.);
#2583=ORIENTED_EDGE('',*,*,#4174,.T.);
#2584=ORIENTED_EDGE('',*,*,#4222,.F.);
#2585=ORIENTED_EDGE('',*,*,#4228,.F.);
#2586=ORIENTED_EDGE('',*,*,#4229,.F.);
#2587=ORIENTED_EDGE('',*,*,#4230,.F.);
#2588=ORIENTED_EDGE('',*,*,#4192,.T.);
#2589=ORIENTED_EDGE('',*,*,#4231,.F.);
#2590=ORIENTED_EDGE('',*,*,#4232,.F.);
#2591=ORIENTED_EDGE('',*,*,#4233,.F.);
#2592=ORIENTED_EDGE('',*,*,#4234,.F.);
#2593=ORIENTED_EDGE('',*,*,#4235,.F.);
#2594=ORIENTED_EDGE('',*,*,#4236,.F.);
#2595=ORIENTED_EDGE('',*,*,#4237,.F.);
#2596=ORIENTED_EDGE('',*,*,#4184,.T.);
#2597=ORIENTED_EDGE('',*,*,#4238,.F.);
#2598=ORIENTED_EDGE('',*,*,#4239,.F.);
#2599=ORIENTED_EDGE('',*,*,#4240,.F.);
#2600=ORIENTED_EDGE('',*,*,#4241,.F.);
#2601=ORIENTED_EDGE('',*,*,#4242,.F.);
#2602=ORIENTED_EDGE('',*,*,#4243,.F.);
#2603=ORIENTED_EDGE('',*,*,#4244,.F.);
#2604=ORIENTED_EDGE('',*,*,#4176,.T.);
#2605=ORIENTED_EDGE('',*,*,#4227,.T.);
#2606=ORIENTED_EDGE('',*,*,#4245,.F.);
#2607=ORIENTED_EDGE('',*,*,#4246,.F.);
#2608=ORIENTED_EDGE('',*,*,#4247,.F.);
#2609=ORIENTED_EDGE('',*,*,#4248,.F.);
#2610=ORIENTED_EDGE('',*,*,#4249,.F.);
#2611=ORIENTED_EDGE('',*,*,#4250,.F.);
#2612=ORIENTED_EDGE('',*,*,#4218,.T.);
#2613=ORIENTED_EDGE('',*,*,#4251,.F.);
#2614=ORIENTED_EDGE('',*,*,#4252,.F.);
#2615=ORIENTED_EDGE('',*,*,#4253,.F.);
#2616=ORIENTED_EDGE('',*,*,#4254,.F.);
#2617=ORIENTED_EDGE('',*,*,#4255,.F.);
#2618=ORIENTED_EDGE('',*,*,#4256,.F.);
#2619=ORIENTED_EDGE('',*,*,#4257,.F.);
#2620=ORIENTED_EDGE('',*,*,#4210,.T.);
#2621=ORIENTED_EDGE('',*,*,#4258,.F.);
#2622=ORIENTED_EDGE('',*,*,#4259,.F.);
#2623=ORIENTED_EDGE('',*,*,#4260,.F.);
#2624=ORIENTED_EDGE('',*,*,#4261,.F.);
#2625=ORIENTED_EDGE('',*,*,#4262,.F.);
#2626=ORIENTED_EDGE('',*,*,#4263,.F.);
#2627=ORIENTED_EDGE('',*,*,#4264,.F.);
#2628=ORIENTED_EDGE('',*,*,#4202,.T.);
#2629=ORIENTED_EDGE('',*,*,#4265,.F.);
#2630=ORIENTED_EDGE('',*,*,#4266,.F.);
#2631=ORIENTED_EDGE('',*,*,#4267,.F.);
#2632=ORIENTED_EDGE('',*,*,#4268,.F.);
#2633=ORIENTED_EDGE('',*,*,#4269,.F.);
#2634=ORIENTED_EDGE('',*,*,#4270,.F.);
#2635=ORIENTED_EDGE('',*,*,#4271,.F.);
#2636=ORIENTED_EDGE('',*,*,#4272,.F.);
#2637=ORIENTED_EDGE('',*,*,#4273,.F.);
#2638=ORIENTED_EDGE('',*,*,#4274,.F.);
#2639=ORIENTED_EDGE('',*,*,#4275,.F.);
#2640=ORIENTED_EDGE('',*,*,#4276,.F.);
#2641=ORIENTED_EDGE('',*,*,#4277,.F.);
#2642=ORIENTED_EDGE('',*,*,#4278,.F.);
#2643=ORIENTED_EDGE('',*,*,#4279,.F.);
#2644=ORIENTED_EDGE('',*,*,#4280,.F.);
#2645=ORIENTED_EDGE('',*,*,#4281,.F.);
#2646=ORIENTED_EDGE('',*,*,#4282,.F.);
#2647=ORIENTED_EDGE('',*,*,#4283,.F.);
#2648=ORIENTED_EDGE('',*,*,#4284,.F.);
#2649=ORIENTED_EDGE('',*,*,#4285,.F.);
#2650=ORIENTED_EDGE('',*,*,#4286,.F.);
#2651=ORIENTED_EDGE('',*,*,#4287,.F.);
#2652=ORIENTED_EDGE('',*,*,#4244,.T.);
#2653=ORIENTED_EDGE('',*,*,#4288,.F.);
#2654=ORIENTED_EDGE('',*,*,#4289,.F.);
#2655=ORIENTED_EDGE('',*,*,#4290,.F.);
#2656=ORIENTED_EDGE('',*,*,#4178,.T.);
#2657=ORIENTED_EDGE('',*,*,#4291,.T.);
#2658=ORIENTED_EDGE('',*,*,#4180,.T.);
#2659=ORIENTED_EDGE('',*,*,#4290,.T.);
#2660=ORIENTED_EDGE('',*,*,#4292,.T.);
#2661=ORIENTED_EDGE('',*,*,#4182,.T.);
#2662=ORIENTED_EDGE('',*,*,#4291,.F.);
#2663=ORIENTED_EDGE('',*,*,#4293,.F.);
#2664=ORIENTED_EDGE('',*,*,#4294,.F.);
#2665=ORIENTED_EDGE('',*,*,#4238,.T.);
#2666=ORIENTED_EDGE('',*,*,#4237,.T.);
#2667=ORIENTED_EDGE('',*,*,#4295,.F.);
#2668=ORIENTED_EDGE('',*,*,#4296,.F.);
#2669=ORIENTED_EDGE('',*,*,#4297,.F.);
#2670=ORIENTED_EDGE('',*,*,#4186,.T.);
#2671=ORIENTED_EDGE('',*,*,#4297,.T.);
#2672=ORIENTED_EDGE('',*,*,#4298,.T.);
#2673=ORIENTED_EDGE('',*,*,#4299,.T.);
#2674=ORIENTED_EDGE('',*,*,#4188,.T.);
#2675=ORIENTED_EDGE('',*,*,#4190,.T.);
#2676=ORIENTED_EDGE('',*,*,#4299,.F.);
#2677=ORIENTED_EDGE('',*,*,#4300,.F.);
#2678=ORIENTED_EDGE('',*,*,#4301,.F.);
#2679=ORIENTED_EDGE('',*,*,#4231,.T.);
#2680=ORIENTED_EDGE('',*,*,#4230,.T.);
#2681=ORIENTED_EDGE('',*,*,#4302,.F.);
#2682=ORIENTED_EDGE('',*,*,#4303,.F.);
#2683=ORIENTED_EDGE('',*,*,#4304,.F.);
#2684=ORIENTED_EDGE('',*,*,#4194,.T.);
#2685=ORIENTED_EDGE('',*,*,#4305,.T.);
#2686=ORIENTED_EDGE('',*,*,#4306,.T.);
#2687=ORIENTED_EDGE('',*,*,#4198,.T.);
#2688=ORIENTED_EDGE('',*,*,#4196,.T.);
#2689=ORIENTED_EDGE('',*,*,#4304,.T.);
#2690=ORIENTED_EDGE('',*,*,#4200,.T.);
#2691=ORIENTED_EDGE('',*,*,#4306,.F.);
#2692=ORIENTED_EDGE('',*,*,#4307,.F.);
#2693=ORIENTED_EDGE('',*,*,#4308,.F.);
#2694=ORIENTED_EDGE('',*,*,#4265,.T.);
#2695=ORIENTED_EDGE('',*,*,#4264,.T.);
#2696=ORIENTED_EDGE('',*,*,#4309,.F.);
#2697=ORIENTED_EDGE('',*,*,#4310,.F.);
#2698=ORIENTED_EDGE('',*,*,#4311,.F.);
#2699=ORIENTED_EDGE('',*,*,#4204,.T.);
#2700=ORIENTED_EDGE('',*,*,#4311,.T.);
#2701=ORIENTED_EDGE('',*,*,#4312,.T.);
#2702=ORIENTED_EDGE('',*,*,#4313,.T.);
#2703=ORIENTED_EDGE('',*,*,#4206,.T.);
#2704=ORIENTED_EDGE('',*,*,#4208,.T.);
#2705=ORIENTED_EDGE('',*,*,#4313,.F.);
#2706=ORIENTED_EDGE('',*,*,#4314,.F.);
#2707=ORIENTED_EDGE('',*,*,#4315,.F.);
#2708=ORIENTED_EDGE('',*,*,#4258,.T.);
#2709=ORIENTED_EDGE('',*,*,#4257,.T.);
#2710=ORIENTED_EDGE('',*,*,#4316,.F.);
#2711=ORIENTED_EDGE('',*,*,#4317,.F.);
#2712=ORIENTED_EDGE('',*,*,#4318,.F.);
#2713=ORIENTED_EDGE('',*,*,#4212,.T.);
#2714=ORIENTED_EDGE('',*,*,#4319,.T.);
#2715=ORIENTED_EDGE('',*,*,#4214,.T.);
#2716=ORIENTED_EDGE('',*,*,#4318,.T.);
#2717=ORIENTED_EDGE('',*,*,#4320,.T.);
#2718=ORIENTED_EDGE('',*,*,#4216,.T.);
#2719=ORIENTED_EDGE('',*,*,#4319,.F.);
#2720=ORIENTED_EDGE('',*,*,#4321,.F.);
#2721=ORIENTED_EDGE('',*,*,#4322,.F.);
#2722=ORIENTED_EDGE('',*,*,#4251,.T.);
#2723=ORIENTED_EDGE('',*,*,#4323,.F.);
#2724=ORIENTED_EDGE('',*,*,#4223,.F.);
#2725=ORIENTED_EDGE('',*,*,#4220,.T.);
#2726=ORIENTED_EDGE('',*,*,#4250,.T.);
#2727=ORIENTED_EDGE('',*,*,#4324,.F.);
#2728=ORIENTED_EDGE('',*,*,#4325,.T.);
#2729=ORIENTED_EDGE('',*,*,#4326,.T.);
#2730=ORIENTED_EDGE('',*,*,#4221,.T.);
#2731=ORIENTED_EDGE('',*,*,#4327,.F.);
#2732=ORIENTED_EDGE('',*,*,#4328,.F.);
#2733=ORIENTED_EDGE('',*,*,#4329,.F.);
#2734=ORIENTED_EDGE('',*,*,#4330,.F.);
#2735=ORIENTED_EDGE('',*,*,#4293,.T.);
#2736=ORIENTED_EDGE('',*,*,#4292,.F.);
#2737=ORIENTED_EDGE('',*,*,#4289,.T.);
#2738=ORIENTED_EDGE('',*,*,#4331,.F.);
#2739=ORIENTED_EDGE('',*,*,#4332,.F.);
#2740=ORIENTED_EDGE('',*,*,#4333,.F.);
#2741=ORIENTED_EDGE('',*,*,#4296,.T.);
#2742=ORIENTED_EDGE('',*,*,#4334,.F.);
#2743=ORIENTED_EDGE('',*,*,#4335,.F.);
#2744=ORIENTED_EDGE('',*,*,#4336,.F.);
#2745=ORIENTED_EDGE('',*,*,#4337,.F.);
#2746=ORIENTED_EDGE('',*,*,#4338,.F.);
#2747=ORIENTED_EDGE('',*,*,#4300,.T.);
#2748=ORIENTED_EDGE('',*,*,#4298,.F.);
#2749=ORIENTED_EDGE('',*,*,#4303,.T.);
#2750=ORIENTED_EDGE('',*,*,#4339,.F.);
#2751=ORIENTED_EDGE('',*,*,#4340,.F.);
#2752=ORIENTED_EDGE('',*,*,#4341,.F.);
#2753=ORIENTED_EDGE('',*,*,#4342,.F.);
#2754=ORIENTED_EDGE('',*,*,#4343,.F.);
#2755=ORIENTED_EDGE('',*,*,#4307,.T.);
#2756=ORIENTED_EDGE('',*,*,#4305,.F.);
#2757=ORIENTED_EDGE('',*,*,#4310,.T.);
#2758=ORIENTED_EDGE('',*,*,#4344,.F.);
#2759=ORIENTED_EDGE('',*,*,#4345,.F.);
#2760=ORIENTED_EDGE('',*,*,#4346,.F.);
#2761=ORIENTED_EDGE('',*,*,#4347,.F.);
#2762=ORIENTED_EDGE('',*,*,#4348,.F.);
#2763=ORIENTED_EDGE('',*,*,#4314,.T.);
#2764=ORIENTED_EDGE('',*,*,#4312,.F.);
#2765=ORIENTED_EDGE('',*,*,#4317,.T.);
#2766=ORIENTED_EDGE('',*,*,#4349,.F.);
#2767=ORIENTED_EDGE('',*,*,#4350,.F.);
#2768=ORIENTED_EDGE('',*,*,#4351,.F.);
#2769=ORIENTED_EDGE('',*,*,#4352,.F.);
#2770=ORIENTED_EDGE('',*,*,#4353,.F.);
#2771=ORIENTED_EDGE('',*,*,#4321,.T.);
#2772=ORIENTED_EDGE('',*,*,#4320,.F.);
#2773=ORIENTED_EDGE('',*,*,#4354,.F.);
#2774=ORIENTED_EDGE('',*,*,#4355,.F.);
#2775=ORIENTED_EDGE('',*,*,#4225,.T.);
#2776=ORIENTED_EDGE('',*,*,#4224,.F.);
#2777=ORIENTED_EDGE('',*,*,#4323,.T.);
#2778=ORIENTED_EDGE('',*,*,#4356,.F.);
#2779=ORIENTED_EDGE('',*,*,#4357,.F.);
#2780=ORIENTED_EDGE('',*,*,#4358,.F.);
#2781=ORIENTED_EDGE('',*,*,#4359,.F.);
#2782=ORIENTED_EDGE('',*,*,#4360,.F.);
#2783=ORIENTED_EDGE('',*,*,#4361,.F.);
#2784=ORIENTED_EDGE('',*,*,#4362,.F.);
#2785=ORIENTED_EDGE('',*,*,#4363,.F.);
#2786=ORIENTED_EDGE('',*,*,#4364,.F.);
#2787=ORIENTED_EDGE('',*,*,#4365,.F.);
#2788=ORIENTED_EDGE('',*,*,#4366,.F.);
#2789=ORIENTED_EDGE('',*,*,#4367,.F.);
#2790=ORIENTED_EDGE('',*,*,#4368,.F.);
#2791=ORIENTED_EDGE('',*,*,#4369,.F.);
#2792=ORIENTED_EDGE('',*,*,#4370,.F.);
#2793=ORIENTED_EDGE('',*,*,#4371,.F.);
#2794=ORIENTED_EDGE('',*,*,#4372,.F.);
#2795=ORIENTED_EDGE('',*,*,#4373,.F.);
#2796=ORIENTED_EDGE('',*,*,#4374,.F.);
#2797=ORIENTED_EDGE('',*,*,#4375,.F.);
#2798=ORIENTED_EDGE('',*,*,#4376,.F.);
#2799=ORIENTED_EDGE('',*,*,#4377,.F.);
#2800=ORIENTED_EDGE('',*,*,#4245,.T.);
#2801=ORIENTED_EDGE('',*,*,#4226,.T.);
#2802=ORIENTED_EDGE('',*,*,#4355,.T.);
#2803=ORIENTED_EDGE('',*,*,#4287,.T.);
#2804=ORIENTED_EDGE('',*,*,#4376,.T.);
#2805=ORIENTED_EDGE('',*,*,#4375,.T.);
#2806=ORIENTED_EDGE('',*,*,#4286,.T.);
#2807=ORIENTED_EDGE('',*,*,#4285,.T.);
#2808=ORIENTED_EDGE('',*,*,#4374,.T.);
#2809=ORIENTED_EDGE('',*,*,#4284,.T.);
#2810=ORIENTED_EDGE('',*,*,#4373,.T.);
#2811=ORIENTED_EDGE('',*,*,#4283,.T.);
#2812=ORIENTED_EDGE('',*,*,#4372,.T.);
#2813=ORIENTED_EDGE('',*,*,#4282,.T.);
#2814=ORIENTED_EDGE('',*,*,#4371,.T.);
#2815=ORIENTED_EDGE('',*,*,#4281,.T.);
#2816=ORIENTED_EDGE('',*,*,#4370,.T.);
#2817=ORIENTED_EDGE('',*,*,#4280,.T.);
#2818=ORIENTED_EDGE('',*,*,#4369,.T.);
#2819=ORIENTED_EDGE('',*,*,#4279,.T.);
#2820=ORIENTED_EDGE('',*,*,#4368,.T.);
#2821=ORIENTED_EDGE('',*,*,#4278,.T.);
#2822=ORIENTED_EDGE('',*,*,#4367,.T.);
#2823=ORIENTED_EDGE('',*,*,#4277,.T.);
#2824=ORIENTED_EDGE('',*,*,#4366,.T.);
#2825=ORIENTED_EDGE('',*,*,#4276,.T.);
#2826=ORIENTED_EDGE('',*,*,#4365,.T.);
#2827=ORIENTED_EDGE('',*,*,#4275,.T.);
#2828=ORIENTED_EDGE('',*,*,#4364,.T.);
#2829=ORIENTED_EDGE('',*,*,#4274,.T.);
#2830=ORIENTED_EDGE('',*,*,#4363,.T.);
#2831=ORIENTED_EDGE('',*,*,#4273,.T.);
#2832=ORIENTED_EDGE('',*,*,#4362,.T.);
#2833=ORIENTED_EDGE('',*,*,#4272,.T.);
#2834=ORIENTED_EDGE('',*,*,#4361,.T.);
#2835=ORIENTED_EDGE('',*,*,#4271,.T.);
#2836=ORIENTED_EDGE('',*,*,#4360,.T.);
#2837=ORIENTED_EDGE('',*,*,#4270,.T.);
#2838=ORIENTED_EDGE('',*,*,#4359,.T.);
#2839=ORIENTED_EDGE('',*,*,#4378,.F.);
#2840=ORIENTED_EDGE('',*,*,#4232,.T.);
#2841=ORIENTED_EDGE('',*,*,#4301,.T.);
#2842=ORIENTED_EDGE('',*,*,#4338,.T.);
#2843=ORIENTED_EDGE('',*,*,#4378,.T.);
#2844=ORIENTED_EDGE('',*,*,#4337,.T.);
#2845=ORIENTED_EDGE('',*,*,#4379,.F.);
#2846=ORIENTED_EDGE('',*,*,#4233,.T.);
#2847=ORIENTED_EDGE('',*,*,#4234,.T.);
#2848=ORIENTED_EDGE('',*,*,#4379,.T.);
#2849=ORIENTED_EDGE('',*,*,#4336,.T.);
#2850=ORIENTED_EDGE('',*,*,#4380,.F.);
#2851=ORIENTED_EDGE('',*,*,#4235,.T.);
#2852=ORIENTED_EDGE('',*,*,#4380,.T.);
#2853=ORIENTED_EDGE('',*,*,#4335,.T.);
#2854=ORIENTED_EDGE('',*,*,#4381,.F.);
#2855=ORIENTED_EDGE('',*,*,#4381,.T.);
#2856=ORIENTED_EDGE('',*,*,#4334,.T.);
#2857=ORIENTED_EDGE('',*,*,#4295,.T.);
#2858=ORIENTED_EDGE('',*,*,#4236,.T.);
#2859=ORIENTED_EDGE('',*,*,#4382,.F.);
#2860=ORIENTED_EDGE('',*,*,#4239,.T.);
#2861=ORIENTED_EDGE('',*,*,#4294,.T.);
#2862=ORIENTED_EDGE('',*,*,#4330,.T.);
#2863=ORIENTED_EDGE('',*,*,#4382,.T.);
#2864=ORIENTED_EDGE('',*,*,#4329,.T.);
#2865=ORIENTED_EDGE('',*,*,#4383,.F.);
#2866=ORIENTED_EDGE('',*,*,#4240,.T.);
#2867=ORIENTED_EDGE('',*,*,#4241,.T.);
#2868=ORIENTED_EDGE('',*,*,#4383,.T.);
#2869=ORIENTED_EDGE('',*,*,#4333,.T.);
#2870=ORIENTED_EDGE('',*,*,#4384,.F.);
#2871=ORIENTED_EDGE('',*,*,#4242,.T.);
#2872=ORIENTED_EDGE('',*,*,#4384,.T.);
#2873=ORIENTED_EDGE('',*,*,#4332,.T.);
#2874=ORIENTED_EDGE('',*,*,#4385,.F.);
#2875=ORIENTED_EDGE('',*,*,#4385,.T.);
#2876=ORIENTED_EDGE('',*,*,#4331,.T.);
#2877=ORIENTED_EDGE('',*,*,#4288,.T.);
#2878=ORIENTED_EDGE('',*,*,#4243,.T.);
#2879=ORIENTED_EDGE('',*,*,#4246,.T.);
#2880=ORIENTED_EDGE('',*,*,#4377,.T.);
#2881=ORIENTED_EDGE('',*,*,#4354,.T.);
#2882=ORIENTED_EDGE('',*,*,#4386,.F.);
#2883=ORIENTED_EDGE('',*,*,#4247,.T.);
#2884=ORIENTED_EDGE('',*,*,#4386,.T.);
#2885=ORIENTED_EDGE('',*,*,#4358,.T.);
#2886=ORIENTED_EDGE('',*,*,#4387,.F.);
#2887=ORIENTED_EDGE('',*,*,#4248,.T.);
#2888=ORIENTED_EDGE('',*,*,#4387,.T.);
#2889=ORIENTED_EDGE('',*,*,#4357,.T.);
#2890=ORIENTED_EDGE('',*,*,#4388,.F.);
#2891=ORIENTED_EDGE('',*,*,#4388,.T.);
#2892=ORIENTED_EDGE('',*,*,#4356,.T.);
#2893=ORIENTED_EDGE('',*,*,#4324,.T.);
#2894=ORIENTED_EDGE('',*,*,#4249,.T.);
#2895=ORIENTED_EDGE('',*,*,#4389,.F.);
#2896=ORIENTED_EDGE('',*,*,#4252,.T.);
#2897=ORIENTED_EDGE('',*,*,#4322,.T.);
#2898=ORIENTED_EDGE('',*,*,#4353,.T.);
#2899=ORIENTED_EDGE('',*,*,#4253,.T.);
#2900=ORIENTED_EDGE('',*,*,#4389,.T.);
#2901=ORIENTED_EDGE('',*,*,#4352,.T.);
#2902=ORIENTED_EDGE('',*,*,#4390,.F.);
#2903=ORIENTED_EDGE('',*,*,#4351,.T.);
#2904=ORIENTED_EDGE('',*,*,#4391,.F.);
#2905=ORIENTED_EDGE('',*,*,#4254,.T.);
#2906=ORIENTED_EDGE('',*,*,#4390,.T.);
#2907=ORIENTED_EDGE('',*,*,#4391,.T.);
#2908=ORIENTED_EDGE('',*,*,#4350,.T.);
#2909=ORIENTED_EDGE('',*,*,#4392,.F.);
#2910=ORIENTED_EDGE('',*,*,#4255,.T.);
#2911=ORIENTED_EDGE('',*,*,#4392,.T.);
#2912=ORIENTED_EDGE('',*,*,#4349,.T.);
#2913=ORIENTED_EDGE('',*,*,#4316,.T.);
#2914=ORIENTED_EDGE('',*,*,#4256,.T.);
#2915=ORIENTED_EDGE('',*,*,#4393,.F.);
#2916=ORIENTED_EDGE('',*,*,#4259,.T.);
#2917=ORIENTED_EDGE('',*,*,#4315,.T.);
#2918=ORIENTED_EDGE('',*,*,#4348,.T.);
#2919=ORIENTED_EDGE('',*,*,#4260,.T.);
#2920=ORIENTED_EDGE('',*,*,#4393,.T.);
#2921=ORIENTED_EDGE('',*,*,#4347,.T.);
#2922=ORIENTED_EDGE('',*,*,#4394,.F.);
#2923=ORIENTED_EDGE('',*,*,#4346,.T.);
#2924=ORIENTED_EDGE('',*,*,#4395,.F.);
#2925=ORIENTED_EDGE('',*,*,#4261,.T.);
#2926=ORIENTED_EDGE('',*,*,#4394,.T.);
#2927=ORIENTED_EDGE('',*,*,#4395,.T.);
#2928=ORIENTED_EDGE('',*,*,#4345,.T.);
#2929=ORIENTED_EDGE('',*,*,#4396,.F.);
#2930=ORIENTED_EDGE('',*,*,#4262,.T.);
#2931=ORIENTED_EDGE('',*,*,#4396,.T.);
#2932=ORIENTED_EDGE('',*,*,#4344,.T.);
#2933=ORIENTED_EDGE('',*,*,#4309,.T.);
#2934=ORIENTED_EDGE('',*,*,#4263,.T.);
#2935=ORIENTED_EDGE('',*,*,#4397,.F.);
#2936=ORIENTED_EDGE('',*,*,#4266,.T.);
#2937=ORIENTED_EDGE('',*,*,#4308,.T.);
#2938=ORIENTED_EDGE('',*,*,#4343,.T.);
#2939=ORIENTED_EDGE('',*,*,#4267,.T.);
#2940=ORIENTED_EDGE('',*,*,#4397,.T.);
#2941=ORIENTED_EDGE('',*,*,#4342,.T.);
#2942=ORIENTED_EDGE('',*,*,#4398,.F.);
#2943=ORIENTED_EDGE('',*,*,#4398,.T.);
#2944=ORIENTED_EDGE('',*,*,#4341,.T.);
#2945=ORIENTED_EDGE('',*,*,#4399,.F.);
#2946=ORIENTED_EDGE('',*,*,#4268,.T.);
#2947=ORIENTED_EDGE('',*,*,#4269,.T.);
#2948=ORIENTED_EDGE('',*,*,#4399,.T.);
#2949=ORIENTED_EDGE('',*,*,#4340,.T.);
#2950=ORIENTED_EDGE('',*,*,#4400,.F.);
#2951=ORIENTED_EDGE('',*,*,#4400,.T.);
#2952=ORIENTED_EDGE('',*,*,#4339,.T.);
#2953=ORIENTED_EDGE('',*,*,#4302,.T.);
#2954=ORIENTED_EDGE('',*,*,#4229,.T.);
#2955=ORIENTED_EDGE('',*,*,#4401,.T.);
#2956=ORIENTED_EDGE('',*,*,#4402,.T.);
#2957=ORIENTED_EDGE('',*,*,#4228,.T.);
#2958=ORIENTED_EDGE('',*,*,#4403,.T.);
#2959=ORIENTED_EDGE('',*,*,#4404,.T.);
#2960=ORIENTED_EDGE('',*,*,#4326,.F.);
#2961=ORIENTED_EDGE('',*,*,#4325,.F.);
#2962=ORIENTED_EDGE('',*,*,#4405,.F.);
#2963=ORIENTED_EDGE('',*,*,#4406,.F.);
#2964=ORIENTED_EDGE('',*,*,#4328,.T.);
#2965=ORIENTED_EDGE('',*,*,#4407,.T.);
#2966=ORIENTED_EDGE('',*,*,#4408,.T.);
#2967=ORIENTED_EDGE('',*,*,#4327,.T.);
#2968=ORIENTED_EDGE('',*,*,#4401,.F.);
#2969=ORIENTED_EDGE('',*,*,#4402,.F.);
#2970=ORIENTED_EDGE('',*,*,#4408,.F.);
#2971=ORIENTED_EDGE('',*,*,#4407,.F.);
#2972=ORIENTED_EDGE('',*,*,#4409,.F.);
#2973=ORIENTED_EDGE('',*,*,#4404,.F.);
#2974=ORIENTED_EDGE('',*,*,#4403,.F.);
#2975=ORIENTED_EDGE('',*,*,#4406,.T.);
#2976=ORIENTED_EDGE('',*,*,#4405,.T.);
#2977=ORIENTED_EDGE('',*,*,#4410,.T.);
#2978=ORIENTED_EDGE('',*,*,#4411,.T.);
#2979=ORIENTED_EDGE('',*,*,#4412,.F.);
#2980=ORIENTED_EDGE('',*,*,#4413,.F.);
#2981=ORIENTED_EDGE('',*,*,#4414,.F.);
#2982=ORIENTED_EDGE('',*,*,#4415,.F.);
#2983=ORIENTED_EDGE('',*,*,#4416,.F.);
#2984=ORIENTED_EDGE('',*,*,#4417,.F.);
#2985=ORIENTED_EDGE('',*,*,#4418,.F.);
#2986=ORIENTED_EDGE('',*,*,#4419,.F.);
#2987=ORIENTED_EDGE('',*,*,#4420,.F.);
#2988=ORIENTED_EDGE('',*,*,#4421,.F.);
#2989=ORIENTED_EDGE('',*,*,#4422,.F.);
#2990=ORIENTED_EDGE('',*,*,#4423,.F.);
#2991=ORIENTED_EDGE('',*,*,#4424,.F.);
#2992=ORIENTED_EDGE('',*,*,#4425,.F.);
#2993=ORIENTED_EDGE('',*,*,#4426,.F.);
#2994=ORIENTED_EDGE('',*,*,#4427,.F.);
#2995=ORIENTED_EDGE('',*,*,#4428,.F.);
#2996=ORIENTED_EDGE('',*,*,#4429,.F.);
#2997=ORIENTED_EDGE('',*,*,#4430,.F.);
#2998=ORIENTED_EDGE('',*,*,#4431,.F.);
#2999=ORIENTED_EDGE('',*,*,#4432,.F.);
#3000=ORIENTED_EDGE('',*,*,#4433,.F.);
#3001=ORIENTED_EDGE('',*,*,#4434,.F.);
#3002=ORIENTED_EDGE('',*,*,#4435,.F.);
#3003=ORIENTED_EDGE('',*,*,#4436,.F.);
#3004=ORIENTED_EDGE('',*,*,#4437,.F.);
#3005=ORIENTED_EDGE('',*,*,#4438,.F.);
#3006=ORIENTED_EDGE('',*,*,#4439,.F.);
#3007=ORIENTED_EDGE('',*,*,#4440,.F.);
#3008=ORIENTED_EDGE('',*,*,#4441,.F.);
#3009=ORIENTED_EDGE('',*,*,#4442,.F.);
#3010=ORIENTED_EDGE('',*,*,#4443,.F.);
#3011=ORIENTED_EDGE('',*,*,#4409,.T.);
#3012=ORIENTED_EDGE('',*,*,#4410,.F.);
#3013=ORIENTED_EDGE('',*,*,#4444,.F.);
#3014=ORIENTED_EDGE('',*,*,#4445,.F.);
#3015=ORIENTED_EDGE('',*,*,#4446,.F.);
#3016=ORIENTED_EDGE('',*,*,#4447,.F.);
#3017=ORIENTED_EDGE('',*,*,#4448,.F.);
#3018=ORIENTED_EDGE('',*,*,#4449,.F.);
#3019=ORIENTED_EDGE('',*,*,#4450,.F.);
#3020=ORIENTED_EDGE('',*,*,#4451,.F.);
#3021=ORIENTED_EDGE('',*,*,#4452,.F.);
#3022=ORIENTED_EDGE('',*,*,#4453,.F.);
#3023=ORIENTED_EDGE('',*,*,#4454,.F.);
#3024=ORIENTED_EDGE('',*,*,#4455,.F.);
#3025=ORIENTED_EDGE('',*,*,#4456,.F.);
#3026=ORIENTED_EDGE('',*,*,#4457,.F.);
#3027=ORIENTED_EDGE('',*,*,#4458,.F.);
#3028=ORIENTED_EDGE('',*,*,#4459,.F.);
#3029=ORIENTED_EDGE('',*,*,#4460,.F.);
#3030=ORIENTED_EDGE('',*,*,#4444,.T.);
#3031=ORIENTED_EDGE('',*,*,#4411,.F.);
#3032=ORIENTED_EDGE('',*,*,#4458,.T.);
#3033=ORIENTED_EDGE('',*,*,#4461,.F.);
#3034=ORIENTED_EDGE('',*,*,#4462,.F.);
#3035=ORIENTED_EDGE('',*,*,#4463,.F.);
#3036=ORIENTED_EDGE('',*,*,#4464,.F.);
#3037=ORIENTED_EDGE('',*,*,#4465,.F.);
#3038=ORIENTED_EDGE('',*,*,#4466,.F.);
#3039=ORIENTED_EDGE('',*,*,#4467,.F.);
#3040=ORIENTED_EDGE('',*,*,#4468,.F.);
#3041=ORIENTED_EDGE('',*,*,#4469,.F.);
#3042=ORIENTED_EDGE('',*,*,#4470,.F.);
#3043=ORIENTED_EDGE('',*,*,#4471,.F.);
#3044=ORIENTED_EDGE('',*,*,#4443,.T.);
#3045=ORIENTED_EDGE('',*,*,#4472,.T.);
#3046=ORIENTED_EDGE('',*,*,#4473,.T.);
#3047=ORIENTED_EDGE('',*,*,#4474,.T.);
#3048=ORIENTED_EDGE('',*,*,#4475,.T.);
#3049=ORIENTED_EDGE('',*,*,#4442,.T.);
#3050=ORIENTED_EDGE('',*,*,#4476,.T.);
#3051=ORIENTED_EDGE('',*,*,#4475,.F.);
#3052=ORIENTED_EDGE('',*,*,#4477,.T.);
#3053=ORIENTED_EDGE('',*,*,#4476,.F.);
#3054=ORIENTED_EDGE('',*,*,#4441,.T.);
#3055=ORIENTED_EDGE('',*,*,#4478,.T.);
#3056=ORIENTED_EDGE('',*,*,#4479,.T.);
#3057=ORIENTED_EDGE('',*,*,#4480,.T.);
#3058=ORIENTED_EDGE('',*,*,#4440,.T.);
#3059=ORIENTED_EDGE('',*,*,#4481,.T.);
#3060=ORIENTED_EDGE('',*,*,#4482,.T.);
#3061=ORIENTED_EDGE('',*,*,#4483,.T.);
#3062=ORIENTED_EDGE('',*,*,#4439,.T.);
#3063=ORIENTED_EDGE('',*,*,#4484,.T.);
#3064=ORIENTED_EDGE('',*,*,#4485,.T.);
#3065=ORIENTED_EDGE('',*,*,#4438,.T.);
#3066=ORIENTED_EDGE('',*,*,#4486,.T.);
#3067=ORIENTED_EDGE('',*,*,#4485,.F.);
#3068=ORIENTED_EDGE('',*,*,#4487,.T.);
#3069=ORIENTED_EDGE('',*,*,#4486,.F.);
#3070=ORIENTED_EDGE('',*,*,#4437,.T.);
#3071=ORIENTED_EDGE('',*,*,#4488,.T.);
#3072=ORIENTED_EDGE('',*,*,#4489,.T.);
#3073=ORIENTED_EDGE('',*,*,#4436,.T.);
#3074=ORIENTED_EDGE('',*,*,#4464,.T.);
#3075=ORIENTED_EDGE('',*,*,#4490,.F.);
#3076=ORIENTED_EDGE('',*,*,#4491,.F.);
#3077=ORIENTED_EDGE('',*,*,#4492,.F.);
#3078=ORIENTED_EDGE('',*,*,#4413,.T.);
#3079=ORIENTED_EDGE('',*,*,#4493,.F.);
#3080=ORIENTED_EDGE('',*,*,#4494,.T.);
#3081=ORIENTED_EDGE('',*,*,#4495,.T.);
#3082=ORIENTED_EDGE('',*,*,#4496,.T.);
#3083=ORIENTED_EDGE('',*,*,#4497,.T.);
#3084=ORIENTED_EDGE('',*,*,#4414,.T.);
#3085=ORIENTED_EDGE('',*,*,#4492,.T.);
#3086=ORIENTED_EDGE('',*,*,#4415,.T.);
#3087=ORIENTED_EDGE('',*,*,#4497,.F.);
#3088=ORIENTED_EDGE('',*,*,#4498,.F.);
#3089=ORIENTED_EDGE('',*,*,#4499,.F.);
#3090=ORIENTED_EDGE('',*,*,#4462,.T.);
#3091=ORIENTED_EDGE('',*,*,#4500,.F.);
#3092=ORIENTED_EDGE('',*,*,#4500,.T.);
#3093=ORIENTED_EDGE('',*,*,#4461,.T.);
#3094=ORIENTED_EDGE('',*,*,#4457,.T.);
#3095=ORIENTED_EDGE('',*,*,#4501,.T.);
#3096=ORIENTED_EDGE('',*,*,#4416,.T.);
#3097=ORIENTED_EDGE('',*,*,#4456,.T.);
#3098=ORIENTED_EDGE('',*,*,#4502,.F.);
#3099=ORIENTED_EDGE('',*,*,#4503,.F.);
#3100=ORIENTED_EDGE('',*,*,#4504,.F.);
#3101=ORIENTED_EDGE('',*,*,#4417,.T.);
#3102=ORIENTED_EDGE('',*,*,#4501,.F.);
#3103=ORIENTED_EDGE('',*,*,#4505,.T.);
#3104=ORIENTED_EDGE('',*,*,#4506,.T.);
#3105=ORIENTED_EDGE('',*,*,#4507,.T.);
#3106=ORIENTED_EDGE('',*,*,#4508,.T.);
#3107=ORIENTED_EDGE('',*,*,#4418,.T.);
#3108=ORIENTED_EDGE('',*,*,#4504,.T.);
#3109=ORIENTED_EDGE('',*,*,#4419,.T.);
#3110=ORIENTED_EDGE('',*,*,#4508,.F.);
#3111=ORIENTED_EDGE('',*,*,#4509,.F.);
#3112=ORIENTED_EDGE('',*,*,#4510,.F.);
#3113=ORIENTED_EDGE('',*,*,#4454,.T.);
#3114=ORIENTED_EDGE('',*,*,#4511,.F.);
#3115=ORIENTED_EDGE('',*,*,#4453,.T.);
#3116=ORIENTED_EDGE('',*,*,#4512,.T.);
#3117=ORIENTED_EDGE('',*,*,#4513,.T.);
#3118=ORIENTED_EDGE('',*,*,#4420,.T.);
#3119=ORIENTED_EDGE('',*,*,#4511,.T.);
#3120=ORIENTED_EDGE('',*,*,#4421,.T.);
#3121=ORIENTED_EDGE('',*,*,#4513,.F.);
#3122=ORIENTED_EDGE('',*,*,#4514,.T.);
#3123=ORIENTED_EDGE('',*,*,#4515,.T.);
#3124=ORIENTED_EDGE('',*,*,#4516,.T.);
#3125=ORIENTED_EDGE('',*,*,#4517,.T.);
#3126=ORIENTED_EDGE('',*,*,#4518,.T.);
#3127=ORIENTED_EDGE('',*,*,#4519,.T.);
#3128=ORIENTED_EDGE('',*,*,#4422,.T.);
#3129=ORIENTED_EDGE('',*,*,#4520,.F.);
#3130=ORIENTED_EDGE('',*,*,#4423,.T.);
#3131=ORIENTED_EDGE('',*,*,#4519,.F.);
#3132=ORIENTED_EDGE('',*,*,#4521,.F.);
#3133=ORIENTED_EDGE('',*,*,#4522,.F.);
#3134=ORIENTED_EDGE('',*,*,#4450,.T.);
#3135=ORIENTED_EDGE('',*,*,#4449,.T.);
#3136=ORIENTED_EDGE('',*,*,#4523,.T.);
#3137=ORIENTED_EDGE('',*,*,#4424,.T.);
#3138=ORIENTED_EDGE('',*,*,#4520,.T.);
#3139=ORIENTED_EDGE('',*,*,#4448,.T.);
#3140=ORIENTED_EDGE('',*,*,#4524,.F.);
#3141=ORIENTED_EDGE('',*,*,#4525,.F.);
#3142=ORIENTED_EDGE('',*,*,#4526,.F.);
#3143=ORIENTED_EDGE('',*,*,#4425,.T.);
#3144=ORIENTED_EDGE('',*,*,#4523,.F.);
#3145=ORIENTED_EDGE('',*,*,#4527,.T.);
#3146=ORIENTED_EDGE('',*,*,#4528,.T.);
#3147=ORIENTED_EDGE('',*,*,#4529,.T.);
#3148=ORIENTED_EDGE('',*,*,#4530,.T.);
#3149=ORIENTED_EDGE('',*,*,#4426,.T.);
#3150=ORIENTED_EDGE('',*,*,#4526,.T.);
#3151=ORIENTED_EDGE('',*,*,#4427,.T.);
#3152=ORIENTED_EDGE('',*,*,#4530,.F.);
#3153=ORIENTED_EDGE('',*,*,#4531,.F.);
#3154=ORIENTED_EDGE('',*,*,#4532,.F.);
#3155=ORIENTED_EDGE('',*,*,#4446,.T.);
#3156=ORIENTED_EDGE('',*,*,#4533,.F.);
#3157=ORIENTED_EDGE('',*,*,#4460,.T.);
#3158=ORIENTED_EDGE('',*,*,#4534,.T.);
#3159=ORIENTED_EDGE('',*,*,#4428,.T.);
#3160=ORIENTED_EDGE('',*,*,#4533,.T.);
#3161=ORIENTED_EDGE('',*,*,#4445,.T.);
#3162=ORIENTED_EDGE('',*,*,#4459,.T.);
#3163=ORIENTED_EDGE('',*,*,#4535,.F.);
#3164=ORIENTED_EDGE('',*,*,#4536,.F.);
#3165=ORIENTED_EDGE('',*,*,#4537,.F.);
#3166=ORIENTED_EDGE('',*,*,#4429,.T.);
#3167=ORIENTED_EDGE('',*,*,#4534,.F.);
#3168=ORIENTED_EDGE('',*,*,#4538,.T.);
#3169=ORIENTED_EDGE('',*,*,#4539,.T.);
#3170=ORIENTED_EDGE('',*,*,#4540,.T.);
#3171=ORIENTED_EDGE('',*,*,#4541,.T.);
#3172=ORIENTED_EDGE('',*,*,#4430,.T.);
#3173=ORIENTED_EDGE('',*,*,#4537,.T.);
#3174=ORIENTED_EDGE('',*,*,#4431,.T.);
#3175=ORIENTED_EDGE('',*,*,#4541,.F.);
#3176=ORIENTED_EDGE('',*,*,#4542,.F.);
#3177=ORIENTED_EDGE('',*,*,#4543,.F.);
#3178=ORIENTED_EDGE('',*,*,#4470,.T.);
#3179=ORIENTED_EDGE('',*,*,#4544,.F.);
#3180=ORIENTED_EDGE('',*,*,#4469,.T.);
#3181=ORIENTED_EDGE('',*,*,#4545,.T.);
#3182=ORIENTED_EDGE('',*,*,#4432,.T.);
#3183=ORIENTED_EDGE('',*,*,#4544,.T.);
#3184=ORIENTED_EDGE('',*,*,#4468,.T.);
#3185=ORIENTED_EDGE('',*,*,#4546,.F.);
#3186=ORIENTED_EDGE('',*,*,#4547,.F.);
#3187=ORIENTED_EDGE('',*,*,#4548,.F.);
#3188=ORIENTED_EDGE('',*,*,#4433,.T.);
#3189=ORIENTED_EDGE('',*,*,#4545,.F.);
#3190=ORIENTED_EDGE('',*,*,#4549,.T.);
#3191=ORIENTED_EDGE('',*,*,#4550,.T.);
#3192=ORIENTED_EDGE('',*,*,#4551,.T.);
#3193=ORIENTED_EDGE('',*,*,#4552,.T.);
#3194=ORIENTED_EDGE('',*,*,#4434,.T.);
#3195=ORIENTED_EDGE('',*,*,#4548,.T.);
#3196=ORIENTED_EDGE('',*,*,#4435,.T.);
#3197=ORIENTED_EDGE('',*,*,#4552,.F.);
#3198=ORIENTED_EDGE('',*,*,#4553,.F.);
#3199=ORIENTED_EDGE('',*,*,#4554,.F.);
#3200=ORIENTED_EDGE('',*,*,#4466,.T.);
#3201=ORIENTED_EDGE('',*,*,#4555,.F.);
#3202=ORIENTED_EDGE('',*,*,#4465,.T.);
#3203=ORIENTED_EDGE('',*,*,#4493,.T.);
#3204=ORIENTED_EDGE('',*,*,#4412,.T.);
#3205=ORIENTED_EDGE('',*,*,#4555,.T.);
#3206=ORIENTED_EDGE('',*,*,#4447,.T.);
#3207=ORIENTED_EDGE('',*,*,#4532,.T.);
#3208=ORIENTED_EDGE('',*,*,#4556,.T.);
#3209=ORIENTED_EDGE('',*,*,#4557,.T.);
#3210=ORIENTED_EDGE('',*,*,#4558,.T.);
#3211=ORIENTED_EDGE('',*,*,#4524,.T.);
#3212=ORIENTED_EDGE('',*,*,#4559,.T.);
#3213=ORIENTED_EDGE('',*,*,#4560,.T.);
#3214=ORIENTED_EDGE('',*,*,#4561,.T.);
#3215=ORIENTED_EDGE('',*,*,#4562,.T.);
#3216=ORIENTED_EDGE('',*,*,#4563,.F.);
#3217=ORIENTED_EDGE('',*,*,#4564,.T.);
#3218=ORIENTED_EDGE('',*,*,#4451,.T.);
#3219=ORIENTED_EDGE('',*,*,#4522,.T.);
#3220=ORIENTED_EDGE('',*,*,#4565,.T.);
#3221=ORIENTED_EDGE('',*,*,#4566,.T.);
#3222=ORIENTED_EDGE('',*,*,#4452,.T.);
#3223=ORIENTED_EDGE('',*,*,#4564,.F.);
#3224=ORIENTED_EDGE('',*,*,#4567,.F.);
#3225=ORIENTED_EDGE('',*,*,#4514,.F.);
#3226=ORIENTED_EDGE('',*,*,#4512,.F.);
#3227=ORIENTED_EDGE('',*,*,#4455,.T.);
#3228=ORIENTED_EDGE('',*,*,#4510,.T.);
#3229=ORIENTED_EDGE('',*,*,#4568,.T.);
#3230=ORIENTED_EDGE('',*,*,#4569,.T.);
#3231=ORIENTED_EDGE('',*,*,#4570,.T.);
#3232=ORIENTED_EDGE('',*,*,#4502,.T.);
#3233=ORIENTED_EDGE('',*,*,#4571,.T.);
#3234=ORIENTED_EDGE('',*,*,#4572,.T.);
#3235=ORIENTED_EDGE('',*,*,#4463,.T.);
#3236=ORIENTED_EDGE('',*,*,#4499,.T.);
#3237=ORIENTED_EDGE('',*,*,#4573,.T.);
#3238=ORIENTED_EDGE('',*,*,#4574,.T.);
#3239=ORIENTED_EDGE('',*,*,#4575,.T.);
#3240=ORIENTED_EDGE('',*,*,#4490,.T.);
#3241=ORIENTED_EDGE('',*,*,#4576,.T.);
#3242=ORIENTED_EDGE('',*,*,#4577,.T.);
#3243=ORIENTED_EDGE('',*,*,#4467,.T.);
#3244=ORIENTED_EDGE('',*,*,#4554,.T.);
#3245=ORIENTED_EDGE('',*,*,#4578,.T.);
#3246=ORIENTED_EDGE('',*,*,#4579,.T.);
#3247=ORIENTED_EDGE('',*,*,#4580,.T.);
#3248=ORIENTED_EDGE('',*,*,#4546,.T.);
#3249=ORIENTED_EDGE('',*,*,#4581,.T.);
#3250=ORIENTED_EDGE('',*,*,#4582,.T.);
#3251=ORIENTED_EDGE('',*,*,#4471,.T.);
#3252=ORIENTED_EDGE('',*,*,#4543,.T.);
#3253=ORIENTED_EDGE('',*,*,#4583,.T.);
#3254=ORIENTED_EDGE('',*,*,#4584,.T.);
#3255=ORIENTED_EDGE('',*,*,#4585,.T.);
#3256=ORIENTED_EDGE('',*,*,#4535,.T.);
#3257=ORIENTED_EDGE('',*,*,#4586,.T.);
#3258=ORIENTED_EDGE('',*,*,#4587,.T.);
#3259=ORIENTED_EDGE('',*,*,#4588,.F.);
#3260=ORIENTED_EDGE('',*,*,#4589,.F.);
#3261=ORIENTED_EDGE('',*,*,#4590,.F.);
#3262=ORIENTED_EDGE('',*,*,#4591,.F.);
#3263=ORIENTED_EDGE('',*,*,#4472,.F.);
#3264=ORIENTED_EDGE('',*,*,#4473,.F.);
#3265=ORIENTED_EDGE('',*,*,#4592,.F.);
#3266=ORIENTED_EDGE('',*,*,#4593,.F.);
#3267=ORIENTED_EDGE('',*,*,#4594,.F.);
#3268=ORIENTED_EDGE('',*,*,#4595,.F.);
#3269=ORIENTED_EDGE('',*,*,#4474,.F.);
#3270=ORIENTED_EDGE('',*,*,#4477,.F.);
#3271=ORIENTED_EDGE('',*,*,#4479,.F.);
#3272=ORIENTED_EDGE('',*,*,#4478,.F.);
#3273=ORIENTED_EDGE('',*,*,#4480,.F.);
#3274=ORIENTED_EDGE('',*,*,#4596,.F.);
#3275=ORIENTED_EDGE('',*,*,#4597,.F.);
#3276=ORIENTED_EDGE('',*,*,#4598,.F.);
#3277=ORIENTED_EDGE('',*,*,#4599,.F.);
#3278=ORIENTED_EDGE('',*,*,#4482,.F.);
#3279=ORIENTED_EDGE('',*,*,#4481,.F.);
#3280=ORIENTED_EDGE('',*,*,#4483,.F.);
#3281=ORIENTED_EDGE('',*,*,#4600,.F.);
#3282=ORIENTED_EDGE('',*,*,#4601,.F.);
#3283=ORIENTED_EDGE('',*,*,#4602,.F.);
#3284=ORIENTED_EDGE('',*,*,#4603,.F.);
#3285=ORIENTED_EDGE('',*,*,#4484,.F.);
#3286=ORIENTED_EDGE('',*,*,#4487,.F.);
#3287=ORIENTED_EDGE('',*,*,#4604,.F.);
#3288=ORIENTED_EDGE('',*,*,#4605,.F.);
#3289=ORIENTED_EDGE('',*,*,#4606,.F.);
#3290=ORIENTED_EDGE('',*,*,#4607,.F.);
#3291=ORIENTED_EDGE('',*,*,#4608,.F.);
#3292=ORIENTED_EDGE('',*,*,#4609,.F.);
#3293=ORIENTED_EDGE('',*,*,#4610,.F.);
#3294=ORIENTED_EDGE('',*,*,#4611,.F.);
#3295=ORIENTED_EDGE('',*,*,#4489,.F.);
#3296=ORIENTED_EDGE('',*,*,#4488,.F.);
#3297=ORIENTED_EDGE('',*,*,#4494,.F.);
#3298=ORIENTED_EDGE('',*,*,#4491,.T.);
#3299=ORIENTED_EDGE('',*,*,#4575,.F.);
#3300=ORIENTED_EDGE('',*,*,#4612,.T.);
#3301=ORIENTED_EDGE('',*,*,#4613,.T.);
#3302=ORIENTED_EDGE('',*,*,#4496,.F.);
#3303=ORIENTED_EDGE('',*,*,#4614,.F.);
#3304=ORIENTED_EDGE('',*,*,#4615,.T.);
#3305=ORIENTED_EDGE('',*,*,#4573,.F.);
#3306=ORIENTED_EDGE('',*,*,#4498,.T.);
#3307=ORIENTED_EDGE('',*,*,#4613,.F.);
#3308=ORIENTED_EDGE('',*,*,#4616,.T.);
#3309=ORIENTED_EDGE('',*,*,#4614,.T.);
#3310=ORIENTED_EDGE('',*,*,#4495,.F.);
#3311=ORIENTED_EDGE('',*,*,#4570,.F.);
#3312=ORIENTED_EDGE('',*,*,#4617,.T.);
#3313=ORIENTED_EDGE('',*,*,#4618,.F.);
#3314=ORIENTED_EDGE('',*,*,#4505,.F.);
#3315=ORIENTED_EDGE('',*,*,#4503,.T.);
#3316=ORIENTED_EDGE('',*,*,#4619,.T.);
#3317=ORIENTED_EDGE('',*,*,#4568,.F.);
#3318=ORIENTED_EDGE('',*,*,#4509,.T.);
#3319=ORIENTED_EDGE('',*,*,#4507,.F.);
#3320=ORIENTED_EDGE('',*,*,#4620,.T.);
#3321=ORIENTED_EDGE('',*,*,#4618,.T.);
#3322=ORIENTED_EDGE('',*,*,#4621,.T.);
#3323=ORIENTED_EDGE('',*,*,#4620,.F.);
#3324=ORIENTED_EDGE('',*,*,#4506,.F.);
#3325=ORIENTED_EDGE('',*,*,#4622,.T.);
#3326=ORIENTED_EDGE('',*,*,#4516,.F.);
#3327=ORIENTED_EDGE('',*,*,#4515,.F.);
#3328=ORIENTED_EDGE('',*,*,#4521,.T.);
#3329=ORIENTED_EDGE('',*,*,#4518,.F.);
#3330=ORIENTED_EDGE('',*,*,#4623,.T.);
#3331=ORIENTED_EDGE('',*,*,#4624,.T.);
#3332=ORIENTED_EDGE('',*,*,#4561,.F.);
#3333=ORIENTED_EDGE('',*,*,#4623,.F.);
#3334=ORIENTED_EDGE('',*,*,#4517,.F.);
#3335=ORIENTED_EDGE('',*,*,#4625,.T.);
#3336=ORIENTED_EDGE('',*,*,#4626,.T.);
#3337=ORIENTED_EDGE('',*,*,#4527,.F.);
#3338=ORIENTED_EDGE('',*,*,#4525,.T.);
#3339=ORIENTED_EDGE('',*,*,#4558,.F.);
#3340=ORIENTED_EDGE('',*,*,#4627,.T.);
#3341=ORIENTED_EDGE('',*,*,#4628,.T.);
#3342=ORIENTED_EDGE('',*,*,#4629,.T.);
#3343=ORIENTED_EDGE('',*,*,#4556,.F.);
#3344=ORIENTED_EDGE('',*,*,#4531,.T.);
#3345=ORIENTED_EDGE('',*,*,#4529,.F.);
#3346=ORIENTED_EDGE('',*,*,#4630,.T.);
#3347=ORIENTED_EDGE('',*,*,#4628,.F.);
#3348=ORIENTED_EDGE('',*,*,#4631,.T.);
#3349=ORIENTED_EDGE('',*,*,#4630,.F.);
#3350=ORIENTED_EDGE('',*,*,#4528,.F.);
#3351=ORIENTED_EDGE('',*,*,#4538,.F.);
#3352=ORIENTED_EDGE('',*,*,#4536,.T.);
#3353=ORIENTED_EDGE('',*,*,#4585,.F.);
#3354=ORIENTED_EDGE('',*,*,#4632,.T.);
#3355=ORIENTED_EDGE('',*,*,#4633,.T.);
#3356=ORIENTED_EDGE('',*,*,#4634,.T.);
#3357=ORIENTED_EDGE('',*,*,#4583,.F.);
#3358=ORIENTED_EDGE('',*,*,#4542,.T.);
#3359=ORIENTED_EDGE('',*,*,#4540,.F.);
#3360=ORIENTED_EDGE('',*,*,#4635,.T.);
#3361=ORIENTED_EDGE('',*,*,#4633,.F.);
#3362=ORIENTED_EDGE('',*,*,#4636,.T.);
#3363=ORIENTED_EDGE('',*,*,#4635,.F.);
#3364=ORIENTED_EDGE('',*,*,#4539,.F.);
#3365=ORIENTED_EDGE('',*,*,#4549,.F.);
#3366=ORIENTED_EDGE('',*,*,#4547,.T.);
#3367=ORIENTED_EDGE('',*,*,#4580,.F.);
#3368=ORIENTED_EDGE('',*,*,#4637,.T.);
#3369=ORIENTED_EDGE('',*,*,#4638,.T.);
#3370=ORIENTED_EDGE('',*,*,#4639,.T.);
#3371=ORIENTED_EDGE('',*,*,#4578,.F.);
#3372=ORIENTED_EDGE('',*,*,#4553,.T.);
#3373=ORIENTED_EDGE('',*,*,#4551,.F.);
#3374=ORIENTED_EDGE('',*,*,#4640,.T.);
#3375=ORIENTED_EDGE('',*,*,#4638,.F.);
#3376=ORIENTED_EDGE('',*,*,#4641,.T.);
#3377=ORIENTED_EDGE('',*,*,#4640,.F.);
#3378=ORIENTED_EDGE('',*,*,#4550,.F.);
#3379=ORIENTED_EDGE('',*,*,#4588,.T.);
#3380=ORIENTED_EDGE('',*,*,#4642,.T.);
#3381=ORIENTED_EDGE('',*,*,#4560,.F.);
#3382=ORIENTED_EDGE('',*,*,#4643,.T.);
#3383=ORIENTED_EDGE('',*,*,#4589,.T.);
#3384=ORIENTED_EDGE('',*,*,#4642,.F.);
#3385=ORIENTED_EDGE('',*,*,#4591,.T.);
#3386=ORIENTED_EDGE('',*,*,#4590,.T.);
#3387=ORIENTED_EDGE('',*,*,#4643,.F.);
#3388=ORIENTED_EDGE('',*,*,#4559,.F.);
#3389=ORIENTED_EDGE('',*,*,#4627,.F.);
#3390=ORIENTED_EDGE('',*,*,#4557,.F.);
#3391=ORIENTED_EDGE('',*,*,#4629,.F.);
#3392=ORIENTED_EDGE('',*,*,#4631,.F.);
#3393=ORIENTED_EDGE('',*,*,#4592,.T.);
#3394=ORIENTED_EDGE('',*,*,#4644,.T.);
#3395=ORIENTED_EDGE('',*,*,#4566,.F.);
#3396=ORIENTED_EDGE('',*,*,#4645,.T.);
#3397=ORIENTED_EDGE('',*,*,#4593,.T.);
#3398=ORIENTED_EDGE('',*,*,#4644,.F.);
#3399=ORIENTED_EDGE('',*,*,#4595,.T.);
#3400=ORIENTED_EDGE('',*,*,#4594,.T.);
#3401=ORIENTED_EDGE('',*,*,#4645,.F.);
#3402=ORIENTED_EDGE('',*,*,#4565,.F.);
#3403=ORIENTED_EDGE('',*,*,#4624,.F.);
#3404=ORIENTED_EDGE('',*,*,#4626,.F.);
#3405=ORIENTED_EDGE('',*,*,#4646,.T.);
#3406=ORIENTED_EDGE('',*,*,#4562,.F.);
#3407=ORIENTED_EDGE('',*,*,#4625,.F.);
#3408=ORIENTED_EDGE('',*,*,#4622,.F.);
#3409=ORIENTED_EDGE('',*,*,#4567,.T.);
#3410=ORIENTED_EDGE('',*,*,#4563,.T.);
#3411=ORIENTED_EDGE('',*,*,#4646,.F.);
#3412=ORIENTED_EDGE('',*,*,#4599,.T.);
#3413=ORIENTED_EDGE('',*,*,#4647,.T.);
#3414=ORIENTED_EDGE('',*,*,#4572,.F.);
#3415=ORIENTED_EDGE('',*,*,#4648,.T.);
#3416=ORIENTED_EDGE('',*,*,#4596,.T.);
#3417=ORIENTED_EDGE('',*,*,#4647,.F.);
#3418=ORIENTED_EDGE('',*,*,#4598,.T.);
#3419=ORIENTED_EDGE('',*,*,#4597,.T.);
#3420=ORIENTED_EDGE('',*,*,#4648,.F.);
#3421=ORIENTED_EDGE('',*,*,#4571,.F.);
#3422=ORIENTED_EDGE('',*,*,#4621,.F.);
#3423=ORIENTED_EDGE('',*,*,#4617,.F.);
#3424=ORIENTED_EDGE('',*,*,#4569,.F.);
#3425=ORIENTED_EDGE('',*,*,#4619,.F.);
#3426=ORIENTED_EDGE('',*,*,#4603,.T.);
#3427=ORIENTED_EDGE('',*,*,#4649,.T.);
#3428=ORIENTED_EDGE('',*,*,#4577,.F.);
#3429=ORIENTED_EDGE('',*,*,#4650,.T.);
#3430=ORIENTED_EDGE('',*,*,#4600,.T.);
#3431=ORIENTED_EDGE('',*,*,#4649,.F.);
#3432=ORIENTED_EDGE('',*,*,#4602,.T.);
#3433=ORIENTED_EDGE('',*,*,#4601,.T.);
#3434=ORIENTED_EDGE('',*,*,#4650,.F.);
#3435=ORIENTED_EDGE('',*,*,#4576,.F.);
#3436=ORIENTED_EDGE('',*,*,#4612,.F.);
#3437=ORIENTED_EDGE('',*,*,#4574,.F.);
#3438=ORIENTED_EDGE('',*,*,#4615,.F.);
#3439=ORIENTED_EDGE('',*,*,#4616,.F.);
#3440=ORIENTED_EDGE('',*,*,#4607,.T.);
#3441=ORIENTED_EDGE('',*,*,#4651,.T.);
#3442=ORIENTED_EDGE('',*,*,#4582,.F.);
#3443=ORIENTED_EDGE('',*,*,#4652,.T.);
#3444=ORIENTED_EDGE('',*,*,#4604,.T.);
#3445=ORIENTED_EDGE('',*,*,#4651,.F.);
#3446=ORIENTED_EDGE('',*,*,#4606,.T.);
#3447=ORIENTED_EDGE('',*,*,#4605,.T.);
#3448=ORIENTED_EDGE('',*,*,#4652,.F.);
#3449=ORIENTED_EDGE('',*,*,#4581,.F.);
#3450=ORIENTED_EDGE('',*,*,#4637,.F.);
#3451=ORIENTED_EDGE('',*,*,#4579,.F.);
#3452=ORIENTED_EDGE('',*,*,#4639,.F.);
#3453=ORIENTED_EDGE('',*,*,#4641,.F.);
#3454=ORIENTED_EDGE('',*,*,#4608,.T.);
#3455=ORIENTED_EDGE('',*,*,#4653,.T.);
#3456=ORIENTED_EDGE('',*,*,#4587,.F.);
#3457=ORIENTED_EDGE('',*,*,#4654,.T.);
#3458=ORIENTED_EDGE('',*,*,#4609,.T.);
#3459=ORIENTED_EDGE('',*,*,#4653,.F.);
#3460=ORIENTED_EDGE('',*,*,#4611,.T.);
#3461=ORIENTED_EDGE('',*,*,#4610,.T.);
#3462=ORIENTED_EDGE('',*,*,#4654,.F.);
#3463=ORIENTED_EDGE('',*,*,#4586,.F.);
#3464=ORIENTED_EDGE('',*,*,#4632,.F.);
#3465=ORIENTED_EDGE('',*,*,#4584,.F.);
#3466=ORIENTED_EDGE('',*,*,#4634,.F.);
#3467=ORIENTED_EDGE('',*,*,#4636,.F.);
#4050=EDGE_CURVE('',#5049,#5049,#5697,.F.);
#4051=EDGE_CURVE('',#5050,#5050,#5698,.T.);
#4052=EDGE_CURVE('',#5051,#5051,#5699,.F.);
#4053=EDGE_CURVE('',#5052,#5052,#5700,.T.);
#4054=EDGE_CURVE('',#5053,#5053,#5701,.T.);
#4055=EDGE_CURVE('',#5054,#5054,#5702,.F.);
#4056=EDGE_CURVE('',#5055,#5055,#5703,.T.);
#4057=EDGE_CURVE('',#5056,#5056,#5704,.F.);
#4058=EDGE_CURVE('',#5057,#5057,#5705,.F.);
#4059=EDGE_CURVE('',#5058,#5058,#5706,.T.);
#4060=EDGE_CURVE('',#5059,#5059,#5707,.F.);
#4061=EDGE_CURVE('',#5060,#5060,#5708,.T.);
#4062=EDGE_CURVE('',#5061,#5061,#5709,.T.);
#4063=EDGE_CURVE('',#5062,#5062,#5710,.F.);
#4064=EDGE_CURVE('',#5063,#5063,#5711,.T.);
#4065=EDGE_CURVE('',#5064,#5064,#5712,.F.);
#4066=EDGE_CURVE('',#5065,#5065,#5713,.F.);
#4067=EDGE_CURVE('',#5066,#5066,#5714,.T.);
#4068=EDGE_CURVE('',#5067,#5067,#5715,.F.);
#4069=EDGE_CURVE('',#5068,#5068,#5716,.T.);
#4070=EDGE_CURVE('',#5069,#5069,#5717,.T.);
#4071=EDGE_CURVE('',#5070,#5070,#5718,.F.);
#4072=EDGE_CURVE('',#5071,#5071,#5719,.T.);
#4073=EDGE_CURVE('',#5072,#5072,#5720,.F.);
#4074=EDGE_CURVE('',#5073,#5073,#5721,.F.);
#4075=EDGE_CURVE('',#5074,#5074,#5722,.T.);
#4076=EDGE_CURVE('',#5075,#5075,#5723,.F.);
#4077=EDGE_CURVE('',#5076,#5076,#5724,.F.);
#4078=EDGE_CURVE('',#5077,#5077,#5725,.T.);
#4079=EDGE_CURVE('',#5078,#5078,#5726,.T.);
#4080=EDGE_CURVE('',#5079,#5079,#5727,.T.);
#4081=EDGE_CURVE('',#5080,#5080,#5728,.F.);
#4082=EDGE_CURVE('',#5081,#5081,#5729,.F.);
#4083=EDGE_CURVE('',#5082,#5082,#5730,.F.);
#4084=EDGE_CURVE('',#5083,#5083,#5731,.F.);
#4085=EDGE_CURVE('',#5084,#5084,#5732,.T.);
#4086=EDGE_CURVE('',#5085,#5085,#5733,.T.);
#4087=EDGE_CURVE('',#5086,#5086,#5734,.T.);
#4088=EDGE_CURVE('',#5087,#5087,#5735,.T.);
#4089=EDGE_CURVE('',#5088,#5088,#5736,.T.);
#4090=EDGE_CURVE('',#5089,#5089,#5737,.T.);
#4091=EDGE_CURVE('',#5090,#5090,#5738,.T.);
#4092=EDGE_CURVE('',#5091,#5091,#5739,.T.);
#4093=EDGE_CURVE('',#5092,#5092,#5740,.T.);
#4094=EDGE_CURVE('',#5093,#5093,#5741,.T.);
#4095=EDGE_CURVE('',#5094,#5094,#5742,.T.);
#4096=EDGE_CURVE('',#5095,#5095,#5743,.T.);
#4097=EDGE_CURVE('',#5096,#5096,#5744,.T.);
#4098=EDGE_CURVE('',#5097,#5097,#5745,.T.);
#4099=EDGE_CURVE('',#5098,#5098,#5746,.T.);
#4100=EDGE_CURVE('',#5099,#5099,#5747,.T.);
#4101=EDGE_CURVE('',#5100,#5100,#5748,.T.);
#4102=EDGE_CURVE('',#5101,#5101,#5749,.T.);
#4103=EDGE_CURVE('',#5102,#5102,#5750,.T.);
#4104=EDGE_CURVE('',#5103,#5103,#5751,.T.);
#4105=EDGE_CURVE('',#5104,#5104,#5752,.T.);
#4106=EDGE_CURVE('',#5105,#5105,#5753,.T.);
#4107=EDGE_CURVE('',#5106,#5106,#5754,.T.);
#4108=EDGE_CURVE('',#5107,#5107,#5755,.T.);
#4109=EDGE_CURVE('',#5108,#5108,#5756,.T.);
#4110=EDGE_CURVE('',#5109,#5109,#5757,.T.);
#4111=EDGE_CURVE('',#5110,#5110,#5758,.T.);
#4112=EDGE_CURVE('',#5111,#5111,#5759,.T.);
#4113=EDGE_CURVE('',#5112,#5112,#5760,.T.);
#4114=EDGE_CURVE('',#5113,#5113,#5761,.T.);
#4115=EDGE_CURVE('',#5114,#5114,#5762,.T.);
#4116=EDGE_CURVE('',#5115,#5115,#5763,.T.);
#4117=EDGE_CURVE('',#5116,#5116,#5764,.T.);
#4118=EDGE_CURVE('',#5117,#5117,#5765,.T.);
#4119=EDGE_CURVE('',#5118,#5118,#5766,.T.);
#4120=EDGE_CURVE('',#5119,#5119,#5767,.T.);
#4121=EDGE_CURVE('',#5120,#5120,#5768,.T.);
#4122=EDGE_CURVE('',#5121,#5122,#5769,.T.);
#4123=EDGE_CURVE('',#5122,#5121,#539,.T.);
#4124=EDGE_CURVE('',#5123,#5124,#5770,.T.);
#4125=EDGE_CURVE('',#5124,#5123,#540,.F.);
#4126=EDGE_CURVE('',#5125,#5125,#5771,.T.);
#4127=EDGE_CURVE('',#5126,#5126,#5772,.T.);
#4128=EDGE_CURVE('',#5127,#5128,#541,.F.);
#4129=EDGE_CURVE('',#5128,#5127,#5773,.F.);
#4130=EDGE_CURVE('',#5129,#5130,#5774,.T.);
#4131=EDGE_CURVE('',#5130,#5129,#542,.F.);
#4132=EDGE_CURVE('',#5131,#5132,#543,.F.);
#4133=EDGE_CURVE('',#5132,#5131,#544,.F.);
#4134=EDGE_CURVE('',#5133,#5133,#5775,.T.);
#4135=EDGE_CURVE('',#5134,#5135,#545,.F.);
#4136=EDGE_CURVE('',#5135,#5134,#5776,.T.);
#4137=EDGE_CURVE('',#5136,#5136,#5777,.F.);
#4138=EDGE_CURVE('',#5137,#5135,#546,.T.);
#4139=EDGE_CURVE('',#5138,#5137,#5778,.T.);
#4140=EDGE_CURVE('',#5134,#5138,#547,.T.);
#4141=EDGE_CURVE('',#5137,#5138,#548,.T.);
#4142=EDGE_CURVE('',#5139,#5140,#5779,.T.);
#4143=EDGE_CURVE('',#5140,#5139,#549,.F.);
#4144=EDGE_CURVE('',#5141,#5142,#550,.F.);
#4145=EDGE_CURVE('',#5142,#5143,#551,.F.);
#4146=EDGE_CURVE('',#5143,#5144,#552,.F.);
#4147=EDGE_CURVE('',#5144,#5145,#553,.F.);
#4148=EDGE_CURVE('',#5145,#5146,#554,.F.);
#4149=EDGE_CURVE('',#5146,#5147,#555,.F.);
#4150=EDGE_CURVE('',#5147,#5148,#556,.F.);
#4151=EDGE_CURVE('',#5148,#5149,#557,.F.);
#4152=EDGE_CURVE('',#5149,#5150,#558,.F.);
#4153=EDGE_CURVE('',#5150,#5151,#559,.F.);
#4154=EDGE_CURVE('',#5151,#5152,#560,.F.);
#4155=EDGE_CURVE('',#5152,#5153,#561,.F.);
#4156=EDGE_CURVE('',#5153,#5154,#562,.F.);
#4157=EDGE_CURVE('',#5154,#5155,#5780,.F.);
#4158=EDGE_CURVE('',#5155,#5156,#563,.F.);
#4159=EDGE_CURVE('',#5156,#5157,#564,.F.);
#4160=EDGE_CURVE('',#5157,#5158,#565,.F.);
#4161=EDGE_CURVE('',#5158,#5159,#566,.F.);
#4162=EDGE_CURVE('',#5159,#5160,#567,.F.);
#4163=EDGE_CURVE('',#5160,#5161,#568,.F.);
#4164=EDGE_CURVE('',#5161,#5162,#5781,.F.);
#4165=EDGE_CURVE('',#5162,#5163,#569,.F.);
#4166=EDGE_CURVE('',#5163,#5164,#570,.F.);
#4167=EDGE_CURVE('',#5164,#5165,#571,.F.);
#4168=EDGE_CURVE('',#5165,#5166,#572,.F.);
#4169=EDGE_CURVE('',#5166,#5141,#573,.F.);
#4170=EDGE_CURVE('',#5167,#5167,#5782,.F.);
#4171=EDGE_CURVE('',#5168,#5169,#5783,.T.);
#4172=EDGE_CURVE('',#5156,#5168,#574,.F.);
#4173=EDGE_CURVE('',#5169,#5154,#575,.F.);
#4174=EDGE_CURVE('',#5170,#5168,#576,.T.);
#4175=EDGE_CURVE('',#5157,#5170,#577,.T.);
#4176=EDGE_CURVE('',#5171,#5170,#5784,.F.);
#4177=EDGE_CURVE('',#5158,#5171,#578,.F.);
#4178=EDGE_CURVE('',#5172,#5171,#579,.T.);
#4179=EDGE_CURVE('',#5159,#5172,#580,.T.);
#4180=EDGE_CURVE('',#5173,#5172,#581,.T.);
#4181=EDGE_CURVE('',#5160,#5173,#582,.F.);
#4182=EDGE_CURVE('',#5174,#5173,#583,.T.);
#4183=EDGE_CURVE('',#5161,#5174,#584,.T.);
#4184=EDGE_CURVE('',#5175,#5174,#5785,.F.);
#4185=EDGE_CURVE('',#5162,#5175,#585,.F.);
#4186=EDGE_CURVE('',#5176,#5175,#586,.T.);
#4187=EDGE_CURVE('',#5163,#5176,#587,.T.);
#4188=EDGE_CURVE('',#5177,#5176,#588,.T.);
#4189=EDGE_CURVE('',#5164,#5177,#589,.F.);
#4190=EDGE_CURVE('',#5178,#5177,#590,.T.);
#4191=EDGE_CURVE('',#5165,#5178,#591,.T.);
#4192=EDGE_CURVE('',#5179,#5178,#5786,.F.);
#4193=EDGE_CURVE('',#5166,#5179,#592,.F.);
#4194=EDGE_CURVE('',#5180,#5179,#593,.T.);
#4195=EDGE_CURVE('',#5141,#5180,#594,.T.);
#4196=EDGE_CURVE('',#5181,#5180,#595,.T.);
#4197=EDGE_CURVE('',#5142,#5181,#5787,.T.);
#4198=EDGE_CURVE('',#5182,#5181,#596,.T.);
#4199=EDGE_CURVE('',#5143,#5182,#597,.F.);
#4200=EDGE_CURVE('',#5183,#5182,#598,.T.);
#4201=EDGE_CURVE('',#5144,#5183,#599,.T.);
#4202=EDGE_CURVE('',#5184,#5183,#5788,.F.);
#4203=EDGE_CURVE('',#5145,#5184,#600,.F.);
#4204=EDGE_CURVE('',#5185,#5184,#601,.T.);
#4205=EDGE_CURVE('',#5146,#5185,#602,.T.);
#4206=EDGE_CURVE('',#5186,#5185,#603,.T.);
#4207=EDGE_CURVE('',#5147,#5186,#604,.F.);
#4208=EDGE_CURVE('',#5187,#5186,#605,.T.);
#4209=EDGE_CURVE('',#5148,#5187,#606,.T.);
#4210=EDGE_CURVE('',#5188,#5187,#5789,.F.);
#4211=EDGE_CURVE('',#5149,#5188,#607,.F.);
#4212=EDGE_CURVE('',#5189,#5188,#608,.T.);
#4213=EDGE_CURVE('',#5150,#5189,#609,.T.);
#4214=EDGE_CURVE('',#5190,#5189,#610,.T.);
#4215=EDGE_CURVE('',#5151,#5190,#611,.F.);
#4216=EDGE_CURVE('',#5191,#5190,#612,.T.);
#4217=EDGE_CURVE('',#5152,#5191,#613,.T.);
#4218=EDGE_CURVE('',#5192,#5191,#5790,.F.);
#4219=EDGE_CURVE('',#5153,#5192,#614,.F.);
#4220=EDGE_CURVE('',#5169,#5192,#615,.T.);
#4221=EDGE_CURVE('',#5193,#5193,#5791,.T.);
#4222=EDGE_CURVE('',#5194,#5168,#616,.F.);
#4223=EDGE_CURVE('',#5169,#5195,#617,.F.);
#4224=EDGE_CURVE('',#5195,#5194,#5792,.F.);
#4225=EDGE_CURVE('',#5196,#5194,#5793,.F.);
#4226=EDGE_CURVE('',#5197,#5196,#618,.F.);
#4227=EDGE_CURVE('',#5170,#5197,#5794,.T.);
#4228=EDGE_CURVE('',#5198,#5198,#5795,.F.);
#4229=EDGE_CURVE('',#5199,#5200,#619,.T.);
#4230=EDGE_CURVE('',#5179,#5199,#5796,.F.);
#4231=EDGE_CURVE('',#5201,#5178,#5797,.F.);
#4232=EDGE_CURVE('',#5202,#5201,#620,.T.);
#4233=EDGE_CURVE('',#5203,#5202,#5798,.F.);
#4234=EDGE_CURVE('',#5204,#5203,#5799,.F.);
#4235=EDGE_CURVE('',#5205,#5204,#5800,.F.);
#4236=EDGE_CURVE('',#5206,#5205,#621,.T.);
#4237=EDGE_CURVE('',#5175,#5206,#5801,.F.);
#4238=EDGE_CURVE('',#5207,#5174,#5802,.F.);
#4239=EDGE_CURVE('',#5208,#5207,#622,.T.);
#4240=EDGE_CURVE('',#5209,#5208,#5803,.F.);
#4241=EDGE_CURVE('',#5210,#5209,#5804,.F.);
#4242=EDGE_CURVE('',#5211,#5210,#5805,.F.);
#4243=EDGE_CURVE('',#5212,#5211,#623,.T.);
#4244=EDGE_CURVE('',#5171,#5212,#5806,.F.);
#4245=EDGE_CURVE('',#5213,#5197,#624,.T.);
#4246=EDGE_CURVE('',#5214,#5213,#5807,.F.);
#4247=EDGE_CURVE('',#5215,#5214,#5808,.F.);
#4248=EDGE_CURVE('',#5216,#5215,#5809,.F.);
#4249=EDGE_CURVE('',#5217,#5216,#625,.T.);
#4250=EDGE_CURVE('',#5192,#5217,#5810,.F.);
#4251=EDGE_CURVE('',#5218,#5191,#5811,.F.);
#4252=EDGE_CURVE('',#5219,#5218,#626,.T.);
#4253=EDGE_CURVE('',#5220,#5219,#5812,.F.);
#4254=EDGE_CURVE('',#5221,#5220,#5813,.F.);
#4255=EDGE_CURVE('',#5222,#5221,#5814,.F.);
#4256=EDGE_CURVE('',#5223,#5222,#627,.T.);
#4257=EDGE_CURVE('',#5188,#5223,#5815,.F.);
#4258=EDGE_CURVE('',#5224,#5187,#5816,.F.);
#4259=EDGE_CURVE('',#5225,#5224,#628,.T.);
#4260=EDGE_CURVE('',#5226,#5225,#5817,.F.);
#4261=EDGE_CURVE('',#5227,#5226,#5818,.F.);
#4262=EDGE_CURVE('',#5228,#5227,#5819,.F.);
#4263=EDGE_CURVE('',#5229,#5228,#629,.T.);
#4264=EDGE_CURVE('',#5184,#5229,#5820,.F.);
#4265=EDGE_CURVE('',#5230,#5183,#5821,.F.);
#4266=EDGE_CURVE('',#5231,#5230,#630,.T.);
#4267=EDGE_CURVE('',#5232,#5231,#5822,.F.);
#4268=EDGE_CURVE('',#5233,#5232,#5823,.F.);
#4269=EDGE_CURVE('',#5200,#5233,#5824,.F.);
#4270=EDGE_CURVE('',#5234,#5234,#5825,.T.);
#4271=EDGE_CURVE('',#5235,#5235,#5826,.T.);
#4272=EDGE_CURVE('',#5236,#5236,#5827,.T.);
#4273=EDGE_CURVE('',#5237,#5237,#5828,.T.);
#4274=EDGE_CURVE('',#5238,#5238,#5829,.T.);
#4275=EDGE_CURVE('',#5239,#5239,#5830,.T.);
#4276=EDGE_CURVE('',#5240,#5240,#5831,.T.);
#4277=EDGE_CURVE('',#5241,#5241,#5832,.T.);
#4278=EDGE_CURVE('',#5242,#5242,#5833,.T.);
#4279=EDGE_CURVE('',#5243,#5243,#5834,.T.);
#4280=EDGE_CURVE('',#5244,#5244,#5835,.T.);
#4281=EDGE_CURVE('',#5245,#5245,#5836,.T.);
#4282=EDGE_CURVE('',#5246,#5246,#5837,.T.);
#4283=EDGE_CURVE('',#5247,#5247,#5838,.T.);
#4284=EDGE_CURVE('',#5248,#5248,#5839,.T.);
#4285=EDGE_CURVE('',#5249,#5249,#5840,.T.);
#4286=EDGE_CURVE('',#5250,#5250,#5841,.T.);
#4287=EDGE_CURVE('',#5251,#5251,#5842,.T.);
#4288=EDGE_CURVE('',#5252,#5212,#631,.F.);
#4289=EDGE_CURVE('',#5253,#5252,#5843,.F.);
#4290=EDGE_CURVE('',#5172,#5253,#632,.F.);
#4291=EDGE_CURVE('',#5254,#5173,#633,.F.);
#4292=EDGE_CURVE('',#5253,#5254,#5844,.F.);
#4293=EDGE_CURVE('',#5255,#5254,#5845,.F.);
#4294=EDGE_CURVE('',#5207,#5255,#634,.F.);
#4295=EDGE_CURVE('',#5256,#5206,#635,.F.);
#4296=EDGE_CURVE('',#5257,#5256,#5846,.F.);
#4297=EDGE_CURVE('',#5176,#5257,#636,.F.);
#4298=EDGE_CURVE('',#5257,#5258,#5847,.F.);
#4299=EDGE_CURVE('',#5258,#5177,#637,.F.);
#4300=EDGE_CURVE('',#5259,#5258,#5848,.F.);
#4301=EDGE_CURVE('',#5201,#5259,#638,.F.);
#4302=EDGE_CURVE('',#5260,#5199,#639,.F.);
#4303=EDGE_CURVE('',#5261,#5260,#5849,.F.);
#4304=EDGE_CURVE('',#5180,#5261,#640,.F.);
#4305=EDGE_CURVE('',#5261,#5262,#5850,.F.);
#4306=EDGE_CURVE('',#5262,#5182,#641,.F.);
#4307=EDGE_CURVE('',#5263,#5262,#5851,.F.);
#4308=EDGE_CURVE('',#5230,#5263,#642,.F.);
#4309=EDGE_CURVE('',#5264,#5229,#643,.F.);
#4310=EDGE_CURVE('',#5265,#5264,#5852,.F.);
#4311=EDGE_CURVE('',#5185,#5265,#644,.F.);
#4312=EDGE_CURVE('',#5265,#5266,#5853,.F.);
#4313=EDGE_CURVE('',#5266,#5186,#645,.F.);
#4314=EDGE_CURVE('',#5267,#5266,#5854,.F.);
#4315=EDGE_CURVE('',#5224,#5267,#646,.F.);
#4316=EDGE_CURVE('',#5268,#5223,#647,.F.);
#4317=EDGE_CURVE('',#5269,#5268,#5855,.F.);
#4318=EDGE_CURVE('',#5189,#5269,#648,.F.);
#4319=EDGE_CURVE('',#5270,#5190,#649,.F.);
#4320=EDGE_CURVE('',#5269,#5270,#5856,.F.);
#4321=EDGE_CURVE('',#5271,#5270,#5857,.F.);
#4322=EDGE_CURVE('',#5218,#5271,#650,.F.);
#4323=EDGE_CURVE('',#5195,#5272,#5858,.F.);
#4324=EDGE_CURVE('',#5272,#5217,#651,.F.);
#4325=EDGE_CURVE('',#5273,#5274,#5859,.F.);
#4326=EDGE_CURVE('',#5274,#5273,#652,.T.);
#4327=EDGE_CURVE('',#5275,#5275,#5860,.T.);
#4328=EDGE_CURVE('',#5276,#5276,#5861,.F.);
#4329=EDGE_CURVE('',#5277,#5278,#5862,.T.);
#4330=EDGE_CURVE('',#5255,#5277,#653,.T.);
#4331=EDGE_CURVE('',#5279,#5252,#654,.T.);
#4332=EDGE_CURVE('',#5280,#5279,#5863,.T.);
#4333=EDGE_CURVE('',#5278,#5280,#5864,.T.);
#4334=EDGE_CURVE('',#5281,#5256,#655,.T.);
#4335=EDGE_CURVE('',#5282,#5281,#5865,.T.);
#4336=EDGE_CURVE('',#5283,#5282,#5866,.T.);
#4337=EDGE_CURVE('',#5284,#5283,#5867,.T.);
#4338=EDGE_CURVE('',#5259,#5284,#656,.T.);
#4339=EDGE_CURVE('',#5285,#5260,#657,.T.);
#4340=EDGE_CURVE('',#5286,#5285,#5868,.T.);
#4341=EDGE_CURVE('',#5287,#5286,#5869,.T.);
#4342=EDGE_CURVE('',#5288,#5287,#5870,.T.);
#4343=EDGE_CURVE('',#5263,#5288,#658,.T.);
#4344=EDGE_CURVE('',#5289,#5264,#659,.T.);
#4345=EDGE_CURVE('',#5290,#5289,#5871,.T.);
#4346=EDGE_CURVE('',#5291,#5290,#5872,.T.);
#4347=EDGE_CURVE('',#5292,#5291,#5873,.T.);
#4348=EDGE_CURVE('',#5267,#5292,#660,.T.);
#4349=EDGE_CURVE('',#5293,#5268,#661,.T.);
#4350=EDGE_CURVE('',#5294,#5293,#5874,.T.);
#4351=EDGE_CURVE('',#5295,#5294,#5875,.T.);
#4352=EDGE_CURVE('',#5296,#5295,#5876,.T.);
#4353=EDGE_CURVE('',#5271,#5296,#662,.T.);
#4354=EDGE_CURVE('',#5297,#5298,#5877,.T.);
#4355=EDGE_CURVE('',#5196,#5297,#663,.T.);
#4356=EDGE_CURVE('',#5299,#5272,#664,.T.);
#4357=EDGE_CURVE('',#5300,#5299,#5878,.T.);
#4358=EDGE_CURVE('',#5298,#5300,#5879,.T.);
#4359=EDGE_CURVE('',#5301,#5301,#5880,.F.);
#4360=EDGE_CURVE('',#5302,#5302,#5881,.F.);
#4361=EDGE_CURVE('',#5303,#5303,#5882,.F.);
#4362=EDGE_CURVE('',#5304,#5304,#5883,.F.);
#4363=EDGE_CURVE('',#5305,#5305,#5884,.F.);
#4364=EDGE_CURVE('',#5306,#5306,#5885,.F.);
#4365=EDGE_CURVE('',#5307,#5307,#5886,.F.);
#4366=EDGE_CURVE('',#5308,#5308,#5887,.F.);
#4367=EDGE_CURVE('',#5309,#5309,#5888,.F.);
#4368=EDGE_CURVE('',#5310,#5310,#5889,.F.);
#4369=EDGE_CURVE('',#5311,#5311,#5890,.F.);
#4370=EDGE_CURVE('',#5312,#5312,#5891,.F.);
#4371=EDGE_CURVE('',#5313,#5313,#5892,.F.);
#4372=EDGE_CURVE('',#5314,#5314,#5893,.F.);
#4373=EDGE_CURVE('',#5315,#5315,#5894,.F.);
#4374=EDGE_CURVE('',#5316,#5316,#5895,.F.);
#4375=EDGE_CURVE('',#5317,#5317,#5896,.F.);
#4376=EDGE_CURVE('',#5318,#5318,#5897,.F.);
#4377=EDGE_CURVE('',#5213,#5297,#665,.T.);
#4378=EDGE_CURVE('',#5202,#5284,#666,.T.);
#4379=EDGE_CURVE('',#5203,#5283,#667,.F.);
#4380=EDGE_CURVE('',#5204,#5282,#668,.F.);
#4381=EDGE_CURVE('',#5205,#5281,#669,.F.);
#4382=EDGE_CURVE('',#5208,#5277,#670,.T.);
#4383=EDGE_CURVE('',#5209,#5278,#671,.F.);
#4384=EDGE_CURVE('',#5210,#5280,#672,.F.);
#4385=EDGE_CURVE('',#5211,#5279,#673,.F.);
#4386=EDGE_CURVE('',#5214,#5298,#674,.F.);
#4387=EDGE_CURVE('',#5215,#5300,#675,.F.);
#4388=EDGE_CURVE('',#5216,#5299,#676,.F.);
#4389=EDGE_CURVE('',#5219,#5296,#677,.T.);
#4390=EDGE_CURVE('',#5220,#5295,#678,.F.);
#4391=EDGE_CURVE('',#5221,#5294,#679,.F.);
#4392=EDGE_CURVE('',#5222,#5293,#680,.F.);
#4393=EDGE_CURVE('',#5225,#5292,#681,.T.);
#4394=EDGE_CURVE('',#5226,#5291,#682,.F.);
#4395=EDGE_CURVE('',#5227,#5290,#683,.F.);
#4396=EDGE_CURVE('',#5228,#5289,#684,.F.);
#4397=EDGE_CURVE('',#5231,#5288,#685,.T.);
#4398=EDGE_CURVE('',#5232,#5287,#686,.F.);
#4399=EDGE_CURVE('',#5233,#5286,#687,.F.);
#4400=EDGE_CURVE('',#5200,#5285,#688,.F.);
#4401=EDGE_CURVE('',#5319,#5320,#5898,.T.);
#4402=EDGE_CURVE('',#5320,#5319,#689,.T.);
#4403=EDGE_CURVE('',#5321,#5322,#5899,.T.);
#4404=EDGE_CURVE('',#5322,#5321,#690,.F.);
#4405=EDGE_CURVE('',#5323,#5324,#5900,.T.);
#4406=EDGE_CURVE('',#5324,#5323,#691,.T.);
#4407=EDGE_CURVE('',#5325,#5326,#5901,.F.);
#4408=EDGE_CURVE('',#5326,#5325,#692,.T.);
#4409=EDGE_CURVE('',#5327,#5327,#5902,.T.);
#4410=EDGE_CURVE('',#5328,#5329,#5903,.F.);
#4411=EDGE_CURVE('',#5329,#5328,#693,.F.);
#4412=EDGE_CURVE('',#5330,#5331,#5904,.F.);
#4413=EDGE_CURVE('',#5332,#5330,#694,.T.);
#4414=EDGE_CURVE('',#5333,#5332,#5905,.T.);
#4415=EDGE_CURVE('',#5334,#5333,#695,.T.);
#4416=EDGE_CURVE('',#5335,#5334,#5906,.F.);
#4417=EDGE_CURVE('',#5336,#5335,#696,.T.);
#4418=EDGE_CURVE('',#5337,#5336,#5907,.T.);
#4419=EDGE_CURVE('',#5338,#5337,#697,.T.);
#4420=EDGE_CURVE('',#5339,#5338,#5908,.F.);
#4421=EDGE_CURVE('',#5340,#5339,#698,.T.);
#4422=EDGE_CURVE('',#5341,#5340,#5909,.T.);
#4423=EDGE_CURVE('',#5342,#5341,#699,.T.);
#4424=EDGE_CURVE('',#5343,#5342,#5910,.F.);
#4425=EDGE_CURVE('',#5344,#5343,#700,.T.);
#4426=EDGE_CURVE('',#5345,#5344,#5911,.T.);
#4427=EDGE_CURVE('',#5346,#5345,#701,.T.);
#4428=EDGE_CURVE('',#5347,#5346,#5912,.F.);
#4429=EDGE_CURVE('',#5348,#5347,#702,.T.);
#4430=EDGE_CURVE('',#5349,#5348,#5913,.T.);
#4431=EDGE_CURVE('',#5350,#5349,#703,.T.);
#4432=EDGE_CURVE('',#5351,#5350,#5914,.F.);
#4433=EDGE_CURVE('',#5352,#5351,#704,.T.);
#4434=EDGE_CURVE('',#5353,#5352,#5915,.T.);
#4435=EDGE_CURVE('',#5331,#5353,#705,.T.);
#4436=EDGE_CURVE('',#5354,#5354,#5916,.F.);
#4437=EDGE_CURVE('',#5355,#5356,#5917,.F.);
#4438=EDGE_CURVE('',#5356,#5355,#5918,.F.);
#4439=EDGE_CURVE('',#5357,#5357,#5919,.F.);
#4440=EDGE_CURVE('',#5358,#5358,#5920,.F.);
#4441=EDGE_CURVE('',#5359,#5360,#5921,.F.);
#4442=EDGE_CURVE('',#5360,#5359,#5922,.F.);
#4443=EDGE_CURVE('',#5361,#5361,#5923,.F.);
#4444=EDGE_CURVE('',#5362,#5328,#5924,.F.);
#4445=EDGE_CURVE('',#5363,#5362,#706,.T.);
#4446=EDGE_CURVE('',#5364,#5363,#707,.T.);
#4447=EDGE_CURVE('',#5365,#5364,#708,.T.);
#4448=EDGE_CURVE('',#5366,#5365,#709,.T.);
#4449=EDGE_CURVE('',#5367,#5366,#710,.T.);
#4450=EDGE_CURVE('',#5368,#5367,#711,.T.);
#4451=EDGE_CURVE('',#5369,#5368,#5925,.T.);
#4452=EDGE_CURVE('',#5370,#5369,#712,.T.);
#4453=EDGE_CURVE('',#5371,#5370,#713,.T.);
#4454=EDGE_CURVE('',#5372,#5371,#714,.T.);
#4455=EDGE_CURVE('',#5373,#5372,#715,.T.);
#4456=EDGE_CURVE('',#5374,#5373,#716,.T.);
#4457=EDGE_CURVE('',#5375,#5374,#717,.T.);
#4458=EDGE_CURVE('',#5329,#5375,#5926,.T.);
#4459=EDGE_CURVE('',#5376,#5377,#718,.T.);
#4460=EDGE_CURVE('',#5362,#5376,#719,.T.);
#4461=EDGE_CURVE('',#5378,#5375,#720,.T.);
#4462=EDGE_CURVE('',#5379,#5378,#721,.T.);
#4463=EDGE_CURVE('',#5380,#5379,#722,.T.);
#4464=EDGE_CURVE('',#5381,#5380,#723,.T.);
#4465=EDGE_CURVE('',#5382,#5381,#724,.T.);
#4466=EDGE_CURVE('',#5383,#5382,#725,.T.);
#4467=EDGE_CURVE('',#5384,#5383,#726,.T.);
#4468=EDGE_CURVE('',#5385,#5384,#727,.T.);
#4469=EDGE_CURVE('',#5386,#5385,#728,.T.);
#4470=EDGE_CURVE('',#5387,#5386,#729,.T.);
#4471=EDGE_CURVE('',#5377,#5387,#730,.T.);
#4472=EDGE_CURVE('',#5388,#5389,#5927,.T.);
#4473=EDGE_CURVE('',#5389,#5388,#731,.T.);
#4474=EDGE_CURVE('',#5390,#5391,#5928,.T.);
#4475=EDGE_CURVE('',#5391,#5360,#732,.T.);
#4476=EDGE_CURVE('',#5359,#5390,#733,.T.);
#4477=EDGE_CURVE('',#5391,#5390,#734,.T.);
#4478=EDGE_CURVE('',#5392,#5393,#735,.T.);
#4479=EDGE_CURVE('',#5393,#5394,#5929,.F.);
#4480=EDGE_CURVE('',#5394,#5392,#5930,.T.);
#4481=EDGE_CURVE('',#5395,#5396,#736,.T.);
#4482=EDGE_CURVE('',#5396,#5397,#5931,.F.);
#4483=EDGE_CURVE('',#5397,#5395,#5932,.T.);
#4484=EDGE_CURVE('',#5398,#5399,#5933,.T.);
#4485=EDGE_CURVE('',#5399,#5356,#737,.T.);
#4486=EDGE_CURVE('',#5355,#5398,#738,.T.);
#4487=EDGE_CURVE('',#5399,#5398,#5934,.T.);
#4488=EDGE_CURVE('',#5400,#5401,#739,.T.);
#4489=EDGE_CURVE('',#5401,#5400,#5935,.T.);
#4490=EDGE_CURVE('',#5402,#5380,#740,.T.);
#4491=EDGE_CURVE('',#5403,#5402,#741,.T.);
#4492=EDGE_CURVE('',#5332,#5403,#742,.T.);
#4493=EDGE_CURVE('',#5381,#5330,#743,.T.);
#4494=EDGE_CURVE('',#5403,#5404,#744,.T.);
#4495=EDGE_CURVE('',#5404,#5405,#745,.T.);
#4496=EDGE_CURVE('',#5405,#5406,#746,.T.);
#4497=EDGE_CURVE('',#5406,#5333,#747,.T.);
#4498=EDGE_CURVE('',#5407,#5406,#748,.T.);
#4499=EDGE_CURVE('',#5379,#5407,#749,.T.);
#4500=EDGE_CURVE('',#5334,#5378,#750,.T.);
#4501=EDGE_CURVE('',#5374,#5335,#751,.F.);
#4502=EDGE_CURVE('',#5408,#5373,#752,.T.);
#4503=EDGE_CURVE('',#5409,#5408,#753,.T.);
#4504=EDGE_CURVE('',#5336,#5409,#754,.T.);
#4505=EDGE_CURVE('',#5409,#5410,#755,.T.);
#4506=EDGE_CURVE('',#5410,#5411,#756,.T.);
#4507=EDGE_CURVE('',#5411,#5412,#757,.F.);
#4508=EDGE_CURVE('',#5412,#5337,#758,.T.);
#4509=EDGE_CURVE('',#5413,#5412,#759,.T.);
#4510=EDGE_CURVE('',#5372,#5413,#760,.T.);
#4511=EDGE_CURVE('',#5338,#5371,#761,.T.);
#4512=EDGE_CURVE('',#5370,#5414,#762,.F.);
#4513=EDGE_CURVE('',#5414,#5339,#763,.T.);
#4514=EDGE_CURVE('',#5414,#5415,#764,.F.);
#4515=EDGE_CURVE('',#5415,#5340,#5936,.F.);
#4516=EDGE_CURVE('',#5340,#5416,#5937,.T.);
#4517=EDGE_CURVE('',#5416,#5417,#5938,.F.);
#4518=EDGE_CURVE('',#5417,#5418,#765,.F.);
#4519=EDGE_CURVE('',#5418,#5341,#766,.T.);
#4520=EDGE_CURVE('',#5342,#5367,#767,.T.);
#4521=EDGE_CURVE('',#5419,#5418,#768,.T.);
#4522=EDGE_CURVE('',#5368,#5419,#769,.T.);
#4523=EDGE_CURVE('',#5366,#5343,#770,.F.);
#4524=EDGE_CURVE('',#5420,#5365,#771,.T.);
#4525=EDGE_CURVE('',#5421,#5420,#772,.T.);
#4526=EDGE_CURVE('',#5344,#5421,#773,.T.);
#4527=EDGE_CURVE('',#5421,#5422,#774,.T.);
#4528=EDGE_CURVE('',#5422,#5423,#775,.T.);
#4529=EDGE_CURVE('',#5423,#5424,#776,.F.);
#4530=EDGE_CURVE('',#5424,#5345,#777,.T.);
#4531=EDGE_CURVE('',#5425,#5424,#778,.T.);
#4532=EDGE_CURVE('',#5364,#5425,#779,.T.);
#4533=EDGE_CURVE('',#5346,#5363,#780,.T.);
#4534=EDGE_CURVE('',#5376,#5347,#781,.F.);
#4535=EDGE_CURVE('',#5426,#5377,#782,.T.);
#4536=EDGE_CURVE('',#5427,#5426,#783,.T.);
#4537=EDGE_CURVE('',#5348,#5427,#784,.T.);
#4538=EDGE_CURVE('',#5427,#5428,#785,.T.);
#4539=EDGE_CURVE('',#5428,#5429,#786,.T.);
#4540=EDGE_CURVE('',#5429,#5430,#787,.F.);
#4541=EDGE_CURVE('',#5430,#5349,#788,.T.);
#4542=EDGE_CURVE('',#5431,#5430,#789,.T.);
#4543=EDGE_CURVE('',#5387,#5431,#790,.T.);
#4544=EDGE_CURVE('',#5350,#5386,#791,.T.);
#4545=EDGE_CURVE('',#5385,#5351,#792,.F.);
#4546=EDGE_CURVE('',#5432,#5384,#793,.T.);
#4547=EDGE_CURVE('',#5433,#5432,#794,.T.);
#4548=EDGE_CURVE('',#5352,#5433,#795,.T.);
#4549=EDGE_CURVE('',#5433,#5434,#796,.T.);
#4550=EDGE_CURVE('',#5434,#5435,#797,.T.);
#4551=EDGE_CURVE('',#5435,#5436,#798,.F.);
#4552=EDGE_CURVE('',#5436,#5353,#799,.T.);
#4553=EDGE_CURVE('',#5437,#5436,#800,.T.);
#4554=EDGE_CURVE('',#5383,#5437,#801,.T.);
#4555=EDGE_CURVE('',#5331,#5382,#802,.T.);
#4556=EDGE_CURVE('',#5425,#5438,#803,.T.);
#4557=EDGE_CURVE('',#5438,#5439,#804,.F.);
#4558=EDGE_CURVE('',#5439,#5420,#805,.T.);
#4559=EDGE_CURVE('',#5440,#5441,#806,.F.);
#4560=EDGE_CURVE('',#5441,#5440,#807,.F.);
#4561=EDGE_CURVE('',#5419,#5442,#808,.T.);
#4562=EDGE_CURVE('',#5442,#5443,#5939,.F.);
#4563=EDGE_CURVE('',#5444,#5443,#809,.F.);
#4564=EDGE_CURVE('',#5444,#5369,#810,.T.);
#4565=EDGE_CURVE('',#5445,#5446,#811,.F.);
#4566=EDGE_CURVE('',#5446,#5445,#812,.F.);
#4567=EDGE_CURVE('',#5415,#5444,#813,.T.);
#4568=EDGE_CURVE('',#5413,#5447,#814,.T.);
#4569=EDGE_CURVE('',#5447,#5448,#815,.F.);
#4570=EDGE_CURVE('',#5448,#5408,#816,.T.);
#4571=EDGE_CURVE('',#5449,#5450,#817,.F.);
#4572=EDGE_CURVE('',#5450,#5449,#818,.F.);
#4573=EDGE_CURVE('',#5407,#5451,#819,.T.);
#4574=EDGE_CURVE('',#5451,#5452,#820,.F.);
#4575=EDGE_CURVE('',#5452,#5402,#821,.T.);
#4576=EDGE_CURVE('',#5453,#5454,#822,.F.);
#4577=EDGE_CURVE('',#5454,#5453,#823,.F.);
#4578=EDGE_CURVE('',#5437,#5455,#824,.T.);
#4579=EDGE_CURVE('',#5455,#5456,#825,.F.);
#4580=EDGE_CURVE('',#5456,#5432,#826,.T.);
#4581=EDGE_CURVE('',#5457,#5458,#827,.F.);
#4582=EDGE_CURVE('',#5458,#5457,#828,.F.);
#4583=EDGE_CURVE('',#5431,#5459,#829,.T.);
#4584=EDGE_CURVE('',#5459,#5460,#830,.F.);
#4585=EDGE_CURVE('',#5460,#5426,#831,.T.);
#4586=EDGE_CURVE('',#5461,#5462,#832,.F.);
#4587=EDGE_CURVE('',#5462,#5461,#833,.F.);
#4588=EDGE_CURVE('',#5463,#5464,#834,.F.);
#4589=EDGE_CURVE('',#5465,#5463,#835,.F.);
#4590=EDGE_CURVE('',#5466,#5465,#836,.F.);
#4591=EDGE_CURVE('',#5464,#5466,#837,.F.);
#4592=EDGE_CURVE('',#5467,#5468,#838,.F.);
#4593=EDGE_CURVE('',#5469,#5467,#839,.F.);
#4594=EDGE_CURVE('',#5470,#5469,#840,.F.);
#4595=EDGE_CURVE('',#5468,#5470,#841,.F.);
#4596=EDGE_CURVE('',#5471,#5472,#842,.F.);
#4597=EDGE_CURVE('',#5473,#5471,#843,.F.);
#4598=EDGE_CURVE('',#5474,#5473,#844,.F.);
#4599=EDGE_CURVE('',#5472,#5474,#845,.F.);
#4600=EDGE_CURVE('',#5475,#5476,#846,.F.);
#4601=EDGE_CURVE('',#5477,#5475,#847,.F.);
#4602=EDGE_CURVE('',#5478,#5477,#848,.F.);
#4603=EDGE_CURVE('',#5476,#5478,#849,.F.);
#4604=EDGE_CURVE('',#5479,#5480,#850,.F.);
#4605=EDGE_CURVE('',#5481,#5479,#851,.F.);
#4606=EDGE_CURVE('',#5482,#5481,#852,.F.);
#4607=EDGE_CURVE('',#5480,#5482,#853,.F.);
#4608=EDGE_CURVE('',#5483,#5484,#854,.F.);
#4609=EDGE_CURVE('',#5485,#5483,#855,.F.);
#4610=EDGE_CURVE('',#5486,#5485,#856,.F.);
#4611=EDGE_CURVE('',#5484,#5486,#857,.F.);
#4612=EDGE_CURVE('',#5452,#5487,#858,.T.);
#4613=EDGE_CURVE('',#5487,#5404,#859,.F.);
#4614=EDGE_CURVE('',#5488,#5405,#860,.F.);
#4615=EDGE_CURVE('',#5488,#5451,#861,.T.);
#4616=EDGE_CURVE('',#5487,#5488,#862,.F.);
#4617=EDGE_CURVE('',#5448,#5489,#863,.T.);
#4618=EDGE_CURVE('',#5410,#5489,#864,.F.);
#4619=EDGE_CURVE('',#5490,#5447,#865,.F.);
#4620=EDGE_CURVE('',#5411,#5490,#866,.F.);
#4621=EDGE_CURVE('',#5489,#5490,#867,.F.);
#4622=EDGE_CURVE('',#5415,#5416,#868,.F.);
#4623=EDGE_CURVE('',#5417,#5491,#869,.F.);
#4624=EDGE_CURVE('',#5491,#5442,#870,.F.);
#4625=EDGE_CURVE('',#5416,#5492,#871,.F.);
#4626=EDGE_CURVE('',#5492,#5491,#5940,.T.);
#4627=EDGE_CURVE('',#5439,#5493,#872,.T.);
#4628=EDGE_CURVE('',#5493,#5422,#873,.F.);
#4629=EDGE_CURVE('',#5494,#5438,#874,.F.);
#4630=EDGE_CURVE('',#5423,#5494,#875,.F.);
#4631=EDGE_CURVE('',#5493,#5494,#876,.F.);
#4632=EDGE_CURVE('',#5460,#5495,#877,.T.);
#4633=EDGE_CURVE('',#5495,#5428,#878,.F.);
#4634=EDGE_CURVE('',#5496,#5459,#879,.F.);
#4635=EDGE_CURVE('',#5429,#5496,#880,.F.);
#4636=EDGE_CURVE('',#5495,#5496,#881,.F.);
#4637=EDGE_CURVE('',#5456,#5497,#882,.T.);
#4638=EDGE_CURVE('',#5497,#5434,#883,.F.);
#4639=EDGE_CURVE('',#5498,#5455,#884,.F.);
#4640=EDGE_CURVE('',#5435,#5498,#885,.F.);
#4641=EDGE_CURVE('',#5497,#5498,#886,.F.);
#4642=EDGE_CURVE('',#5464,#5440,#5941,.T.);
#4643=EDGE_CURVE('',#5441,#5465,#5942,.T.);
#4644=EDGE_CURVE('',#5468,#5445,#5943,.T.);
#4645=EDGE_CURVE('',#5446,#5469,#5944,.T.);
#4646=EDGE_CURVE('',#5492,#5443,#887,.F.);
#4647=EDGE_CURVE('',#5474,#5449,#5945,.T.);
#4648=EDGE_CURVE('',#5450,#5471,#5946,.T.);
#4649=EDGE_CURVE('',#5478,#5453,#5947,.T.);
#4650=EDGE_CURVE('',#5454,#5475,#5948,.T.);
#4651=EDGE_CURVE('',#5482,#5457,#5949,.T.);
#4652=EDGE_CURVE('',#5458,#5479,#5950,.T.);
#4653=EDGE_CURVE('',#5484,#5461,#5951,.T.);
#4654=EDGE_CURVE('',#5462,#5485,#5952,.T.);
#5049=VERTEX_POINT('',#13703);
#5050=VERTEX_POINT('',#13705);
#5051=VERTEX_POINT('',#13708);
#5052=VERTEX_POINT('',#13711);
#5053=VERTEX_POINT('',#13714);
#5054=VERTEX_POINT('',#13717);
#5055=VERTEX_POINT('',#13720);
#5056=VERTEX_POINT('',#13723);
#5057=VERTEX_POINT('',#13726);
#5058=VERTEX_POINT('',#13729);
#5059=VERTEX_POINT('',#13732);
#5060=VERTEX_POINT('',#13735);
#5061=VERTEX_POINT('',#13738);
#5062=VERTEX_POINT('',#13741);
#5063=VERTEX_POINT('',#13744);
#5064=VERTEX_POINT('',#13747);
#5065=VERTEX_POINT('',#13750);
#5066=VERTEX_POINT('',#13753);
#5067=VERTEX_POINT('',#13756);
#5068=VERTEX_POINT('',#13759);
#5069=VERTEX_POINT('',#13762);
#5070=VERTEX_POINT('',#13765);
#5071=VERTEX_POINT('',#13768);
#5072=VERTEX_POINT('',#13771);
#5073=VERTEX_POINT('',#13774);
#5074=VERTEX_POINT('',#13777);
#5075=VERTEX_POINT('',#13780);
#5076=VERTEX_POINT('',#13783);
#5077=VERTEX_POINT('',#13786);
#5078=VERTEX_POINT('',#13789);
#5079=VERTEX_POINT('',#13792);
#5080=VERTEX_POINT('',#13795);
#5081=VERTEX_POINT('',#13798);
#5082=VERTEX_POINT('',#13801);
#5083=VERTEX_POINT('',#13804);
#5084=VERTEX_POINT('',#13806);
#5085=VERTEX_POINT('',#13808);
#5086=VERTEX_POINT('',#13810);
#5087=VERTEX_POINT('',#13812);
#5088=VERTEX_POINT('',#13814);
#5089=VERTEX_POINT('',#13816);
#5090=VERTEX_POINT('',#13818);
#5091=VERTEX_POINT('',#13820);
#5092=VERTEX_POINT('',#13822);
#5093=VERTEX_POINT('',#13824);
#5094=VERTEX_POINT('',#13826);
#5095=VERTEX_POINT('',#13828);
#5096=VERTEX_POINT('',#13830);
#5097=VERTEX_POINT('',#13832);
#5098=VERTEX_POINT('',#13834);
#5099=VERTEX_POINT('',#13836);
#5100=VERTEX_POINT('',#13838);
#5101=VERTEX_POINT('',#13840);
#5102=VERTEX_POINT('',#13843);
#5103=VERTEX_POINT('',#13846);
#5104=VERTEX_POINT('',#13849);
#5105=VERTEX_POINT('',#13852);
#5106=VERTEX_POINT('',#13855);
#5107=VERTEX_POINT('',#13858);
#5108=VERTEX_POINT('',#13861);
#5109=VERTEX_POINT('',#13864);
#5110=VERTEX_POINT('',#13867);
#5111=VERTEX_POINT('',#13870);
#5112=VERTEX_POINT('',#13873);
#5113=VERTEX_POINT('',#13876);
#5114=VERTEX_POINT('',#13879);
#5115=VERTEX_POINT('',#13882);
#5116=VERTEX_POINT('',#13885);
#5117=VERTEX_POINT('',#13888);
#5118=VERTEX_POINT('',#13891);
#5119=VERTEX_POINT('',#13894);
#5120=VERTEX_POINT('',#13897);
#5121=VERTEX_POINT('',#13900);
#5122=VERTEX_POINT('',#13901);
#5123=VERTEX_POINT('',#13915);
#5124=VERTEX_POINT('',#13916);
#5125=VERTEX_POINT('',#13930);
#5126=VERTEX_POINT('',#13932);
#5127=VERTEX_POINT('',#13945);
#5128=VERTEX_POINT('',#13946);
#5129=VERTEX_POINT('',#13950);
#5130=VERTEX_POINT('',#13951);
#5131=VERTEX_POINT('',#13975);
#5132=VERTEX_POINT('',#13976);
#5133=VERTEX_POINT('',#13991);
#5134=VERTEX_POINT('',#14004);
#5135=VERTEX_POINT('',#14005);
#5136=VERTEX_POINT('',#14009);
#5137=VERTEX_POINT('',#14015);
#5138=VERTEX_POINT('',#14017);
#5139=VERTEX_POINT('',#14036);
#5140=VERTEX_POINT('',#14037);
#5141=VERTEX_POINT('',#14054);
#5142=VERTEX_POINT('',#14055);
#5143=VERTEX_POINT('',#14060);
#5144=VERTEX_POINT('',#14071);
#5145=VERTEX_POINT('',#14076);
#5146=VERTEX_POINT('',#14087);
#5147=VERTEX_POINT('',#14092);
#5148=VERTEX_POINT('',#14103);
#5149=VERTEX_POINT('',#14108);
#5150=VERTEX_POINT('',#14119);
#5151=VERTEX_POINT('',#14124);
#5152=VERTEX_POINT('',#14135);
#5153=VERTEX_POINT('',#14140);
#5154=VERTEX_POINT('',#14151);
#5155=VERTEX_POINT('',#14153);
#5156=VERTEX_POINT('',#14158);
#5157=VERTEX_POINT('',#14169);
#5158=VERTEX_POINT('',#14174);
#5159=VERTEX_POINT('',#14185);
#5160=VERTEX_POINT('',#14190);
#5161=VERTEX_POINT('',#14201);
#5162=VERTEX_POINT('',#14203);
#5163=VERTEX_POINT('',#14214);
#5164=VERTEX_POINT('',#14219);
#5165=VERTEX_POINT('',#14230);
#5166=VERTEX_POINT('',#14235);
#5167=VERTEX_POINT('',#14248);
#5168=VERTEX_POINT('',#14251);
#5169=VERTEX_POINT('',#14252);
#5170=VERTEX_POINT('',#14283);
#5171=VERTEX_POINT('',#14291);
#5172=VERTEX_POINT('',#14302);
#5173=VERTEX_POINT('',#14321);
#5174=VERTEX_POINT('',#14339);
#5175=VERTEX_POINT('',#14347);
#5176=VERTEX_POINT('',#14358);
#5177=VERTEX_POINT('',#14377);
#5178=VERTEX_POINT('',#14395);
#5179=VERTEX_POINT('',#14403);
#5180=VERTEX_POINT('',#14414);
#5181=VERTEX_POINT('',#14425);
#5182=VERTEX_POINT('',#14432);
#5183=VERTEX_POINT('',#14443);
#5184=VERTEX_POINT('',#14451);
#5185=VERTEX_POINT('',#14462);
#5186=VERTEX_POINT('',#14473);
#5187=VERTEX_POINT('',#14484);
#5188=VERTEX_POINT('',#14492);
#5189=VERTEX_POINT('',#14503);
#5190=VERTEX_POINT('',#14514);
#5191=VERTEX_POINT('',#14525);
#5192=VERTEX_POINT('',#14533);
#5193=VERTEX_POINT('',#14546);
#5194=VERTEX_POINT('',#14552);
#5195=VERTEX_POINT('',#14557);
#5196=VERTEX_POINT('',#14561);
#5197=VERTEX_POINT('',#14566);
#5198=VERTEX_POINT('',#14570);
#5199=VERTEX_POINT('',#14575);
#5200=VERTEX_POINT('',#14576);
#5201=VERTEX_POINT('',#14579);
#5202=VERTEX_POINT('',#14584);
#5203=VERTEX_POINT('',#14586);
#5204=VERTEX_POINT('',#14588);
#5205=VERTEX_POINT('',#14590);
#5206=VERTEX_POINT('',#14595);
#5207=VERTEX_POINT('',#14598);
#5208=VERTEX_POINT('',#14603);
#5209=VERTEX_POINT('',#14605);
#5210=VERTEX_POINT('',#14607);
#5211=VERTEX_POINT('',#14609);
#5212=VERTEX_POINT('',#14614);
#5213=VERTEX_POINT('',#14620);
#5214=VERTEX_POINT('',#14622);
#5215=VERTEX_POINT('',#14624);
#5216=VERTEX_POINT('',#14626);
#5217=VERTEX_POINT('',#14631);
#5218=VERTEX_POINT('',#14634);
#5219=VERTEX_POINT('',#14639);
#5220=VERTEX_POINT('',#14641);
#5221=VERTEX_POINT('',#14643);
#5222=VERTEX_POINT('',#14645);
#5223=VERTEX_POINT('',#14650);
#5224=VERTEX_POINT('',#14653);
#5225=VERTEX_POINT('',#14658);
#5226=VERTEX_POINT('',#14660);
#5227=VERTEX_POINT('',#14662);
#5228=VERTEX_POINT('',#14664);
#5229=VERTEX_POINT('',#14669);
#5230=VERTEX_POINT('',#14672);
#5231=VERTEX_POINT('',#14677);
#5232=VERTEX_POINT('',#14679);
#5233=VERTEX_POINT('',#14681);
#5234=VERTEX_POINT('',#14684);
#5235=VERTEX_POINT('',#14686);
#5236=VERTEX_POINT('',#14688);
#5237=VERTEX_POINT('',#14690);
#5238=VERTEX_POINT('',#14692);
#5239=VERTEX_POINT('',#14694);
#5240=VERTEX_POINT('',#14696);
#5241=VERTEX_POINT('',#14698);
#5242=VERTEX_POINT('',#14700);
#5243=VERTEX_POINT('',#14702);
#5244=VERTEX_POINT('',#14704);
#5245=VERTEX_POINT('',#14706);
#5246=VERTEX_POINT('',#14708);
#5247=VERTEX_POINT('',#14710);
#5248=VERTEX_POINT('',#14712);
#5249=VERTEX_POINT('',#14714);
#5250=VERTEX_POINT('',#14716);
#5251=VERTEX_POINT('',#14718);
#5252=VERTEX_POINT('',#14724);
#5253=VERTEX_POINT('',#14726);
#5254=VERTEX_POINT('',#14736);
#5255=VERTEX_POINT('',#14740);
#5256=VERTEX_POINT('',#14750);
#5257=VERTEX_POINT('',#14752);
#5258=VERTEX_POINT('',#14759);
#5259=VERTEX_POINT('',#14766);
#5260=VERTEX_POINT('',#14776);
#5261=VERTEX_POINT('',#14778);
#5262=VERTEX_POINT('',#14785);
#5263=VERTEX_POINT('',#14792);
#5264=VERTEX_POINT('',#14802);
#5265=VERTEX_POINT('',#14804);
#5266=VERTEX_POINT('',#14811);
#5267=VERTEX_POINT('',#14818);
#5268=VERTEX_POINT('',#14828);
#5269=VERTEX_POINT('',#14830);
#5270=VERTEX_POINT('',#14840);
#5271=VERTEX_POINT('',#14844);
#5272=VERTEX_POINT('',#14851);
#5273=VERTEX_POINT('',#14858);
#5274=VERTEX_POINT('',#14859);
#5275=VERTEX_POINT('',#14873);
#5276=VERTEX_POINT('',#14875);
#5277=VERTEX_POINT('',#14877);
#5278=VERTEX_POINT('',#14878);
#5279=VERTEX_POINT('',#14887);
#5280=VERTEX_POINT('',#14889);
#5281=VERTEX_POINT('',#14895);
#5282=VERTEX_POINT('',#14897);
#5283=VERTEX_POINT('',#14899);
#5284=VERTEX_POINT('',#14901);
#5285=VERTEX_POINT('',#14910);
#5286=VERTEX_POINT('',#14912);
#5287=VERTEX_POINT('',#14914);
#5288=VERTEX_POINT('',#14916);
#5289=VERTEX_POINT('',#14925);
#5290=VERTEX_POINT('',#14927);
#5291=VERTEX_POINT('',#14929);
#5292=VERTEX_POINT('',#14931);
#5293=VERTEX_POINT('',#14940);
#5294=VERTEX_POINT('',#14942);
#5295=VERTEX_POINT('',#14944);
#5296=VERTEX_POINT('',#14946);
#5297=VERTEX_POINT('',#14952);
#5298=VERTEX_POINT('',#14953);
#5299=VERTEX_POINT('',#14962);
#5300=VERTEX_POINT('',#14964);
#5301=VERTEX_POINT('',#14967);
#5302=VERTEX_POINT('',#14969);
#5303=VERTEX_POINT('',#14971);
#5304=VERTEX_POINT('',#14973);
#5305=VERTEX_POINT('',#14975);
#5306=VERTEX_POINT('',#14977);
#5307=VERTEX_POINT('',#14979);
#5308=VERTEX_POINT('',#14981);
#5309=VERTEX_POINT('',#14983);
#5310=VERTEX_POINT('',#14985);
#5311=VERTEX_POINT('',#14987);
#5312=VERTEX_POINT('',#14989);
#5313=VERTEX_POINT('',#14991);
#5314=VERTEX_POINT('',#14993);
#5315=VERTEX_POINT('',#14995);
#5316=VERTEX_POINT('',#14997);
#5317=VERTEX_POINT('',#14999);
#5318=VERTEX_POINT('',#15001);
#5319=VERTEX_POINT('',#15148);
#5320=VERTEX_POINT('',#15149);
#5321=VERTEX_POINT('',#15163);
#5322=VERTEX_POINT('',#15164);
#5323=VERTEX_POINT('',#15178);
#5324=VERTEX_POINT('',#15179);
#5325=VERTEX_POINT('',#15193);
#5326=VERTEX_POINT('',#15194);
#5327=VERTEX_POINT('',#15209);
#5328=VERTEX_POINT('',#15212);
#5329=VERTEX_POINT('',#15213);
#5330=VERTEX_POINT('',#15227);
#5331=VERTEX_POINT('',#15228);
#5332=VERTEX_POINT('',#15233);
#5333=VERTEX_POINT('',#15235);
#5334=VERTEX_POINT('',#15240);
#5335=VERTEX_POINT('',#15242);
#5336=VERTEX_POINT('',#15247);
#5337=VERTEX_POINT('',#15249);
#5338=VERTEX_POINT('',#15254);
#5339=VERTEX_POINT('',#15256);
#5340=VERTEX_POINT('',#15261);
#5341=VERTEX_POINT('',#15263);
#5342=VERTEX_POINT('',#15268);
#5343=VERTEX_POINT('',#15270);
#5344=VERTEX_POINT('',#15275);
#5345=VERTEX_POINT('',#15277);
#5346=VERTEX_POINT('',#15282);
#5347=VERTEX_POINT('',#15284);
#5348=VERTEX_POINT('',#15289);
#5349=VERTEX_POINT('',#15291);
#5350=VERTEX_POINT('',#15296);
#5351=VERTEX_POINT('',#15298);
#5352=VERTEX_POINT('',#15303);
#5353=VERTEX_POINT('',#15305);
#5354=VERTEX_POINT('',#15311);
#5355=VERTEX_POINT('',#15313);
#5356=VERTEX_POINT('',#15314);
#5357=VERTEX_POINT('',#15317);
#5358=VERTEX_POINT('',#15319);
#5359=VERTEX_POINT('',#15321);
#5360=VERTEX_POINT('',#15322);
#5361=VERTEX_POINT('',#15325);
#5362=VERTEX_POINT('',#15328);
#5363=VERTEX_POINT('',#15333);
#5364=VERTEX_POINT('',#15338);
#5365=VERTEX_POINT('',#15343);
#5366=VERTEX_POINT('',#15348);
#5367=VERTEX_POINT('',#15353);
#5368=VERTEX_POINT('',#15358);
#5369=VERTEX_POINT('',#15360);
#5370=VERTEX_POINT('',#15365);
#5371=VERTEX_POINT('',#15370);
#5372=VERTEX_POINT('',#15375);
#5373=VERTEX_POINT('',#15380);
#5374=VERTEX_POINT('',#15385);
#5375=VERTEX_POINT('',#15390);
#5376=VERTEX_POINT('',#15397);
#5377=VERTEX_POINT('',#15398);
#5378=VERTEX_POINT('',#15407);
#5379=VERTEX_POINT('',#15412);
#5380=VERTEX_POINT('',#15417);
#5381=VERTEX_POINT('',#15422);
#5382=VERTEX_POINT('',#15427);
#5383=VERTEX_POINT('',#15432);
#5384=VERTEX_POINT('',#15437);
#5385=VERTEX_POINT('',#15442);
#5386=VERTEX_POINT('',#15447);
#5387=VERTEX_POINT('',#15452);
#5388=VERTEX_POINT('',#15459);
#5389=VERTEX_POINT('',#15460);
#5390=VERTEX_POINT('',#15468);
#5391=VERTEX_POINT('',#15469);
#5392=VERTEX_POINT('',#15491);
#5393=VERTEX_POINT('',#15492);
#5394=VERTEX_POINT('',#15494);
#5395=VERTEX_POINT('',#15502);
#5396=VERTEX_POINT('',#15503);
#5397=VERTEX_POINT('',#15505);
#5398=VERTEX_POINT('',#15509);
#5399=VERTEX_POINT('',#15510);
#5400=VERTEX_POINT('',#15527);
#5401=VERTEX_POINT('',#15528);
#5402=VERTEX_POINT('',#15535);
#5403=VERTEX_POINT('',#15540);
#5404=VERTEX_POINT('',#15554);
#5405=VERTEX_POINT('',#15559);
#5406=VERTEX_POINT('',#15564);
#5407=VERTEX_POINT('',#15574);
#5408=VERTEX_POINT('',#15593);
#5409=VERTEX_POINT('',#15598);
#5410=VERTEX_POINT('',#15608);
#5411=VERTEX_POINT('',#15613);
#5412=VERTEX_POINT('',#15618);
#5413=VERTEX_POINT('',#15628);
#5414=VERTEX_POINT('',#15642);
#5415=VERTEX_POINT('',#15652);
#5416=VERTEX_POINT('',#15656);
#5417=VERTEX_POINT('',#15658);
#5418=VERTEX_POINT('',#15663);
#5419=VERTEX_POINT('',#15677);
#5420=VERTEX_POINT('',#15692);
#5421=VERTEX_POINT('',#15697);
#5422=VERTEX_POINT('',#15707);
#5423=VERTEX_POINT('',#15712);
#5424=VERTEX_POINT('',#15717);
#5425=VERTEX_POINT('',#15727);
#5426=VERTEX_POINT('',#15746);
#5427=VERTEX_POINT('',#15751);
#5428=VERTEX_POINT('',#15761);
#5429=VERTEX_POINT('',#15766);
#5430=VERTEX_POINT('',#15771);
#5431=VERTEX_POINT('',#15781);
#5432=VERTEX_POINT('',#15800);
#5433=VERTEX_POINT('',#15805);
#5434=VERTEX_POINT('',#15815);
#5435=VERTEX_POINT('',#15820);
#5436=VERTEX_POINT('',#15825);
#5437=VERTEX_POINT('',#15835);
#5438=VERTEX_POINT('',#15850);
#5439=VERTEX_POINT('',#15855);
#5440=VERTEX_POINT('',#15869);
#5441=VERTEX_POINT('',#15870);
#5442=VERTEX_POINT('',#15886);
#5443=VERTEX_POINT('',#15888);
#5444=VERTEX_POINT('',#15893);
#5445=VERTEX_POINT('',#15907);
#5446=VERTEX_POINT('',#15908);
#5447=VERTEX_POINT('',#15929);
#5448=VERTEX_POINT('',#15934);
#5449=VERTEX_POINT('',#15948);
#5450=VERTEX_POINT('',#15949);
#5451=VERTEX_POINT('',#15965);
#5452=VERTEX_POINT('',#15970);
#5453=VERTEX_POINT('',#15984);
#5454=VERTEX_POINT('',#15985);
#5455=VERTEX_POINT('',#16001);
#5456=VERTEX_POINT('',#16006);
#5457=VERTEX_POINT('',#16020);
#5458=VERTEX_POINT('',#16021);
#5459=VERTEX_POINT('',#16037);
#5460=VERTEX_POINT('',#16042);
#5461=VERTEX_POINT('',#16056);
#5462=VERTEX_POINT('',#16057);
#5463=VERTEX_POINT('',#16073);
#5464=VERTEX_POINT('',#16074);
#5465=VERTEX_POINT('',#16100);
#5466=VERTEX_POINT('',#16105);
#5467=VERTEX_POINT('',#16130);
#5468=VERTEX_POINT('',#16131);
#5469=VERTEX_POINT('',#16157);
#5470=VERTEX_POINT('',#16162);
#5471=VERTEX_POINT('',#16208);
#5472=VERTEX_POINT('',#16209);
#5473=VERTEX_POINT('',#16214);
#5474=VERTEX_POINT('',#16232);
#5475=VERTEX_POINT('',#16263);
#5476=VERTEX_POINT('',#16264);
#5477=VERTEX_POINT('',#16269);
#5478=VERTEX_POINT('',#16289);
#5479=VERTEX_POINT('',#16320);
#5480=VERTEX_POINT('',#16321);
#5481=VERTEX_POINT('',#16326);
#5482=VERTEX_POINT('',#16346);
#5483=VERTEX_POINT('',#16356);
#5484=VERTEX_POINT('',#16357);
#5485=VERTEX_POINT('',#16381);
#5486=VERTEX_POINT('',#16386);
#5487=VERTEX_POINT('',#16411);
#5488=VERTEX_POINT('',#16421);
#5489=VERTEX_POINT('',#16436);
#5490=VERTEX_POINT('',#16446);
#5491=VERTEX_POINT('',#16466);
#5492=VERTEX_POINT('',#16476);
#5493=VERTEX_POINT('',#16483);
#5494=VERTEX_POINT('',#16493);
#5495=VERTEX_POINT('',#16508);
#5496=VERTEX_POINT('',#16518);
#5497=VERTEX_POINT('',#16533);
#5498=VERTEX_POINT('',#16543);
#5697=CIRCLE('',#8693,0.016);
#5698=CIRCLE('',#8694,0.016);
#5699=CIRCLE('',#8696,0.01635);
#5700=CIRCLE('',#8698,0.01635);
#5701=CIRCLE('',#8700,0.01635);
#5702=CIRCLE('',#8702,0.01635);
#5703=CIRCLE('',#8704,0.016);
#5704=CIRCLE('',#8706,0.016);
#5705=CIRCLE('',#8708,0.016);
#5706=CIRCLE('',#8710,0.016);
#5707=CIRCLE('',#8712,0.01635);
#5708=CIRCLE('',#8714,0.01635);
#5709=CIRCLE('',#8716,0.01635);
#5710=CIRCLE('',#8718,0.01635);
#5711=CIRCLE('',#8720,0.016);
#5712=CIRCLE('',#8722,0.016);
#5713=CIRCLE('',#8724,0.016);
#5714=CIRCLE('',#8726,0.016);
#5715=CIRCLE('',#8728,0.01635);
#5716=CIRCLE('',#8730,0.01635);
#5717=CIRCLE('',#8732,0.01635);
#5718=CIRCLE('',#8734,0.01635);
#5719=CIRCLE('',#8736,0.016);
#5720=CIRCLE('',#8738,0.016);
#5721=CIRCLE('',#8740,0.016);
#5722=CIRCLE('',#8742,0.016);
#5723=CIRCLE('',#8744,0.0175);
#5724=CIRCLE('',#8746,0.0125);
#5725=CIRCLE('',#8748,0.0175);
#5726=CIRCLE('',#8750,0.0125);
#5727=CIRCLE('',#8752,0.0185);
#5728=CIRCLE('',#8754,0.0115);
#5729=CIRCLE('',#8756,0.0185);
#5730=CIRCLE('',#8758,0.0114999999999814);
#5731=CIRCLE('',#8760,0.0330000000001318);
#5732=CIRCLE('',#8761,0.0013);
#5733=CIRCLE('',#8762,0.0013);
#5734=CIRCLE('',#8763,0.0013);
#5735=CIRCLE('',#8764,0.0013);
#5736=CIRCLE('',#8765,0.0013);
#5737=CIRCLE('',#8766,0.0013);
#5738=CIRCLE('',#8767,0.0013);
#5739=CIRCLE('',#8768,0.0013);
#5740=CIRCLE('',#8769,0.0013);
#5741=CIRCLE('',#8770,0.0013);
#5742=CIRCLE('',#8771,0.0013);
#5743=CIRCLE('',#8772,0.0013);
#5744=CIRCLE('',#8773,0.0013);
#5745=CIRCLE('',#8774,0.0013);
#5746=CIRCLE('',#8775,0.0013);
#5747=CIRCLE('',#8776,0.0013);
#5748=CIRCLE('',#8777,0.0013);
#5749=CIRCLE('',#8778,0.0013);
#5750=CIRCLE('',#8780,0.012);
#5751=CIRCLE('',#8782,0.0013);
#5752=CIRCLE('',#8784,0.0013);
#5753=CIRCLE('',#8786,0.0013);
#5754=CIRCLE('',#8788,0.0013);
#5755=CIRCLE('',#8790,0.0013);
#5756=CIRCLE('',#8792,0.0013);
#5757=CIRCLE('',#8794,0.0013);
#5758=CIRCLE('',#8796,0.0013);
#5759=CIRCLE('',#8798,0.0013);
#5760=CIRCLE('',#8800,0.0013);
#5761=CIRCLE('',#8802,0.0013);
#5762=CIRCLE('',#8804,0.0013);
#5763=CIRCLE('',#8806,0.0013);
#5764=CIRCLE('',#8808,0.0013);
#5765=CIRCLE('',#8810,0.0013);
#5766=CIRCLE('',#8812,0.0013);
#5767=CIRCLE('',#8814,0.0013);
#5768=CIRCLE('',#8816,0.0013);
#5769=CIRCLE('',#8818,0.033999999999839);
#5770=CIRCLE('',#8820,0.0120000000000334);
#5771=CIRCLE('',#8822,0.0330000000001318);
#5772=CIRCLE('',#8823,0.0195);
#5773=CIRCLE('',#8825,0.034);
#5774=CIRCLE('',#8827,0.0115);
#5775=CIRCLE('',#8831,0.0115);
#5776=CIRCLE('',#8833,0.016303847577153);
#5777=CIRCLE('',#8835,0.0125);
#5778=CIRCLE('',#8837,0.016035898385);
#5779=CIRCLE('',#8840,0.0124999999996045);
#5780=CIRCLE('',#8842,0.016035898385);
#5781=CIRCLE('',#8843,0.016035898385);
#5782=CIRCLE('',#8845,0.0127999999998078);
#5783=CIRCLE('',#8847,0.017035898385);
#5784=CIRCLE('',#8850,0.0175358983831627);
#5785=CIRCLE('',#8855,0.0175358983842906);
#5786=CIRCLE('',#8860,0.0175358983832975);
#5787=CIRCLE('',#8863,0.00149999999977719);
#5788=CIRCLE('',#8867,0.0175358983831629);
#5789=CIRCLE('',#8872,0.0175358983842908);
#5790=CIRCLE('',#8877,0.0175358983832977);
#5791=CIRCLE('',#8880,0.0157358983850606);
#5792=CIRCLE('',#8882,0.017035898385);
#5793=CIRCLE('',#8884,0.0015);
#5794=CIRCLE('',#8885,0.0015);
#5795=CIRCLE('',#8887,0.0330000000001318);
#5796=CIRCLE('',#8888,0.0015);
#5797=CIRCLE('',#8889,0.0015);
#5798=CIRCLE('',#8890,0.0015);
#5799=CIRCLE('',#8891,0.024);
#5800=CIRCLE('',#8892,0.0015);
#5801=CIRCLE('',#8893,0.0015);
#5802=CIRCLE('',#8894,0.0015);
#5803=CIRCLE('',#8895,0.0015);
#5804=CIRCLE('',#8896,0.024);
#5805=CIRCLE('',#8897,0.0015);
#5806=CIRCLE('',#8898,0.0015);
#5807=CIRCLE('',#8899,0.0015);
#5808=CIRCLE('',#8900,0.024);
#5809=CIRCLE('',#8901,0.0015);
#5810=CIRCLE('',#8902,0.0015);
#5811=CIRCLE('',#8903,0.0015);
#5812=CIRCLE('',#8904,0.0015);
#5813=CIRCLE('',#8905,0.024);
#5814=CIRCLE('',#8906,0.0015);
#5815=CIRCLE('',#8907,0.0015);
#5816=CIRCLE('',#8908,0.0015);
#5817=CIRCLE('',#8909,0.0015);
#5818=CIRCLE('',#8910,0.024);
#5819=CIRCLE('',#8911,0.0015);
#5820=CIRCLE('',#8912,0.0015);
#5821=CIRCLE('',#8913,0.0015);
#5822=CIRCLE('',#8914,0.0015);
#5823=CIRCLE('',#8915,0.024);
#5824=CIRCLE('',#8916,0.0015);
#5825=CIRCLE('',#8917,0.0013);
#5826=CIRCLE('',#8918,0.0013);
#5827=CIRCLE('',#8919,0.0013);
#5828=CIRCLE('',#8920,0.0013);
#5829=CIRCLE('',#8921,0.0013);
#5830=CIRCLE('',#8922,0.0013);
#5831=CIRCLE('',#8923,0.0013);
#5832=CIRCLE('',#8924,0.0013);
#5833=CIRCLE('',#8925,0.0013);
#5834=CIRCLE('',#8926,0.0013);
#5835=CIRCLE('',#8927,0.0013);
#5836=CIRCLE('',#8928,0.0013);
#5837=CIRCLE('',#8929,0.0013);
#5838=CIRCLE('',#8930,0.0013);
#5839=CIRCLE('',#8931,0.0013);
#5840=CIRCLE('',#8932,0.0013);
#5841=CIRCLE('',#8933,0.0013);
#5842=CIRCLE('',#8934,0.0013);
#5843=CIRCLE('',#8936,0.0015);
#5844=CIRCLE('',#8938,0.017035898385);
#5845=CIRCLE('',#8940,0.0015);
#5846=CIRCLE('',#8942,0.0015);
#5847=CIRCLE('',#8944,0.017035898385);
#5848=CIRCLE('',#8946,0.0015);
#5849=CIRCLE('',#8948,0.0015);
#5850=CIRCLE('',#8950,0.017035898385);
#5851=CIRCLE('',#8952,0.0015);
#5852=CIRCLE('',#8954,0.0015);
#5853=CIRCLE('',#8956,0.017035898385);
#5854=CIRCLE('',#8958,0.0015);
#5855=CIRCLE('',#8960,0.0015);
#5856=CIRCLE('',#8962,0.017035898385);
#5857=CIRCLE('',#8964,0.0015);
#5858=CIRCLE('',#8966,0.0015);
#5859=CIRCLE('',#8968,0.0160358983845746);
#5860=CIRCLE('',#8970,0.0330000000001318);
#5861=CIRCLE('',#8971,0.0163358983848079);
#5862=CIRCLE('',#8972,0.0015);
#5863=CIRCLE('',#8973,0.0015);
#5864=CIRCLE('',#8974,0.024);
#5865=CIRCLE('',#8975,0.0015);
#5866=CIRCLE('',#8976,0.024);
#5867=CIRCLE('',#8977,0.0015);
#5868=CIRCLE('',#8978,0.0015);
#5869=CIRCLE('',#8979,0.024);
#5870=CIRCLE('',#8980,0.0015);
#5871=CIRCLE('',#8981,0.0015);
#5872=CIRCLE('',#8982,0.024);
#5873=CIRCLE('',#8983,0.0015);
#5874=CIRCLE('',#8984,0.0015);
#5875=CIRCLE('',#8985,0.024);
#5876=CIRCLE('',#8986,0.0015);
#5877=CIRCLE('',#8987,0.0015);
#5878=CIRCLE('',#8988,0.0015);
#5879=CIRCLE('',#8989,0.024);
#5880=CIRCLE('',#8990,0.0013);
#5881=CIRCLE('',#8991,0.0013);
#5882=CIRCLE('',#8992,0.0013);
#5883=CIRCLE('',#8993,0.0013);
#5884=CIRCLE('',#8994,0.0013);
#5885=CIRCLE('',#8995,0.0013);
#5886=CIRCLE('',#8996,0.0013);
#5887=CIRCLE('',#8997,0.0013);
#5888=CIRCLE('',#8998,0.0013);
#5889=CIRCLE('',#8999,0.0013);
#5890=CIRCLE('',#9000,0.0013);
#5891=CIRCLE('',#9001,0.0013);
#5892=CIRCLE('',#9002,0.0013);
#5893=CIRCLE('',#9003,0.0013);
#5894=CIRCLE('',#9004,0.0013);
#5895=CIRCLE('',#9005,0.0013);
#5896=CIRCLE('',#9006,0.0013);
#5897=CIRCLE('',#9007,0.0013);
#5898=CIRCLE('',#9057,0.033999999999839);
#5899=CIRCLE('',#9059,0.016035898385);
#5900=CIRCLE('',#9061,0.016035898385);
#5901=CIRCLE('',#9063,0.033999999999839);
#5902=CIRCLE('',#9066,0.0163358983848079);
#5903=CIRCLE('',#9068,0.016035898385);
#5904=CIRCLE('',#9070,0.016535898385);
#5905=CIRCLE('',#9071,0.0236999999709827);
#5906=CIRCLE('',#9072,0.016535898385);
#5907=CIRCLE('',#9073,0.023699999971322);
#5908=CIRCLE('',#9074,0.016535898385);
#5909=CIRCLE('',#9075,0.0236999999560649);
#5910=CIRCLE('',#9076,0.016535898385);
#5911=CIRCLE('',#9077,0.023699999970982);
#5912=CIRCLE('',#9078,0.016535898385);
#5913=CIRCLE('',#9079,0.0236999999713218);
#5914=CIRCLE('',#9080,0.016535898385);
#5915=CIRCLE('',#9081,0.0236999999852865);
#5916=CIRCLE('',#9082,0.00244999999960406);
#5917=CIRCLE('',#9083,0.00244999999980786);
#5918=CIRCLE('',#9084,0.00244999999980786);
#5919=CIRCLE('',#9085,0.00245000000014319);
#5920=CIRCLE('',#9086,0.00245000000014319);
#5921=CIRCLE('',#9087,0.00244999999980786);
#5922=CIRCLE('',#9088,0.00244999999980786);
#5923=CIRCLE('',#9089,0.00244999999960406);
#5924=CIRCLE('',#9091,0.00150000000045805);
#5925=CIRCLE('',#9092,0.0167858983853131);
#5926=CIRCLE('',#9093,0.00150000000045805);
#5927=CIRCLE('',#9096,0.00215000000003398);
#5928=CIRCLE('',#9098,0.00214999999960455);
#5929=CIRCLE('',#9101,0.00214999999988175);
#5930=CIRCLE('',#9102,0.00215000000003398);
#5931=CIRCLE('',#9104,0.00214999999988175);
#5932=CIRCLE('',#9105,0.00215000000003398);
#5933=CIRCLE('',#9107,0.00214999999960455);
#5934=CIRCLE('',#9109,0.00214999999960455);
#5935=CIRCLE('',#9111,0.00215000000003398);
#5936=CIRCLE('',#9121,0.000299999999290666);
#5937=CIRCLE('',#9123,0.000300000000142203);
#5938=CIRCLE('',#9124,0.0239999999561171);
#5939=CIRCLE('',#9141,0.0238500000003131);
#5940=CIRCLE('',#9162,0.024);
#5941=CIRCLE('',#9172,0.000299999999686457);
#5942=CIRCLE('',#9173,0.000300000000366869);
#5943=CIRCLE('',#9175,0.000299999999799668);
#5944=CIRCLE('',#9176,0.000299999999934399);
#5945=CIRCLE('',#9179,0.000300000000165203);
#5946=CIRCLE('',#9180,0.000299999999993383);
#5947=CIRCLE('',#9182,0.000299999999686456);
#5948=CIRCLE('',#9183,0.000300000000366864);
#5949=CIRCLE('',#9185,0.000299999999799668);
#5950=CIRCLE('',#9186,0.000299999999934399);
#5951=CIRCLE('',#9188,0.000300000000165203);
#5952=CIRCLE('',#9189,0.000299999999993381);
#6263=EDGE_LOOP('',(#2258));
#6264=EDGE_LOOP('',(#2259));
#6265=EDGE_LOOP('',(#2260));
#6266=EDGE_LOOP('',(#2261));
#6267=EDGE_LOOP('',(#2262));
#6268=EDGE_LOOP('',(#2263));
#6269=EDGE_LOOP('',(#2264));
#6270=EDGE_LOOP('',(#2265));
#6271=EDGE_LOOP('',(#2266));
#6272=EDGE_LOOP('',(#2267));
#6273=EDGE_LOOP('',(#2268));
#6274=EDGE_LOOP('',(#2269));
#6275=EDGE_LOOP('',(#2270));
#6276=EDGE_LOOP('',(#2271));
#6277=EDGE_LOOP('',(#2272));
#6278=EDGE_LOOP('',(#2273));
#6279=EDGE_LOOP('',(#2274));
#6280=EDGE_LOOP('',(#2275));
#6281=EDGE_LOOP('',(#2276));
#6282=EDGE_LOOP('',(#2277));
#6283=EDGE_LOOP('',(#2278));
#6284=EDGE_LOOP('',(#2279));
#6285=EDGE_LOOP('',(#2280));
#6286=EDGE_LOOP('',(#2281));
#6287=EDGE_LOOP('',(#2282));
#6288=EDGE_LOOP('',(#2283));
#6289=EDGE_LOOP('',(#2284));
#6290=EDGE_LOOP('',(#2285));
#6291=EDGE_LOOP('',(#2286));
#6292=EDGE_LOOP('',(#2287));
#6293=EDGE_LOOP('',(#2288));
#6294=EDGE_LOOP('',(#2289));
#6295=EDGE_LOOP('',(#2290));
#6296=EDGE_LOOP('',(#2291));
#6297=EDGE_LOOP('',(#2292));
#6298=EDGE_LOOP('',(#2293));
#6299=EDGE_LOOP('',(#2294));
#6300=EDGE_LOOP('',(#2295));
#6301=EDGE_LOOP('',(#2296));
#6302=EDGE_LOOP('',(#2297));
#6303=EDGE_LOOP('',(#2298));
#6304=EDGE_LOOP('',(#2299));
#6305=EDGE_LOOP('',(#2300));
#6306=EDGE_LOOP('',(#2301));
#6307=EDGE_LOOP('',(#2302));
#6308=EDGE_LOOP('',(#2303));
#6309=EDGE_LOOP('',(#2304));
#6310=EDGE_LOOP('',(#2305));
#6311=EDGE_LOOP('',(#2306));
#6312=EDGE_LOOP('',(#2307));
#6313=EDGE_LOOP('',(#2308));
#6314=EDGE_LOOP('',(#2309));
#6315=EDGE_LOOP('',(#2310));
#6316=EDGE_LOOP('',(#2311));
#6317=EDGE_LOOP('',(#2312));
#6318=EDGE_LOOP('',(#2313));
#6319=EDGE_LOOP('',(#2314));
#6320=EDGE_LOOP('',(#2315));
#6321=EDGE_LOOP('',(#2316));
#6322=EDGE_LOOP('',(#2317));
#6323=EDGE_LOOP('',(#2318));
#6324=EDGE_LOOP('',(#2319));
#6325=EDGE_LOOP('',(#2320));
#6326=EDGE_LOOP('',(#2321));
#6327=EDGE_LOOP('',(#2322));
#6328=EDGE_LOOP('',(#2323));
#6329=EDGE_LOOP('',(#2324));
#6330=EDGE_LOOP('',(#2325));
#6331=EDGE_LOOP('',(#2326));
#6332=EDGE_LOOP('',(#2327));
#6333=EDGE_LOOP('',(#2328));
#6334=EDGE_LOOP('',(#2329));
#6335=EDGE_LOOP('',(#2330));
#6336=EDGE_LOOP('',(#2331));
#6337=EDGE_LOOP('',(#2332));
#6338=EDGE_LOOP('',(#2333));
#6339=EDGE_LOOP('',(#2334));
#6340=EDGE_LOOP('',(#2335));
#6341=EDGE_LOOP('',(#2336));
#6342=EDGE_LOOP('',(#2337));
#6343=EDGE_LOOP('',(#2338));
#6344=EDGE_LOOP('',(#2339));
#6345=EDGE_LOOP('',(#2340));
#6346=EDGE_LOOP('',(#2341));
#6347=EDGE_LOOP('',(#2342));
#6348=EDGE_LOOP('',(#2343));
#6349=EDGE_LOOP('',(#2344));
#6350=EDGE_LOOP('',(#2345));
#6351=EDGE_LOOP('',(#2346));
#6352=EDGE_LOOP('',(#2347));
#6353=EDGE_LOOP('',(#2348));
#6354=EDGE_LOOP('',(#2349));
#6355=EDGE_LOOP('',(#2350));
#6356=EDGE_LOOP('',(#2351));
#6357=EDGE_LOOP('',(#2352));
#6358=EDGE_LOOP('',(#2353));
#6359=EDGE_LOOP('',(#2354));
#6360=EDGE_LOOP('',(#2355));
#6361=EDGE_LOOP('',(#2356));
#6362=EDGE_LOOP('',(#2357));
#6363=EDGE_LOOP('',(#2358));
#6364=EDGE_LOOP('',(#2359));
#6365=EDGE_LOOP('',(#2360));
#6366=EDGE_LOOP('',(#2361));
#6367=EDGE_LOOP('',(#2362));
#6368=EDGE_LOOP('',(#2363));
#6369=EDGE_LOOP('',(#2364));
#6370=EDGE_LOOP('',(#2365));
#6371=EDGE_LOOP('',(#2366));
#6372=EDGE_LOOP('',(#2367));
#6373=EDGE_LOOP('',(#2368));
#6374=EDGE_LOOP('',(#2369));
#6375=EDGE_LOOP('',(#2370));
#6376=EDGE_LOOP('',(#2371));
#6377=EDGE_LOOP('',(#2372));
#6378=EDGE_LOOP('',(#2373));
#6379=EDGE_LOOP('',(#2374));
#6380=EDGE_LOOP('',(#2375));
#6381=EDGE_LOOP('',(#2376));
#6382=EDGE_LOOP('',(#2377));
#6383=EDGE_LOOP('',(#2378));
#6384=EDGE_LOOP('',(#2379));
#6385=EDGE_LOOP('',(#2380));
#6386=EDGE_LOOP('',(#2381));
#6387=EDGE_LOOP('',(#2382,#2383));
#6388=EDGE_LOOP('',(#2384));
#6389=EDGE_LOOP('',(#2385));
#6390=EDGE_LOOP('',(#2386,#2387));
#6391=EDGE_LOOP('',(#2388));
#6392=EDGE_LOOP('',(#2389));
#6393=EDGE_LOOP('',(#2390));
#6394=EDGE_LOOP('',(#2391));
#6395=EDGE_LOOP('',(#2392));
#6396=EDGE_LOOP('',(#2393));
#6397=EDGE_LOOP('',(#2394));
#6398=EDGE_LOOP('',(#2395));
#6399=EDGE_LOOP('',(#2396));
#6400=EDGE_LOOP('',(#2397));
#6401=EDGE_LOOP('',(#2398));
#6402=EDGE_LOOP('',(#2399));
#6403=EDGE_LOOP('',(#2400));
#6404=EDGE_LOOP('',(#2401));
#6405=EDGE_LOOP('',(#2402));
#6406=EDGE_LOOP('',(#2403));
#6407=EDGE_LOOP('',(#2404));
#6408=EDGE_LOOP('',(#2405));
#6409=EDGE_LOOP('',(#2406));
#6410=EDGE_LOOP('',(#2407));
#6411=EDGE_LOOP('',(#2408,#2409));
#6412=EDGE_LOOP('',(#2410,#2411));
#6413=EDGE_LOOP('',(#2412,#2413));
#6414=EDGE_LOOP('',(#2414,#2415));
#6415=EDGE_LOOP('',(#2416));
#6416=EDGE_LOOP('',(#2417,#2418));
#6417=EDGE_LOOP('',(#2419,#2420));
#6418=EDGE_LOOP('',(#2421));
#6419=EDGE_LOOP('',(#2422,#2423));
#6420=EDGE_LOOP('',(#2424));
#6421=EDGE_LOOP('',(#2425,#2426));
#6422=EDGE_LOOP('',(#2427,#2428));
#6423=EDGE_LOOP('',(#2429));
#6424=EDGE_LOOP('',(#2430));
#6425=EDGE_LOOP('',(#2431,#2432,#2433,#2434));
#6426=EDGE_LOOP('',(#2435,#2436,#2437,#2438));
#6427=EDGE_LOOP('',(#2439,#2440));
#6428=EDGE_LOOP('',(#2441));
#6429=EDGE_LOOP('',(#2442,#2443));
#6430=EDGE_LOOP('',(#2444,#2445,#2446,#2447,#2448,#2449,#2450,#2451,#2452,
#2453,#2454,#2455,#2456,#2457,#2458,#2459,#2460,#2461,#2462,#2463,#2464,
#2465,#2466,#2467,#2468,#2469));
#6431=EDGE_LOOP('',(#2470,#2471));
#6432=EDGE_LOOP('',(#2472));
#6433=EDGE_LOOP('',(#2473,#2474,#2475,#2476,#2477));
#6434=EDGE_LOOP('',(#2478,#2479,#2480,#2481));
#6435=EDGE_LOOP('',(#2482,#2483,#2484,#2485));
#6436=EDGE_LOOP('',(#2486,#2487,#2488,#2489));
#6437=EDGE_LOOP('',(#2490,#2491,#2492,#2493));
#6438=EDGE_LOOP('',(#2494,#2495,#2496,#2497));
#6439=EDGE_LOOP('',(#2498,#2499,#2500,#2501));
#6440=EDGE_LOOP('',(#2502,#2503,#2504,#2505));
#6441=EDGE_LOOP('',(#2506,#2507,#2508,#2509));
#6442=EDGE_LOOP('',(#2510,#2511,#2512,#2513));
#6443=EDGE_LOOP('',(#2514,#2515,#2516,#2517));
#6444=EDGE_LOOP('',(#2518,#2519,#2520,#2521));
#6445=EDGE_LOOP('',(#2522,#2523,#2524,#2525));
#6446=EDGE_LOOP('',(#2526,#2527,#2528,#2529));
#6447=EDGE_LOOP('',(#2530,#2531,#2532,#2533));
#6448=EDGE_LOOP('',(#2534,#2535,#2536,#2537));
#6449=EDGE_LOOP('',(#2538,#2539,#2540,#2541));
#6450=EDGE_LOOP('',(#2542,#2543,#2544,#2545));
#6451=EDGE_LOOP('',(#2546,#2547,#2548,#2549));
#6452=EDGE_LOOP('',(#2550,#2551,#2552,#2553));
#6453=EDGE_LOOP('',(#2554,#2555,#2556,#2557));
#6454=EDGE_LOOP('',(#2558,#2559,#2560,#2561));
#6455=EDGE_LOOP('',(#2562,#2563,#2564,#2565));
#6456=EDGE_LOOP('',(#2566,#2567,#2568,#2569));
#6457=EDGE_LOOP('',(#2570,#2571,#2572,#2573));
#6458=EDGE_LOOP('',(#2574));
#6459=EDGE_LOOP('',(#2575));
#6460=EDGE_LOOP('',(#2576,#2577,#2578,#2579));
#6461=EDGE_LOOP('',(#2580,#2581,#2582,#2583,#2584));
#6462=EDGE_LOOP('',(#2585));
#6463=EDGE_LOOP('',(#2586,#2587,#2588,#2589,#2590,#2591,#2592,#2593,#2594,
#2595,#2596,#2597,#2598,#2599,#2600,#2601,#2602,#2603,#2604,#2605,#2606,
#2607,#2608,#2609,#2610,#2611,#2612,#2613,#2614,#2615,#2616,#2617,#2618,
#2619,#2620,#2621,#2622,#2623,#2624,#2625,#2626,#2627,#2628,#2629,#2630,
#2631,#2632,#2633));
#6464=EDGE_LOOP('',(#2634));
#6465=EDGE_LOOP('',(#2635));
#6466=EDGE_LOOP('',(#2636));
#6467=EDGE_LOOP('',(#2637));
#6468=EDGE_LOOP('',(#2638));
#6469=EDGE_LOOP('',(#2639));
#6470=EDGE_LOOP('',(#2640));
#6471=EDGE_LOOP('',(#2641));
#6472=EDGE_LOOP('',(#2642));
#6473=EDGE_LOOP('',(#2643));
#6474=EDGE_LOOP('',(#2644));
#6475=EDGE_LOOP('',(#2645));
#6476=EDGE_LOOP('',(#2646));
#6477=EDGE_LOOP('',(#2647));
#6478=EDGE_LOOP('',(#2648));
#6479=EDGE_LOOP('',(#2649));
#6480=EDGE_LOOP('',(#2650));
#6481=EDGE_LOOP('',(#2651));
#6482=EDGE_LOOP('',(#2652,#2653,#2654,#2655,#2656));
#6483=EDGE_LOOP('',(#2657,#2658,#2659,#2660));
#6484=EDGE_LOOP('',(#2661,#2662,#2663,#2664,#2665));
#6485=EDGE_LOOP('',(#2666,#2667,#2668,#2669,#2670));
#6486=EDGE_LOOP('',(#2671,#2672,#2673,#2674));
#6487=EDGE_LOOP('',(#2675,#2676,#2677,#2678,#2679));
#6488=EDGE_LOOP('',(#2680,#2681,#2682,#2683,#2684));
#6489=EDGE_LOOP('',(#2685,#2686,#2687,#2688,#2689));
#6490=EDGE_LOOP('',(#2690,#2691,#2692,#2693,#2694));
#6491=EDGE_LOOP('',(#2695,#2696,#2697,#2698,#2699));
#6492=EDGE_LOOP('',(#2700,#2701,#2702,#2703));
#6493=EDGE_LOOP('',(#2704,#2705,#2706,#2707,#2708));
#6494=EDGE_LOOP('',(#2709,#2710,#2711,#2712,#2713));
#6495=EDGE_LOOP('',(#2714,#2715,#2716,#2717));
#6496=EDGE_LOOP('',(#2718,#2719,#2720,#2721,#2722));
#6497=EDGE_LOOP('',(#2723,#2724,#2725,#2726,#2727));
#6498=EDGE_LOOP('',(#2728,#2729));
#6499=EDGE_LOOP('',(#2730));
#6500=EDGE_LOOP('',(#2731));
#6501=EDGE_LOOP('',(#2732));
#6502=EDGE_LOOP('',(#2733,#2734,#2735,#2736,#2737,#2738,#2739,#2740));
#6503=EDGE_LOOP('',(#2741,#2742,#2743,#2744,#2745,#2746,#2747,#2748));
#6504=EDGE_LOOP('',(#2749,#2750,#2751,#2752,#2753,#2754,#2755,#2756));
#6505=EDGE_LOOP('',(#2757,#2758,#2759,#2760,#2761,#2762,#2763,#2764));
#6506=EDGE_LOOP('',(#2765,#2766,#2767,#2768,#2769,#2770,#2771,#2772));
#6507=EDGE_LOOP('',(#2773,#2774,#2775,#2776,#2777,#2778,#2779,#2780));
#6508=EDGE_LOOP('',(#2781));
#6509=EDGE_LOOP('',(#2782));
#6510=EDGE_LOOP('',(#2783));
#6511=EDGE_LOOP('',(#2784));
#6512=EDGE_LOOP('',(#2785));
#6513=EDGE_LOOP('',(#2786));
#6514=EDGE_LOOP('',(#2787));
#6515=EDGE_LOOP('',(#2788));
#6516=EDGE_LOOP('',(#2789));
#6517=EDGE_LOOP('',(#2790));
#6518=EDGE_LOOP('',(#2791));
#6519=EDGE_LOOP('',(#2792));
#6520=EDGE_LOOP('',(#2793));
#6521=EDGE_LOOP('',(#2794));
#6522=EDGE_LOOP('',(#2795));
#6523=EDGE_LOOP('',(#2796));
#6524=EDGE_LOOP('',(#2797));
#6525=EDGE_LOOP('',(#2798));
#6526=EDGE_LOOP('',(#2799,#2800,#2801,#2802));
#6527=EDGE_LOOP('',(#2803));
#6528=EDGE_LOOP('',(#2804));
#6529=EDGE_LOOP('',(#2805));
#6530=EDGE_LOOP('',(#2806));
#6531=EDGE_LOOP('',(#2807));
#6532=EDGE_LOOP('',(#2808));
#6533=EDGE_LOOP('',(#2809));
#6534=EDGE_LOOP('',(#2810));
#6535=EDGE_LOOP('',(#2811));
#6536=EDGE_LOOP('',(#2812));
#6537=EDGE_LOOP('',(#2813));
#6538=EDGE_LOOP('',(#2814));
#6539=EDGE_LOOP('',(#2815));
#6540=EDGE_LOOP('',(#2816));
#6541=EDGE_LOOP('',(#2817));
#6542=EDGE_LOOP('',(#2818));
#6543=EDGE_LOOP('',(#2819));
#6544=EDGE_LOOP('',(#2820));
#6545=EDGE_LOOP('',(#2821));
#6546=EDGE_LOOP('',(#2822));
#6547=EDGE_LOOP('',(#2823));
#6548=EDGE_LOOP('',(#2824));
#6549=EDGE_LOOP('',(#2825));
#6550=EDGE_LOOP('',(#2826));
#6551=EDGE_LOOP('',(#2827));
#6552=EDGE_LOOP('',(#2828));
#6553=EDGE_LOOP('',(#2829));
#6554=EDGE_LOOP('',(#2830));
#6555=EDGE_LOOP('',(#2831));
#6556=EDGE_LOOP('',(#2832));
#6557=EDGE_LOOP('',(#2833));
#6558=EDGE_LOOP('',(#2834));
#6559=EDGE_LOOP('',(#2835));
#6560=EDGE_LOOP('',(#2836));
#6561=EDGE_LOOP('',(#2837));
#6562=EDGE_LOOP('',(#2838));
#6563=EDGE_LOOP('',(#2839,#2840,#2841,#2842));
#6564=EDGE_LOOP('',(#2843,#2844,#2845,#2846));
#6565=EDGE_LOOP('',(#2847,#2848,#2849,#2850));
#6566=EDGE_LOOP('',(#2851,#2852,#2853,#2854));
#6567=EDGE_LOOP('',(#2855,#2856,#2857,#2858));
#6568=EDGE_LOOP('',(#2859,#2860,#2861,#2862));
#6569=EDGE_LOOP('',(#2863,#2864,#2865,#2866));
#6570=EDGE_LOOP('',(#2867,#2868,#2869,#2870));
#6571=EDGE_LOOP('',(#2871,#2872,#2873,#2874));
#6572=EDGE_LOOP('',(#2875,#2876,#2877,#2878));
#6573=EDGE_LOOP('',(#2879,#2880,#2881,#2882));
#6574=EDGE_LOOP('',(#2883,#2884,#2885,#2886));
#6575=EDGE_LOOP('',(#2887,#2888,#2889,#2890));
#6576=EDGE_LOOP('',(#2891,#2892,#2893,#2894));
#6577=EDGE_LOOP('',(#2895,#2896,#2897,#2898));
#6578=EDGE_LOOP('',(#2899,#2900,#2901,#2902));
#6579=EDGE_LOOP('',(#2903,#2904,#2905,#2906));
#6580=EDGE_LOOP('',(#2907,#2908,#2909,#2910));
#6581=EDGE_LOOP('',(#2911,#2912,#2913,#2914));
#6582=EDGE_LOOP('',(#2915,#2916,#2917,#2918));
#6583=EDGE_LOOP('',(#2919,#2920,#2921,#2922));
#6584=EDGE_LOOP('',(#2923,#2924,#2925,#2926));
#6585=EDGE_LOOP('',(#2927,#2928,#2929,#2930));
#6586=EDGE_LOOP('',(#2931,#2932,#2933,#2934));
#6587=EDGE_LOOP('',(#2935,#2936,#2937,#2938));
#6588=EDGE_LOOP('',(#2939,#2940,#2941,#2942));
#6589=EDGE_LOOP('',(#2943,#2944,#2945,#2946));
#6590=EDGE_LOOP('',(#2947,#2948,#2949,#2950));
#6591=EDGE_LOOP('',(#2951,#2952,#2953,#2954));
#6592=EDGE_LOOP('',(#2955,#2956));
#6593=EDGE_LOOP('',(#2957));
#6594=EDGE_LOOP('',(#2958,#2959));
#6595=EDGE_LOOP('',(#2960,#2961));
#6596=EDGE_LOOP('',(#2962,#2963));
#6597=EDGE_LOOP('',(#2964));
#6598=EDGE_LOOP('',(#2965,#2966));
#6599=EDGE_LOOP('',(#2967));
#6600=EDGE_LOOP('',(#2968,#2969));
#6601=EDGE_LOOP('',(#2970,#2971));
#6602=EDGE_LOOP('',(#2972));
#6603=EDGE_LOOP('',(#2973,#2974));
#6604=EDGE_LOOP('',(#2975,#2976));
#6605=EDGE_LOOP('',(#2977,#2978));
#6606=EDGE_LOOP('',(#2979,#2980,#2981,#2982,#2983,#2984,#2985,#2986,#2987,
#2988,#2989,#2990,#2991,#2992,#2993,#2994,#2995,#2996,#2997,#2998,#2999,
#3000,#3001,#3002));
#6607=EDGE_LOOP('',(#3003));
#6608=EDGE_LOOP('',(#3004,#3005));
#6609=EDGE_LOOP('',(#3006));
#6610=EDGE_LOOP('',(#3007));
#6611=EDGE_LOOP('',(#3008,#3009));
#6612=EDGE_LOOP('',(#3010));
#6613=EDGE_LOOP('',(#3011));
#6614=EDGE_LOOP('',(#3012,#3013,#3014,#3015,#3016,#3017,#3018,#3019,#3020,
#3021,#3022,#3023,#3024,#3025,#3026,#3027));
#6615=EDGE_LOOP('',(#3028,#3029,#3030,#3031,#3032,#3033,#3034,#3035,#3036,
#3037,#3038,#3039,#3040,#3041,#3042,#3043));
#6616=EDGE_LOOP('',(#3044));
#6617=EDGE_LOOP('',(#3045,#3046));
#6618=EDGE_LOOP('',(#3047,#3048,#3049,#3050));
#6619=EDGE_LOOP('',(#3051,#3052,#3053,#3054));
#6620=EDGE_LOOP('',(#3055,#3056,#3057));
#6621=EDGE_LOOP('',(#3058));
#6622=EDGE_LOOP('',(#3059,#3060,#3061));
#6623=EDGE_LOOP('',(#3062));
#6624=EDGE_LOOP('',(#3063,#3064,#3065,#3066));
#6625=EDGE_LOOP('',(#3067,#3068,#3069,#3070));
#6626=EDGE_LOOP('',(#3071,#3072));
#6627=EDGE_LOOP('',(#3073));
#6628=EDGE_LOOP('',(#3074,#3075,#3076,#3077,#3078,#3079));
#6629=EDGE_LOOP('',(#3080,#3081,#3082,#3083,#3084,#3085));
#6630=EDGE_LOOP('',(#3086,#3087,#3088,#3089,#3090,#3091));
#6631=EDGE_LOOP('',(#3092,#3093,#3094,#3095,#3096));
#6632=EDGE_LOOP('',(#3097,#3098,#3099,#3100,#3101,#3102));
#6633=EDGE_LOOP('',(#3103,#3104,#3105,#3106,#3107,#3108));
#6634=EDGE_LOOP('',(#3109,#3110,#3111,#3112,#3113,#3114));
#6635=EDGE_LOOP('',(#3115,#3116,#3117,#3118,#3119));
#6636=EDGE_LOOP('',(#3120,#3121,#3122,#3123));
#6637=EDGE_LOOP('',(#3124,#3125,#3126,#3127,#3128));
#6638=EDGE_LOOP('',(#3129,#3130,#3131,#3132,#3133,#3134));
#6639=EDGE_LOOP('',(#3135,#3136,#3137,#3138));
#6640=EDGE_LOOP('',(#3139,#3140,#3141,#3142,#3143,#3144));
#6641=EDGE_LOOP('',(#3145,#3146,#3147,#3148,#3149,#3150));
#6642=EDGE_LOOP('',(#3151,#3152,#3153,#3154,#3155,#3156));
#6643=EDGE_LOOP('',(#3157,#3158,#3159,#3160,#3161));
#6644=EDGE_LOOP('',(#3162,#3163,#3164,#3165,#3166,#3167));
#6645=EDGE_LOOP('',(#3168,#3169,#3170,#3171,#3172,#3173));
#6646=EDGE_LOOP('',(#3174,#3175,#3176,#3177,#3178,#3179));
#6647=EDGE_LOOP('',(#3180,#3181,#3182,#3183));
#6648=EDGE_LOOP('',(#3184,#3185,#3186,#3187,#3188,#3189));
#6649=EDGE_LOOP('',(#3190,#3191,#3192,#3193,#3194,#3195));
#6650=EDGE_LOOP('',(#3196,#3197,#3198,#3199,#3200,#3201));
#6651=EDGE_LOOP('',(#3202,#3203,#3204,#3205));
#6652=EDGE_LOOP('',(#3206,#3207,#3208,#3209,#3210,#3211));
#6653=EDGE_LOOP('',(#3212,#3213));
#6654=EDGE_LOOP('',(#3214,#3215,#3216,#3217,#3218,#3219));
#6655=EDGE_LOOP('',(#3220,#3221));
#6656=EDGE_LOOP('',(#3222,#3223,#3224,#3225,#3226));
#6657=EDGE_LOOP('',(#3227,#3228,#3229,#3230,#3231,#3232));
#6658=EDGE_LOOP('',(#3233,#3234));
#6659=EDGE_LOOP('',(#3235,#3236,#3237,#3238,#3239,#3240));
#6660=EDGE_LOOP('',(#3241,#3242));
#6661=EDGE_LOOP('',(#3243,#3244,#3245,#3246,#3247,#3248));
#6662=EDGE_LOOP('',(#3249,#3250));
#6663=EDGE_LOOP('',(#3251,#3252,#3253,#3254,#3255,#3256));
#6664=EDGE_LOOP('',(#3257,#3258));
#6665=EDGE_LOOP('',(#3259,#3260,#3261,#3262));
#6666=EDGE_LOOP('',(#3263,#3264));
#6667=EDGE_LOOP('',(#3265,#3266,#3267,#3268));
#6668=EDGE_LOOP('',(#3269,#3270));
#6669=EDGE_LOOP('',(#3271,#3272,#3273));
#6670=EDGE_LOOP('',(#3274,#3275,#3276,#3277));
#6671=EDGE_LOOP('',(#3278,#3279,#3280));
#6672=EDGE_LOOP('',(#3281,#3282,#3283,#3284));
#6673=EDGE_LOOP('',(#3285,#3286));
#6674=EDGE_LOOP('',(#3287,#3288,#3289,#3290));
#6675=EDGE_LOOP('',(#3291,#3292,#3293,#3294));
#6676=EDGE_LOOP('',(#3295,#3296));
#6677=EDGE_LOOP('',(#3297,#3298,#3299,#3300,#3301));
#6678=EDGE_LOOP('',(#3302,#3303,#3304,#3305,#3306));
#6679=EDGE_LOOP('',(#3307,#3308,#3309,#3310));
#6680=EDGE_LOOP('',(#3311,#3312,#3313,#3314,#3315));
#6681=EDGE_LOOP('',(#3316,#3317,#3318,#3319,#3320));
#6682=EDGE_LOOP('',(#3321,#3322,#3323,#3324));
#6683=EDGE_LOOP('',(#3325,#3326,#3327));
#6684=EDGE_LOOP('',(#3328,#3329,#3330,#3331,#3332));
#6685=EDGE_LOOP('',(#3333,#3334,#3335,#3336));
#6686=EDGE_LOOP('',(#3337,#3338,#3339,#3340,#3341));
#6687=EDGE_LOOP('',(#3342,#3343,#3344,#3345,#3346));
#6688=EDGE_LOOP('',(#3347,#3348,#3349,#3350));
#6689=EDGE_LOOP('',(#3351,#3352,#3353,#3354,#3355));
#6690=EDGE_LOOP('',(#3356,#3357,#3358,#3359,#3360));
#6691=EDGE_LOOP('',(#3361,#3362,#3363,#3364));
#6692=EDGE_LOOP('',(#3365,#3366,#3367,#3368,#3369));
#6693=EDGE_LOOP('',(#3370,#3371,#3372,#3373,#3374));
#6694=EDGE_LOOP('',(#3375,#3376,#3377,#3378));
#6695=EDGE_LOOP('',(#3379,#3380,#3381,#3382,#3383));
#6696=EDGE_LOOP('',(#3384,#3385,#3386,#3387,#3388));
#6697=EDGE_LOOP('',(#3389,#3390,#3391,#3392));
#6698=EDGE_LOOP('',(#3393,#3394,#3395,#3396,#3397));
#6699=EDGE_LOOP('',(#3398,#3399,#3400,#3401,#3402));
#6700=EDGE_LOOP('',(#3403,#3404,#3405,#3406));
#6701=EDGE_LOOP('',(#3407,#3408,#3409,#3410,#3411));
#6702=EDGE_LOOP('',(#3412,#3413,#3414,#3415,#3416));
#6703=EDGE_LOOP('',(#3417,#3418,#3419,#3420,#3421));
#6704=EDGE_LOOP('',(#3422,#3423,#3424,#3425));
#6705=EDGE_LOOP('',(#3426,#3427,#3428,#3429,#3430));
#6706=EDGE_LOOP('',(#3431,#3432,#3433,#3434,#3435));
#6707=EDGE_LOOP('',(#3436,#3437,#3438,#3439));
#6708=EDGE_LOOP('',(#3440,#3441,#3442,#3443,#3444));
#6709=EDGE_LOOP('',(#3445,#3446,#3447,#3448,#3449));
#6710=EDGE_LOOP('',(#3450,#3451,#3452,#3453));
#6711=EDGE_LOOP('',(#3454,#3455,#3456,#3457,#3458));
#6712=EDGE_LOOP('',(#3459,#3460,#3461,#3462,#3463));
#6713=EDGE_LOOP('',(#3464,#3465,#3466,#3467));
#7024=FACE_BOUND('',#6263,.T.);
#7025=FACE_BOUND('',#6264,.T.);
#7026=FACE_BOUND('',#6265,.T.);
#7027=FACE_BOUND('',#6266,.T.);
#7028=FACE_BOUND('',#6267,.T.);
#7029=FACE_BOUND('',#6268,.T.);
#7030=FACE_BOUND('',#6269,.T.);
#7031=FACE_BOUND('',#6270,.T.);
#7032=FACE_BOUND('',#6271,.T.);
#7033=FACE_BOUND('',#6272,.T.);
#7034=FACE_BOUND('',#6273,.T.);
#7035=FACE_BOUND('',#6274,.T.);
#7036=FACE_BOUND('',#6275,.T.);
#7037=FACE_BOUND('',#6276,.T.);
#7038=FACE_BOUND('',#6277,.T.);
#7039=FACE_BOUND('',#6278,.T.);
#7040=FACE_BOUND('',#6279,.T.);
#7041=FACE_BOUND('',#6280,.T.);
#7042=FACE_BOUND('',#6281,.T.);
#7043=FACE_BOUND('',#6282,.T.);
#7044=FACE_BOUND('',#6283,.T.);
#7045=FACE_BOUND('',#6284,.T.);
#7046=FACE_BOUND('',#6285,.T.);
#7047=FACE_BOUND('',#6286,.T.);
#7048=FACE_BOUND('',#6287,.T.);
#7049=FACE_BOUND('',#6288,.T.);
#7050=FACE_BOUND('',#6289,.T.);
#7051=FACE_BOUND('',#6290,.T.);
#7052=FACE_BOUND('',#6291,.T.);
#7053=FACE_BOUND('',#6292,.T.);
#7054=FACE_BOUND('',#6293,.T.);
#7055=FACE_BOUND('',#6294,.T.);
#7056=FACE_BOUND('',#6295,.T.);
#7057=FACE_BOUND('',#6296,.T.);
#7058=FACE_BOUND('',#6297,.T.);
#7059=FACE_BOUND('',#6298,.T.);
#7060=FACE_BOUND('',#6299,.T.);
#7061=FACE_BOUND('',#6300,.T.);
#7062=FACE_BOUND('',#6301,.T.);
#7063=FACE_BOUND('',#6302,.T.);
#7064=FACE_BOUND('',#6303,.T.);
#7065=FACE_BOUND('',#6304,.T.);
#7066=FACE_BOUND('',#6305,.T.);
#7067=FACE_BOUND('',#6306,.T.);
#7068=FACE_BOUND('',#6307,.T.);
#7069=FACE_BOUND('',#6308,.T.);
#7070=FACE_BOUND('',#6309,.T.);
#7071=FACE_BOUND('',#6310,.T.);
#7072=FACE_BOUND('',#6311,.T.);
#7073=FACE_BOUND('',#6312,.T.);
#7074=FACE_BOUND('',#6313,.T.);
#7075=FACE_BOUND('',#6314,.T.);
#7076=FACE_BOUND('',#6315,.T.);
#7077=FACE_BOUND('',#6316,.T.);
#7078=FACE_BOUND('',#6317,.T.);
#7079=FACE_BOUND('',#6318,.T.);
#7080=FACE_BOUND('',#6319,.T.);
#7081=FACE_BOUND('',#6320,.T.);
#7082=FACE_BOUND('',#6321,.T.);
#7083=FACE_BOUND('',#6322,.T.);
#7084=FACE_BOUND('',#6323,.T.);
#7085=FACE_BOUND('',#6324,.T.);
#7086=FACE_BOUND('',#6325,.T.);
#7087=FACE_BOUND('',#6326,.T.);
#7088=FACE_BOUND('',#6327,.T.);
#7089=FACE_BOUND('',#6328,.T.);
#7090=FACE_BOUND('',#6329,.T.);
#7091=FACE_BOUND('',#6330,.T.);
#7092=FACE_BOUND('',#6331,.T.);
#7093=FACE_BOUND('',#6332,.T.);
#7094=FACE_BOUND('',#6333,.T.);
#7095=FACE_BOUND('',#6334,.T.);
#7096=FACE_BOUND('',#6335,.T.);
#7097=FACE_BOUND('',#6336,.T.);
#7098=FACE_BOUND('',#6337,.T.);
#7099=FACE_BOUND('',#6338,.T.);
#7100=FACE_BOUND('',#6339,.T.);
#7101=FACE_BOUND('',#6340,.T.);
#7102=FACE_BOUND('',#6341,.T.);
#7103=FACE_BOUND('',#6342,.T.);
#7104=FACE_BOUND('',#6343,.T.);
#7105=FACE_BOUND('',#6344,.T.);
#7106=FACE_BOUND('',#6345,.T.);
#7107=FACE_BOUND('',#6346,.T.);
#7108=FACE_BOUND('',#6347,.T.);
#7109=FACE_BOUND('',#6348,.T.);
#7110=FACE_BOUND('',#6349,.T.);
#7111=FACE_BOUND('',#6350,.T.);
#7112=FACE_BOUND('',#6351,.T.);
#7113=FACE_BOUND('',#6352,.T.);
#7114=FACE_BOUND('',#6353,.T.);
#7115=FACE_BOUND('',#6354,.T.);
#7116=FACE_BOUND('',#6355,.T.);
#7117=FACE_BOUND('',#6356,.T.);
#7118=FACE_BOUND('',#6357,.T.);
#7119=FACE_BOUND('',#6358,.T.);
#7120=FACE_BOUND('',#6359,.T.);
#7121=FACE_BOUND('',#6360,.T.);
#7122=FACE_BOUND('',#6361,.T.);
#7123=FACE_BOUND('',#6362,.T.);
#7124=FACE_BOUND('',#6363,.T.);
#7125=FACE_BOUND('',#6364,.T.);
#7126=FACE_BOUND('',#6365,.T.);
#7127=FACE_BOUND('',#6366,.T.);
#7128=FACE_BOUND('',#6367,.T.);
#7129=FACE_BOUND('',#6368,.T.);
#7130=FACE_BOUND('',#6369,.T.);
#7131=FACE_BOUND('',#6370,.T.);
#7132=FACE_BOUND('',#6371,.T.);
#7133=FACE_BOUND('',#6372,.T.);
#7134=FACE_BOUND('',#6373,.T.);
#7135=FACE_BOUND('',#6374,.T.);
#7136=FACE_BOUND('',#6375,.T.);
#7137=FACE_BOUND('',#6376,.T.);
#7138=FACE_BOUND('',#6377,.T.);
#7139=FACE_BOUND('',#6378,.T.);
#7140=FACE_BOUND('',#6379,.T.);
#7141=FACE_BOUND('',#6380,.T.);
#7142=FACE_BOUND('',#6381,.T.);
#7143=FACE_BOUND('',#6382,.T.);
#7144=FACE_BOUND('',#6383,.T.);
#7145=FACE_BOUND('',#6384,.T.);
#7146=FACE_BOUND('',#6385,.T.);
#7147=FACE_BOUND('',#6386,.T.);
#7148=FACE_BOUND('',#6387,.T.);
#7149=FACE_BOUND('',#6388,.T.);
#7150=FACE_BOUND('',#6389,.T.);
#7151=FACE_BOUND('',#6390,.T.);
#7152=FACE_BOUND('',#6391,.T.);
#7153=FACE_BOUND('',#6392,.T.);
#7154=FACE_BOUND('',#6393,.T.);
#7155=FACE_BOUND('',#6394,.T.);
#7156=FACE_BOUND('',#6395,.T.);
#7157=FACE_BOUND('',#6396,.T.);
#7158=FACE_BOUND('',#6397,.T.);
#7159=FACE_BOUND('',#6398,.T.);
#7160=FACE_BOUND('',#6399,.T.);
#7161=FACE_BOUND('',#6400,.T.);
#7162=FACE_BOUND('',#6401,.T.);
#7163=FACE_BOUND('',#6402,.T.);
#7164=FACE_BOUND('',#6403,.T.);
#7165=FACE_BOUND('',#6404,.T.);
#7166=FACE_BOUND('',#6405,.T.);
#7167=FACE_BOUND('',#6406,.T.);
#7168=FACE_BOUND('',#6407,.T.);
#7169=FACE_BOUND('',#6408,.T.);
#7170=FACE_BOUND('',#6409,.T.);
#7171=FACE_BOUND('',#6410,.T.);
#7172=FACE_BOUND('',#6411,.T.);
#7173=FACE_BOUND('',#6412,.T.);
#7174=FACE_BOUND('',#6413,.T.);
#7175=FACE_BOUND('',#6414,.T.);
#7176=FACE_BOUND('',#6415,.T.);
#7177=FACE_BOUND('',#6416,.T.);
#7178=FACE_BOUND('',#6417,.T.);
#7179=FACE_BOUND('',#6418,.T.);
#7180=FACE_BOUND('',#6419,.T.);
#7181=FACE_BOUND('',#6420,.T.);
#7182=FACE_BOUND('',#6421,.T.);
#7183=FACE_BOUND('',#6422,.T.);
#7184=FACE_BOUND('',#6423,.T.);
#7185=FACE_BOUND('',#6424,.T.);
#7186=FACE_BOUND('',#6425,.T.);
#7187=FACE_BOUND('',#6426,.T.);
#7188=FACE_BOUND('',#6427,.T.);
#7189=FACE_BOUND('',#6428,.T.);
#7190=FACE_BOUND('',#6429,.T.);
#7191=FACE_BOUND('',#6430,.T.);
#7192=FACE_BOUND('',#6431,.T.);
#7193=FACE_BOUND('',#6432,.T.);
#7194=FACE_BOUND('',#6433,.T.);
#7195=FACE_BOUND('',#6434,.T.);
#7196=FACE_BOUND('',#6435,.T.);
#7197=FACE_BOUND('',#6436,.T.);
#7198=FACE_BOUND('',#6437,.T.);
#7199=FACE_BOUND('',#6438,.T.);
#7200=FACE_BOUND('',#6439,.T.);
#7201=FACE_BOUND('',#6440,.T.);
#7202=FACE_BOUND('',#6441,.T.);
#7203=FACE_BOUND('',#6442,.T.);
#7204=FACE_BOUND('',#6443,.T.);
#7205=FACE_BOUND('',#6444,.T.);
#7206=FACE_BOUND('',#6445,.T.);
#7207=FACE_BOUND('',#6446,.T.);
#7208=FACE_BOUND('',#6447,.T.);
#7209=FACE_BOUND('',#6448,.T.);
#7210=FACE_BOUND('',#6449,.T.);
#7211=FACE_BOUND('',#6450,.T.);
#7212=FACE_BOUND('',#6451,.T.);
#7213=FACE_BOUND('',#6452,.T.);
#7214=FACE_BOUND('',#6453,.T.);
#7215=FACE_BOUND('',#6454,.T.);
#7216=FACE_BOUND('',#6455,.T.);
#7217=FACE_BOUND('',#6456,.T.);
#7218=FACE_BOUND('',#6457,.T.);
#7219=FACE_BOUND('',#6458,.T.);
#7220=FACE_BOUND('',#6459,.T.);
#7221=FACE_BOUND('',#6460,.T.);
#7222=FACE_BOUND('',#6461,.T.);
#7223=FACE_BOUND('',#6462,.T.);
#7224=FACE_BOUND('',#6463,.T.);
#7225=FACE_BOUND('',#6464,.T.);
#7226=FACE_BOUND('',#6465,.T.);
#7227=FACE_BOUND('',#6466,.T.);
#7228=FACE_BOUND('',#6467,.T.);
#7229=FACE_BOUND('',#6468,.T.);
#7230=FACE_BOUND('',#6469,.T.);
#7231=FACE_BOUND('',#6470,.T.);
#7232=FACE_BOUND('',#6471,.T.);
#7233=FACE_BOUND('',#6472,.T.);
#7234=FACE_BOUND('',#6473,.T.);
#7235=FACE_BOUND('',#6474,.T.);
#7236=FACE_BOUND('',#6475,.T.);
#7237=FACE_BOUND('',#6476,.T.);
#7238=FACE_BOUND('',#6477,.T.);
#7239=FACE_BOUND('',#6478,.T.);
#7240=FACE_BOUND('',#6479,.T.);
#7241=FACE_BOUND('',#6480,.T.);
#7242=FACE_BOUND('',#6481,.T.);
#7243=FACE_BOUND('',#6482,.T.);
#7244=FACE_BOUND('',#6483,.T.);
#7245=FACE_BOUND('',#6484,.T.);
#7246=FACE_BOUND('',#6485,.T.);
#7247=FACE_BOUND('',#6486,.T.);
#7248=FACE_BOUND('',#6487,.T.);
#7249=FACE_BOUND('',#6488,.T.);
#7250=FACE_BOUND('',#6489,.T.);
#7251=FACE_BOUND('',#6490,.T.);
#7252=FACE_BOUND('',#6491,.T.);
#7253=FACE_BOUND('',#6492,.T.);
#7254=FACE_BOUND('',#6493,.T.);
#7255=FACE_BOUND('',#6494,.T.);
#7256=FACE_BOUND('',#6495,.T.);
#7257=FACE_BOUND('',#6496,.T.);
#7258=FACE_BOUND('',#6497,.T.);
#7259=FACE_BOUND('',#6498,.T.);
#7260=FACE_BOUND('',#6499,.T.);
#7261=FACE_BOUND('',#6500,.T.);
#7262=FACE_BOUND('',#6501,.T.);
#7263=FACE_BOUND('',#6502,.T.);
#7264=FACE_BOUND('',#6503,.T.);
#7265=FACE_BOUND('',#6504,.T.);
#7266=FACE_BOUND('',#6505,.T.);
#7267=FACE_BOUND('',#6506,.T.);
#7268=FACE_BOUND('',#6507,.T.);
#7269=FACE_BOUND('',#6508,.T.);
#7270=FACE_BOUND('',#6509,.T.);
#7271=FACE_BOUND('',#6510,.T.);
#7272=FACE_BOUND('',#6511,.T.);
#7273=FACE_BOUND('',#6512,.T.);
#7274=FACE_BOUND('',#6513,.T.);
#7275=FACE_BOUND('',#6514,.T.);
#7276=FACE_BOUND('',#6515,.T.);
#7277=FACE_BOUND('',#6516,.T.);
#7278=FACE_BOUND('',#6517,.T.);
#7279=FACE_BOUND('',#6518,.T.);
#7280=FACE_BOUND('',#6519,.T.);
#7281=FACE_BOUND('',#6520,.T.);
#7282=FACE_BOUND('',#6521,.T.);
#7283=FACE_BOUND('',#6522,.T.);
#7284=FACE_BOUND('',#6523,.T.);
#7285=FACE_BOUND('',#6524,.T.);
#7286=FACE_BOUND('',#6525,.T.);
#7287=FACE_BOUND('',#6526,.T.);
#7288=FACE_BOUND('',#6527,.T.);
#7289=FACE_BOUND('',#6528,.T.);
#7290=FACE_BOUND('',#6529,.T.);
#7291=FACE_BOUND('',#6530,.T.);
#7292=FACE_BOUND('',#6531,.T.);
#7293=FACE_BOUND('',#6532,.T.);
#7294=FACE_BOUND('',#6533,.T.);
#7295=FACE_BOUND('',#6534,.T.);
#7296=FACE_BOUND('',#6535,.T.);
#7297=FACE_BOUND('',#6536,.T.);
#7298=FACE_BOUND('',#6537,.T.);
#7299=FACE_BOUND('',#6538,.T.);
#7300=FACE_BOUND('',#6539,.T.);
#7301=FACE_BOUND('',#6540,.T.);
#7302=FACE_BOUND('',#6541,.T.);
#7303=FACE_BOUND('',#6542,.T.);
#7304=FACE_BOUND('',#6543,.T.);
#7305=FACE_BOUND('',#6544,.T.);
#7306=FACE_BOUND('',#6545,.T.);
#7307=FACE_BOUND('',#6546,.T.);
#7308=FACE_BOUND('',#6547,.T.);
#7309=FACE_BOUND('',#6548,.T.);
#7310=FACE_BOUND('',#6549,.T.);
#7311=FACE_BOUND('',#6550,.T.);
#7312=FACE_BOUND('',#6551,.T.);
#7313=FACE_BOUND('',#6552,.T.);
#7314=FACE_BOUND('',#6553,.T.);
#7315=FACE_BOUND('',#6554,.T.);
#7316=FACE_BOUND('',#6555,.T.);
#7317=FACE_BOUND('',#6556,.T.);
#7318=FACE_BOUND('',#6557,.T.);
#7319=FACE_BOUND('',#6558,.T.);
#7320=FACE_BOUND('',#6559,.T.);
#7321=FACE_BOUND('',#6560,.T.);
#7322=FACE_BOUND('',#6561,.T.);
#7323=FACE_BOUND('',#6562,.T.);
#7324=FACE_BOUND('',#6563,.T.);
#7325=FACE_BOUND('',#6564,.T.);
#7326=FACE_BOUND('',#6565,.T.);
#7327=FACE_BOUND('',#6566,.T.);
#7328=FACE_BOUND('',#6567,.T.);
#7329=FACE_BOUND('',#6568,.T.);
#7330=FACE_BOUND('',#6569,.T.);
#7331=FACE_BOUND('',#6570,.T.);
#7332=FACE_BOUND('',#6571,.T.);
#7333=FACE_BOUND('',#6572,.T.);
#7334=FACE_BOUND('',#6573,.T.);
#7335=FACE_BOUND('',#6574,.T.);
#7336=FACE_BOUND('',#6575,.T.);
#7337=FACE_BOUND('',#6576,.T.);
#7338=FACE_BOUND('',#6577,.T.);
#7339=FACE_BOUND('',#6578,.T.);
#7340=FACE_BOUND('',#6579,.T.);
#7341=FACE_BOUND('',#6580,.T.);
#7342=FACE_BOUND('',#6581,.T.);
#7343=FACE_BOUND('',#6582,.T.);
#7344=FACE_BOUND('',#6583,.T.);
#7345=FACE_BOUND('',#6584,.T.);
#7346=FACE_BOUND('',#6585,.T.);
#7347=FACE_BOUND('',#6586,.T.);
#7348=FACE_BOUND('',#6587,.T.);
#7349=FACE_BOUND('',#6588,.T.);
#7350=FACE_BOUND('',#6589,.T.);
#7351=FACE_BOUND('',#6590,.T.);
#7352=FACE_BOUND('',#6591,.T.);
#7353=FACE_BOUND('',#6592,.T.);
#7354=FACE_BOUND('',#6593,.T.);
#7355=FACE_BOUND('',#6594,.T.);
#7356=FACE_BOUND('',#6595,.T.);
#7357=FACE_BOUND('',#6596,.T.);
#7358=FACE_BOUND('',#6597,.T.);
#7359=FACE_BOUND('',#6598,.T.);
#7360=FACE_BOUND('',#6599,.T.);
#7361=FACE_BOUND('',#6600,.T.);
#7362=FACE_BOUND('',#6601,.T.);
#7363=FACE_BOUND('',#6602,.T.);
#7364=FACE_BOUND('',#6603,.T.);
#7365=FACE_BOUND('',#6604,.T.);
#7366=FACE_BOUND('',#6605,.T.);
#7367=FACE_BOUND('',#6606,.T.);
#7368=FACE_BOUND('',#6607,.T.);
#7369=FACE_BOUND('',#6608,.T.);
#7370=FACE_BOUND('',#6609,.T.);
#7371=FACE_BOUND('',#6610,.T.);
#7372=FACE_BOUND('',#6611,.T.);
#7373=FACE_BOUND('',#6612,.T.);
#7374=FACE_BOUND('',#6613,.T.);
#7375=FACE_BOUND('',#6614,.T.);
#7376=FACE_BOUND('',#6615,.T.);
#7377=FACE_BOUND('',#6616,.T.);
#7378=FACE_BOUND('',#6617,.T.);
#7379=FACE_BOUND('',#6618,.T.);
#7380=FACE_BOUND('',#6619,.T.);
#7381=FACE_BOUND('',#6620,.T.);
#7382=FACE_BOUND('',#6621,.T.);
#7383=FACE_BOUND('',#6622,.T.);
#7384=FACE_BOUND('',#6623,.T.);
#7385=FACE_BOUND('',#6624,.T.);
#7386=FACE_BOUND('',#6625,.T.);
#7387=FACE_BOUND('',#6626,.T.);
#7388=FACE_BOUND('',#6627,.T.);
#7389=FACE_BOUND('',#6628,.T.);
#7390=FACE_BOUND('',#6629,.T.);
#7391=FACE_BOUND('',#6630,.T.);
#7392=FACE_BOUND('',#6631,.T.);
#7393=FACE_BOUND('',#6632,.T.);
#7394=FACE_BOUND('',#6633,.T.);
#7395=FACE_BOUND('',#6634,.T.);
#7396=FACE_BOUND('',#6635,.T.);
#7397=FACE_BOUND('',#6636,.T.);
#7398=FACE_BOUND('',#6637,.T.);
#7399=FACE_BOUND('',#6638,.T.);
#7400=FACE_BOUND('',#6639,.T.);
#7401=FACE_BOUND('',#6640,.T.);
#7402=FACE_BOUND('',#6641,.T.);
#7403=FACE_BOUND('',#6642,.T.);
#7404=FACE_BOUND('',#6643,.T.);
#7405=FACE_BOUND('',#6644,.T.);
#7406=FACE_BOUND('',#6645,.T.);
#7407=FACE_BOUND('',#6646,.T.);
#7408=FACE_BOUND('',#6647,.T.);
#7409=FACE_BOUND('',#6648,.T.);
#7410=FACE_BOUND('',#6649,.T.);
#7411=FACE_BOUND('',#6650,.T.);
#7412=FACE_BOUND('',#6651,.T.);
#7413=FACE_BOUND('',#6652,.T.);
#7414=FACE_BOUND('',#6653,.T.);
#7415=FACE_BOUND('',#6654,.T.);
#7416=FACE_BOUND('',#6655,.T.);
#7417=FACE_BOUND('',#6656,.T.);
#7418=FACE_BOUND('',#6657,.T.);
#7419=FACE_BOUND('',#6658,.T.);
#7420=FACE_BOUND('',#6659,.T.);
#7421=FACE_BOUND('',#6660,.T.);
#7422=FACE_BOUND('',#6661,.T.);
#7423=FACE_BOUND('',#6662,.T.);
#7424=FACE_BOUND('',#6663,.T.);
#7425=FACE_BOUND('',#6664,.T.);
#7426=FACE_BOUND('',#6665,.T.);
#7427=FACE_BOUND('',#6666,.T.);
#7428=FACE_BOUND('',#6667,.T.);
#7429=FACE_BOUND('',#6668,.T.);
#7430=FACE_BOUND('',#6669,.T.);
#7431=FACE_BOUND('',#6670,.T.);
#7432=FACE_BOUND('',#6671,.T.);
#7433=FACE_BOUND('',#6672,.T.);
#7434=FACE_BOUND('',#6673,.T.);
#7435=FACE_BOUND('',#6674,.T.);
#7436=FACE_BOUND('',#6675,.T.);
#7437=FACE_BOUND('',#6676,.T.);
#7438=FACE_BOUND('',#6677,.T.);
#7439=FACE_BOUND('',#6678,.T.);
#7440=FACE_BOUND('',#6679,.T.);
#7441=FACE_BOUND('',#6680,.T.);
#7442=FACE_BOUND('',#6681,.T.);
#7443=FACE_BOUND('',#6682,.T.);
#7444=FACE_BOUND('',#6683,.T.);
#7445=FACE_BOUND('',#6684,.T.);
#7446=FACE_BOUND('',#6685,.T.);
#7447=FACE_BOUND('',#6686,.T.);
#7448=FACE_BOUND('',#6687,.T.);
#7449=FACE_BOUND('',#6688,.T.);
#7450=FACE_BOUND('',#6689,.T.);
#7451=FACE_BOUND('',#6690,.T.);
#7452=FACE_BOUND('',#6691,.T.);
#7453=FACE_BOUND('',#6692,.T.);
#7454=FACE_BOUND('',#6693,.T.);
#7455=FACE_BOUND('',#6694,.T.);
#7456=FACE_BOUND('',#6695,.T.);
#7457=FACE_BOUND('',#6696,.T.);
#7458=FACE_BOUND('',#6697,.T.);
#7459=FACE_BOUND('',#6698,.T.);
#7460=FACE_BOUND('',#6699,.T.);
#7461=FACE_BOUND('',#6700,.T.);
#7462=FACE_BOUND('',#6701,.T.);
#7463=FACE_BOUND('',#6702,.T.);
#7464=FACE_BOUND('',#6703,.T.);
#7465=FACE_BOUND('',#6704,.T.);
#7466=FACE_BOUND('',#6705,.T.);
#7467=FACE_BOUND('',#6706,.T.);
#7468=FACE_BOUND('',#6707,.T.);
#7469=FACE_BOUND('',#6708,.T.);
#7470=FACE_BOUND('',#6709,.T.);
#7471=FACE_BOUND('',#6710,.T.);
#7472=FACE_BOUND('',#6711,.T.);
#7473=FACE_BOUND('',#6712,.T.);
#7474=FACE_BOUND('',#6713,.T.);
#7523=CYLINDRICAL_SURFACE('',#8692,0.016);
#7524=CYLINDRICAL_SURFACE('',#8699,0.01635);
#7525=CYLINDRICAL_SURFACE('',#8701,0.01635);
#7526=CYLINDRICAL_SURFACE('',#8707,0.016);
#7527=CYLINDRICAL_SURFACE('',#8709,0.016);
#7528=CYLINDRICAL_SURFACE('',#8715,0.01635);
#7529=CYLINDRICAL_SURFACE('',#8717,0.01635);
#7530=CYLINDRICAL_SURFACE('',#8723,0.016);
#7531=CYLINDRICAL_SURFACE('',#8725,0.016);
#7532=CYLINDRICAL_SURFACE('',#8731,0.01635);
#7533=CYLINDRICAL_SURFACE('',#8733,0.01635);
#7534=CYLINDRICAL_SURFACE('',#8739,0.016);
#7535=CYLINDRICAL_SURFACE('',#8741,0.016);
#7536=CYLINDRICAL_SURFACE('',#8747,0.0175);
#7537=CYLINDRICAL_SURFACE('',#8749,0.0125);
#7538=CYLINDRICAL_SURFACE('',#8755,0.0185);
#7539=CYLINDRICAL_SURFACE('',#8757,0.0115);
#7540=CYLINDRICAL_SURFACE('',#8781,0.0013);
#7541=CYLINDRICAL_SURFACE('',#8783,0.0013);
#7542=CYLINDRICAL_SURFACE('',#8785,0.0013);
#7543=CYLINDRICAL_SURFACE('',#8787,0.0013);
#7544=CYLINDRICAL_SURFACE('',#8789,0.0013);
#7545=CYLINDRICAL_SURFACE('',#8791,0.0013);
#7546=CYLINDRICAL_SURFACE('',#8793,0.0013);
#7547=CYLINDRICAL_SURFACE('',#8795,0.0013);
#7548=CYLINDRICAL_SURFACE('',#8797,0.0013);
#7549=CYLINDRICAL_SURFACE('',#8799,0.0013);
#7550=CYLINDRICAL_SURFACE('',#8801,0.0013);
#7551=CYLINDRICAL_SURFACE('',#8803,0.0013);
#7552=CYLINDRICAL_SURFACE('',#8805,0.0013);
#7553=CYLINDRICAL_SURFACE('',#8807,0.0013);
#7554=CYLINDRICAL_SURFACE('',#8809,0.0013);
#7555=CYLINDRICAL_SURFACE('',#8811,0.0013);
#7556=CYLINDRICAL_SURFACE('',#8813,0.0013);
#7557=CYLINDRICAL_SURFACE('',#8815,0.0013);
#7558=CYLINDRICAL_SURFACE('',#8819,0.012);
#7559=CYLINDRICAL_SURFACE('',#8824,0.034);
#7560=CYLINDRICAL_SURFACE('',#8828,0.0195);
#7561=CYLINDRICAL_SURFACE('',#8830,0.0115);
#7562=CYLINDRICAL_SURFACE('',#8839,0.0125);
#7563=CYLINDRICAL_SURFACE('',#8841,0.016035898385);
#7564=CYLINDRICAL_SURFACE('',#8848,0.00149895940068901);
#7565=CYLINDRICAL_SURFACE('',#8851,0.001498959108051);
#7566=CYLINDRICAL_SURFACE('',#8853,0.0014989594008755);
#7567=CYLINDRICAL_SURFACE('',#8856,0.00149895910812507);
#7568=CYLINDRICAL_SURFACE('',#8858,0.00149895940094096);
#7569=CYLINDRICAL_SURFACE('',#8861,0.00149895910814045);
#7570=CYLINDRICAL_SURFACE('',#8865,0.0014989594007659);
#7571=CYLINDRICAL_SURFACE('',#8868,0.00149895910811289);
#7572=CYLINDRICAL_SURFACE('',#8870,0.00149895940089024);
#7573=CYLINDRICAL_SURFACE('',#8873,0.00149895910812507);
#7574=CYLINDRICAL_SURFACE('',#8875,0.00149895940094097);
#7575=CYLINDRICAL_SURFACE('',#8878,0.00149895910814057);
#7576=CYLINDRICAL_SURFACE('',#8881,0.017035898385);
#7577=CYLINDRICAL_SURFACE('',#8883,0.0015);
#7578=CYLINDRICAL_SURFACE('',#8935,0.0015);
#7579=CYLINDRICAL_SURFACE('',#8937,0.017035898385);
#7580=CYLINDRICAL_SURFACE('',#8939,0.0015);
#7581=CYLINDRICAL_SURFACE('',#8941,0.0015);
#7582=CYLINDRICAL_SURFACE('',#8943,0.017035898385);
#7583=CYLINDRICAL_SURFACE('',#8945,0.0015);
#7584=CYLINDRICAL_SURFACE('',#8947,0.0015);
#7585=CYLINDRICAL_SURFACE('',#8949,0.017035898385);
#7586=CYLINDRICAL_SURFACE('',#8951,0.0015);
#7587=CYLINDRICAL_SURFACE('',#8953,0.0015);
#7588=CYLINDRICAL_SURFACE('',#8955,0.017035898385);
#7589=CYLINDRICAL_SURFACE('',#8957,0.0015);
#7590=CYLINDRICAL_SURFACE('',#8959,0.0015);
#7591=CYLINDRICAL_SURFACE('',#8961,0.017035898385);
#7592=CYLINDRICAL_SURFACE('',#8963,0.0015);
#7593=CYLINDRICAL_SURFACE('',#8965,0.0015);
#7594=CYLINDRICAL_SURFACE('',#9009,0.0013);
#7595=CYLINDRICAL_SURFACE('',#9010,0.0013);
#7596=CYLINDRICAL_SURFACE('',#9011,0.0013);
#7597=CYLINDRICAL_SURFACE('',#9012,0.0013);
#7598=CYLINDRICAL_SURFACE('',#9013,0.0013);
#7599=CYLINDRICAL_SURFACE('',#9014,0.0013);
#7600=CYLINDRICAL_SURFACE('',#9015,0.0013);
#7601=CYLINDRICAL_SURFACE('',#9016,0.0013);
#7602=CYLINDRICAL_SURFACE('',#9017,0.0013);
#7603=CYLINDRICAL_SURFACE('',#9018,0.0013);
#7604=CYLINDRICAL_SURFACE('',#9019,0.0013);
#7605=CYLINDRICAL_SURFACE('',#9020,0.0013);
#7606=CYLINDRICAL_SURFACE('',#9021,0.0013);
#7607=CYLINDRICAL_SURFACE('',#9022,0.0013);
#7608=CYLINDRICAL_SURFACE('',#9023,0.0013);
#7609=CYLINDRICAL_SURFACE('',#9024,0.0013);
#7610=CYLINDRICAL_SURFACE('',#9025,0.0013);
#7611=CYLINDRICAL_SURFACE('',#9026,0.0013);
#7612=CYLINDRICAL_SURFACE('',#9028,0.0015);
#7613=CYLINDRICAL_SURFACE('',#9029,0.024);
#7614=CYLINDRICAL_SURFACE('',#9030,0.0015);
#7615=CYLINDRICAL_SURFACE('',#9033,0.0015);
#7616=CYLINDRICAL_SURFACE('',#9034,0.024);
#7617=CYLINDRICAL_SURFACE('',#9035,0.0015);
#7618=CYLINDRICAL_SURFACE('',#9037,0.0015);
#7619=CYLINDRICAL_SURFACE('',#9038,0.024);
#7620=CYLINDRICAL_SURFACE('',#9039,0.0015);
#7621=CYLINDRICAL_SURFACE('',#9042,0.0015);
#7622=CYLINDRICAL_SURFACE('',#9043,0.024);
#7623=CYLINDRICAL_SURFACE('',#9044,0.0015);
#7624=CYLINDRICAL_SURFACE('',#9047,0.0015);
#7625=CYLINDRICAL_SURFACE('',#9048,0.024);
#7626=CYLINDRICAL_SURFACE('',#9049,0.0015);
#7627=CYLINDRICAL_SURFACE('',#9052,0.0015);
#7628=CYLINDRICAL_SURFACE('',#9053,0.024);
#7629=CYLINDRICAL_SURFACE('',#9054,0.0015);
#7630=CYLINDRICAL_SURFACE('',#9058,0.016035898385);
#7631=CYLINDRICAL_SURFACE('',#9064,0.034);
#7632=CYLINDRICAL_SURFACE('',#9067,0.016035898385);
#7633=CYLINDRICAL_SURFACE('',#9115,0.016535898385);
#7634=CYLINDRICAL_SURFACE('',#9119,0.016535898385);
#7635=CYLINDRICAL_SURFACE('',#9120,0.000299999999290666);
#7636=CYLINDRICAL_SURFACE('',#9126,0.016535898385);
#7637=CYLINDRICAL_SURFACE('',#9130,0.016535898385);
#7638=CYLINDRICAL_SURFACE('',#9134,0.016535898385);
#7639=CYLINDRICAL_SURFACE('',#9138,0.016535898385);
#7640=CYLINDRICAL_SURFACE('',#9147,0.00214999999988175);
#7641=CYLINDRICAL_SURFACE('',#9148,0.00215);
#7642=CYLINDRICAL_SURFACE('',#9149,0.00214999999988175);
#7643=CYLINDRICAL_SURFACE('',#9150,0.00214999999988175);
#7644=CYLINDRICAL_SURFACE('',#9151,0.00215);
#7645=CYLINDRICAL_SURFACE('',#9152,0.00214999999988175);
#7646=CYLINDRICAL_SURFACE('',#9153,0.0003);
#7647=CYLINDRICAL_SURFACE('',#9154,0.0003);
#7648=CYLINDRICAL_SURFACE('',#9155,0.024);
#7649=CYLINDRICAL_SURFACE('',#9156,0.0003);
#7650=CYLINDRICAL_SURFACE('',#9157,0.0003);
#7651=CYLINDRICAL_SURFACE('',#9158,0.024);
#7652=CYLINDRICAL_SURFACE('',#9160,0.0003);
#7653=CYLINDRICAL_SURFACE('',#9161,0.024);
#7654=CYLINDRICAL_SURFACE('',#9163,0.0003);
#7655=CYLINDRICAL_SURFACE('',#9164,0.0003);
#7656=CYLINDRICAL_SURFACE('',#9165,0.024);
#7657=CYLINDRICAL_SURFACE('',#9166,0.0003);
#7658=CYLINDRICAL_SURFACE('',#9167,0.0003);
#7659=CYLINDRICAL_SURFACE('',#9168,0.024);
#7660=CYLINDRICAL_SURFACE('',#9169,0.0003);
#7661=CYLINDRICAL_SURFACE('',#9170,0.0003);
#7662=CYLINDRICAL_SURFACE('',#9171,0.024);
#7663=CYLINDRICAL_SURFACE('',#9178,0.0003);
#7913=ADVANCED_FACE('',(#7024,#7025),#7523,.F.);
#7914=ADVANCED_FACE('',(#7026,#7027),#1047,.T.);
#7915=ADVANCED_FACE('',(#7028,#7029),#1048,.T.);
#7916=ADVANCED_FACE('',(#7030,#7031),#7524,.F.);
#7917=ADVANCED_FACE('',(#7032,#7033),#7525,.F.);
#7918=ADVANCED_FACE('',(#7034,#7035),#1049,.T.);
#7919=ADVANCED_FACE('',(#7036,#7037),#1050,.T.);
#7920=ADVANCED_FACE('',(#7038,#7039),#7526,.F.);
#7921=ADVANCED_FACE('',(#7040,#7041),#7527,.F.);
#7922=ADVANCED_FACE('',(#7042,#7043),#1051,.T.);
#7923=ADVANCED_FACE('',(#7044,#7045),#1052,.T.);
#7924=ADVANCED_FACE('',(#7046,#7047),#7528,.F.);
#7925=ADVANCED_FACE('',(#7048,#7049),#7529,.F.);
#7926=ADVANCED_FACE('',(#7050,#7051),#1053,.T.);
#7927=ADVANCED_FACE('',(#7052,#7053),#1054,.T.);
#7928=ADVANCED_FACE('',(#7054,#7055),#7530,.F.);
#7929=ADVANCED_FACE('',(#7056,#7057),#7531,.F.);
#7930=ADVANCED_FACE('',(#7058,#7059),#1055,.T.);
#7931=ADVANCED_FACE('',(#7060,#7061),#1056,.T.);
#7932=ADVANCED_FACE('',(#7062,#7063),#7532,.F.);
#7933=ADVANCED_FACE('',(#7064,#7065),#7533,.F.);
#7934=ADVANCED_FACE('',(#7066,#7067),#1057,.T.);
#7935=ADVANCED_FACE('',(#7068,#7069),#1058,.T.);
#7936=ADVANCED_FACE('',(#7070,#7071),#7534,.F.);
#7937=ADVANCED_FACE('',(#7072,#7073),#7535,.F.);
#7938=ADVANCED_FACE('',(#7074,#7075),#1059,.T.);
#7939=ADVANCED_FACE('',(#7076,#7077),#1060,.T.);
#7940=ADVANCED_FACE('',(#7078,#7079),#7536,.F.);
#7941=ADVANCED_FACE('',(#7080,#7081),#7537,.F.);
#7942=ADVANCED_FACE('',(#7082,#7083),#1061,.F.);
#7943=ADVANCED_FACE('',(#7084,#7085),#1062,.T.);
#7944=ADVANCED_FACE('',(#7086,#7087),#7538,.T.);
#7945=ADVANCED_FACE('',(#7088,#7089),#7539,.F.);
#7946=ADVANCED_FACE('',(#7090,#7091,#7092,#7093,#7094,#7095,#7096,#7097,
#7098,#7099,#7100,#7101,#7102,#7103,#7104,#7105,#7106,#7107,#7108,#7109),
#1063,.F.);
#7947=ADVANCED_FACE('',(#7110,#7111),#25,.F.);
#7948=ADVANCED_FACE('',(#7112,#7113),#7540,.F.);
#7949=ADVANCED_FACE('',(#7114,#7115),#7541,.F.);
#7950=ADVANCED_FACE('',(#7116,#7117),#7542,.F.);
#7951=ADVANCED_FACE('',(#7118,#7119),#7543,.F.);
#7952=ADVANCED_FACE('',(#7120,#7121),#7544,.F.);
#7953=ADVANCED_FACE('',(#7122,#7123),#7545,.F.);
#7954=ADVANCED_FACE('',(#7124,#7125),#7546,.F.);
#7955=ADVANCED_FACE('',(#7126,#7127),#7547,.F.);
#7956=ADVANCED_FACE('',(#7128,#7129),#7548,.F.);
#7957=ADVANCED_FACE('',(#7130,#7131),#7549,.F.);
#7958=ADVANCED_FACE('',(#7132,#7133),#7550,.F.);
#7959=ADVANCED_FACE('',(#7134,#7135),#7551,.F.);
#7960=ADVANCED_FACE('',(#7136,#7137),#7552,.F.);
#7961=ADVANCED_FACE('',(#7138,#7139),#7553,.F.);
#7962=ADVANCED_FACE('',(#7140,#7141),#7554,.F.);
#7963=ADVANCED_FACE('',(#7142,#7143),#7555,.F.);
#7964=ADVANCED_FACE('',(#7144,#7145),#7556,.F.);
#7965=ADVANCED_FACE('',(#7146,#7147),#7557,.F.);
#7966=ADVANCED_FACE('',(#7148,#7149),#74,.T.);
#7967=ADVANCED_FACE('',(#7150,#7151),#7558,.F.);
#7968=ADVANCED_FACE('',(#7152,#7153,#7154,#7155,#7156,#7157,#7158,#7159,
#7160,#7161,#7162,#7163,#7164,#7165,#7166,#7167,#7168,#7169,#7170,#7171),
#1064,.F.);
#7969=ADVANCED_FACE('',(#7172,#7173),#7559,.T.);
#7970=ADVANCED_FACE('',(#7174,#7175),#26,.F.);
#7971=ADVANCED_FACE('',(#7176,#7177),#7560,.T.);
#7972=ADVANCED_FACE('',(#7178,#7179),#75,.T.);
#7973=ADVANCED_FACE('',(#7180,#7181),#7561,.F.);
#7974=ADVANCED_FACE('',(#7182,#7183),#27,.T.);
#7975=ADVANCED_FACE('',(#7184,#7185),#1065,.T.);
#7976=ADVANCED_FACE('',(#7186),#76,.F.);
#7977=ADVANCED_FACE('',(#7187),#77,.F.);
#7978=ADVANCED_FACE('',(#7188,#7189),#7562,.F.);
#7979=ADVANCED_FACE('',(#7190,#7191),#7563,.T.);
#7980=ADVANCED_FACE('',(#7192,#7193),#78,.T.);
#7981=ADVANCED_FACE('',(#7194),#79,.F.);
#7982=ADVANCED_FACE('',(#7195),#7564,.F.);
#7983=ADVANCED_FACE('',(#7196),#80,.F.);
#7984=ADVANCED_FACE('',(#7197),#7565,.F.);
#7985=ADVANCED_FACE('',(#7198),#81,.F.);
#7986=ADVANCED_FACE('',(#7199),#7566,.F.);
#7987=ADVANCED_FACE('',(#7200),#82,.F.);
#7988=ADVANCED_FACE('',(#7201),#7567,.F.);
#7989=ADVANCED_FACE('',(#7202),#83,.F.);
#7990=ADVANCED_FACE('',(#7203),#7568,.F.);
#7991=ADVANCED_FACE('',(#7204),#84,.F.);
#7992=ADVANCED_FACE('',(#7205),#7569,.F.);
#7993=ADVANCED_FACE('',(#7206),#85,.F.);
#7994=ADVANCED_FACE('',(#7207),#86,.F.);
#7995=ADVANCED_FACE('',(#7208),#7570,.F.);
#7996=ADVANCED_FACE('',(#7209),#87,.F.);
#7997=ADVANCED_FACE('',(#7210),#7571,.F.);
#7998=ADVANCED_FACE('',(#7211),#88,.F.);
#7999=ADVANCED_FACE('',(#7212),#7572,.F.);
#8000=ADVANCED_FACE('',(#7213),#89,.F.);
#8001=ADVANCED_FACE('',(#7214),#7573,.F.);
#8002=ADVANCED_FACE('',(#7215),#90,.F.);
#8003=ADVANCED_FACE('',(#7216),#7574,.F.);
#8004=ADVANCED_FACE('',(#7217),#91,.F.);
#8005=ADVANCED_FACE('',(#7218),#7575,.F.);
#8006=ADVANCED_FACE('',(#7219,#7220),#1066,.F.);
#8007=ADVANCED_FACE('',(#7221),#7576,.T.);
#8008=ADVANCED_FACE('',(#7222),#7577,.F.);
#8009=ADVANCED_FACE('',(#7223,#7224,#7225,#7226,#7227,#7228,#7229,#7230,
#7231,#7232,#7233,#7234,#7235,#7236,#7237,#7238,#7239,#7240,#7241,#7242),
#1067,.F.);
#8010=ADVANCED_FACE('',(#7243),#7578,.F.);
#8011=ADVANCED_FACE('',(#7244),#7579,.T.);
#8012=ADVANCED_FACE('',(#7245),#7580,.F.);
#8013=ADVANCED_FACE('',(#7246),#7581,.F.);
#8014=ADVANCED_FACE('',(#7247),#7582,.T.);
#8015=ADVANCED_FACE('',(#7248),#7583,.F.);
#8016=ADVANCED_FACE('',(#7249),#7584,.F.);
#8017=ADVANCED_FACE('',(#7250),#7585,.T.);
#8018=ADVANCED_FACE('',(#7251),#7586,.F.);
#8019=ADVANCED_FACE('',(#7252),#7587,.F.);
#8020=ADVANCED_FACE('',(#7253),#7588,.T.);
#8021=ADVANCED_FACE('',(#7254),#7589,.F.);
#8022=ADVANCED_FACE('',(#7255),#7590,.F.);
#8023=ADVANCED_FACE('',(#7256),#7591,.T.);
#8024=ADVANCED_FACE('',(#7257),#7592,.F.);
#8025=ADVANCED_FACE('',(#7258),#7593,.F.);
#8026=ADVANCED_FACE('',(#7259,#7260),#92,.T.);
#8027=ADVANCED_FACE('',(#7261,#7262,#7263,#7264,#7265,#7266,#7267,#7268,
#7269,#7270,#7271,#7272,#7273,#7274,#7275,#7276,#7277,#7278,#7279,#7280,
#7281,#7282,#7283,#7284,#7285,#7286),#1068,.F.);
#8028=ADVANCED_FACE('',(#7287),#1069,.F.);
#8029=ADVANCED_FACE('',(#7288,#7289),#7594,.F.);
#8030=ADVANCED_FACE('',(#7290,#7291),#7595,.F.);
#8031=ADVANCED_FACE('',(#7292,#7293),#7596,.F.);
#8032=ADVANCED_FACE('',(#7294,#7295),#7597,.F.);
#8033=ADVANCED_FACE('',(#7296,#7297),#7598,.F.);
#8034=ADVANCED_FACE('',(#7298,#7299),#7599,.F.);
#8035=ADVANCED_FACE('',(#7300,#7301),#7600,.F.);
#8036=ADVANCED_FACE('',(#7302,#7303),#7601,.F.);
#8037=ADVANCED_FACE('',(#7304,#7305),#7602,.F.);
#8038=ADVANCED_FACE('',(#7306,#7307),#7603,.F.);
#8039=ADVANCED_FACE('',(#7308,#7309),#7604,.F.);
#8040=ADVANCED_FACE('',(#7310,#7311),#7605,.F.);
#8041=ADVANCED_FACE('',(#7312,#7313),#7606,.F.);
#8042=ADVANCED_FACE('',(#7314,#7315),#7607,.F.);
#8043=ADVANCED_FACE('',(#7316,#7317),#7608,.F.);
#8044=ADVANCED_FACE('',(#7318,#7319),#7609,.F.);
#8045=ADVANCED_FACE('',(#7320,#7321),#7610,.F.);
#8046=ADVANCED_FACE('',(#7322,#7323),#7611,.F.);
#8047=ADVANCED_FACE('',(#7324),#1070,.F.);
#8048=ADVANCED_FACE('',(#7325),#7612,.F.);
#8049=ADVANCED_FACE('',(#7326),#7613,.F.);
#8050=ADVANCED_FACE('',(#7327),#7614,.F.);
#8051=ADVANCED_FACE('',(#7328),#1071,.F.);
#8052=ADVANCED_FACE('',(#7329),#1072,.F.);
#8053=ADVANCED_FACE('',(#7330),#7615,.F.);
#8054=ADVANCED_FACE('',(#7331),#7616,.F.);
#8055=ADVANCED_FACE('',(#7332),#7617,.F.);
#8056=ADVANCED_FACE('',(#7333),#1073,.F.);
#8057=ADVANCED_FACE('',(#7334),#7618,.F.);
#8058=ADVANCED_FACE('',(#7335),#7619,.F.);
#8059=ADVANCED_FACE('',(#7336),#7620,.F.);
#8060=ADVANCED_FACE('',(#7337),#1074,.F.);
#8061=ADVANCED_FACE('',(#7338),#1075,.F.);
#8062=ADVANCED_FACE('',(#7339),#7621,.F.);
#8063=ADVANCED_FACE('',(#7340),#7622,.F.);
#8064=ADVANCED_FACE('',(#7341),#7623,.F.);
#8065=ADVANCED_FACE('',(#7342),#1076,.F.);
#8066=ADVANCED_FACE('',(#7343),#1077,.F.);
#8067=ADVANCED_FACE('',(#7344),#7624,.F.);
#8068=ADVANCED_FACE('',(#7345),#7625,.F.);
#8069=ADVANCED_FACE('',(#7346),#7626,.F.);
#8070=ADVANCED_FACE('',(#7347),#1078,.F.);
#8071=ADVANCED_FACE('',(#7348),#1079,.F.);
#8072=ADVANCED_FACE('',(#7349),#7627,.F.);
#8073=ADVANCED_FACE('',(#7350),#7628,.F.);
#8074=ADVANCED_FACE('',(#7351),#7629,.F.);
#8075=ADVANCED_FACE('',(#7352),#1080,.F.);
#8076=ADVANCED_FACE('',(#7353,#7354),#93,.T.);
#8077=ADVANCED_FACE('',(#7355,#7356),#7630,.T.);
#8078=ADVANCED_FACE('',(#7357,#7358),#94,.F.);
#8079=ADVANCED_FACE('',(#7359,#7360),#95,.T.);
#8080=ADVANCED_FACE('',(#7361,#7362),#7631,.T.);
#8081=ADVANCED_FACE('',(#7363,#7364),#96,.F.);
#8082=ADVANCED_FACE('',(#7365,#7366),#7632,.T.);
#8083=ADVANCED_FACE('',(#7367,#7368,#7369,#7370,#7371,#7372,#7373,#7374),
#1081,.F.);
#8084=ADVANCED_FACE('',(#7375),#97,.F.);
#8085=ADVANCED_FACE('',(#7376),#98,.F.);
#8086=ADVANCED_FACE('',(#7377,#7378),#99,.T.);
#8087=ADVANCED_FACE('',(#7379),#100,.T.);
#8088=ADVANCED_FACE('',(#7380),#101,.T.);
#8089=ADVANCED_FACE('',(#7381,#7382),#102,.T.);
#8090=ADVANCED_FACE('',(#7383,#7384),#103,.T.);
#8091=ADVANCED_FACE('',(#7385),#104,.T.);
#8092=ADVANCED_FACE('',(#7386),#105,.T.);
#8093=ADVANCED_FACE('',(#7387,#7388),#106,.T.);
#8094=ADVANCED_FACE('',(#7389),#1082,.F.);
#8095=ADVANCED_FACE('',(#7390),#107,.T.);
#8096=ADVANCED_FACE('',(#7391),#1083,.F.);
#8097=ADVANCED_FACE('',(#7392),#7633,.T.);
#8098=ADVANCED_FACE('',(#7393),#1084,.F.);
#8099=ADVANCED_FACE('',(#7394),#108,.T.);
#8100=ADVANCED_FACE('',(#7395),#1085,.F.);
#8101=ADVANCED_FACE('',(#7396),#7634,.T.);
#8102=ADVANCED_FACE('',(#7397),#7635,.T.);
#8103=ADVANCED_FACE('',(#7398),#109,.T.);
#8104=ADVANCED_FACE('',(#7399),#1086,.F.);
#8105=ADVANCED_FACE('',(#7400),#7636,.T.);
#8106=ADVANCED_FACE('',(#7401),#1087,.F.);
#8107=ADVANCED_FACE('',(#7402),#110,.T.);
#8108=ADVANCED_FACE('',(#7403),#1088,.F.);
#8109=ADVANCED_FACE('',(#7404),#7637,.T.);
#8110=ADVANCED_FACE('',(#7405),#1089,.F.);
#8111=ADVANCED_FACE('',(#7406),#111,.T.);
#8112=ADVANCED_FACE('',(#7407),#1090,.F.);
#8113=ADVANCED_FACE('',(#7408),#7638,.T.);
#8114=ADVANCED_FACE('',(#7409),#1091,.F.);
#8115=ADVANCED_FACE('',(#7410),#112,.T.);
#8116=ADVANCED_FACE('',(#7411),#1092,.F.);
#8117=ADVANCED_FACE('',(#7412),#7639,.T.);
#8118=ADVANCED_FACE('',(#7413,#7414),#28,.T.);
#8119=ADVANCED_FACE('',(#7415,#7416),#29,.T.);
#8120=ADVANCED_FACE('',(#7417),#1093,.F.);
#8121=ADVANCED_FACE('',(#7418,#7419),#30,.T.);
#8122=ADVANCED_FACE('',(#7420,#7421),#31,.T.);
#8123=ADVANCED_FACE('',(#7422,#7423),#32,.T.);
#8124=ADVANCED_FACE('',(#7424,#7425),#33,.T.);
#8125=ADVANCED_FACE('',(#7426,#7427),#7640,.F.);
#8126=ADVANCED_FACE('',(#7428,#7429),#7641,.F.);
#8127=ADVANCED_FACE('',(#7430,#7431),#7642,.F.);
#8128=ADVANCED_FACE('',(#7432,#7433),#7643,.F.);
#8129=ADVANCED_FACE('',(#7434,#7435),#7644,.F.);
#8130=ADVANCED_FACE('',(#7436,#7437),#7645,.F.);
#8131=ADVANCED_FACE('',(#7438),#7646,.T.);
#8132=ADVANCED_FACE('',(#7439),#7647,.T.);
#8133=ADVANCED_FACE('',(#7440),#7648,.T.);
#8134=ADVANCED_FACE('',(#7441),#7649,.T.);
#8135=ADVANCED_FACE('',(#7442),#7650,.T.);
#8136=ADVANCED_FACE('',(#7443),#7651,.T.);
#8137=ADVANCED_FACE('',(#7444),#22,.T.);
#8138=ADVANCED_FACE('',(#7445),#7652,.T.);
#8139=ADVANCED_FACE('',(#7446),#7653,.T.);
#8140=ADVANCED_FACE('',(#7447),#7654,.T.);
#8141=ADVANCED_FACE('',(#7448),#7655,.T.);
#8142=ADVANCED_FACE('',(#7449),#7656,.T.);
#8143=ADVANCED_FACE('',(#7450),#7657,.T.);
#8144=ADVANCED_FACE('',(#7451),#7658,.T.);
#8145=ADVANCED_FACE('',(#7452),#7659,.T.);
#8146=ADVANCED_FACE('',(#7453),#7660,.T.);
#8147=ADVANCED_FACE('',(#7454),#7661,.T.);
#8148=ADVANCED_FACE('',(#7455),#7662,.T.);
#8149=ADVANCED_FACE('',(#7456),#10,.T.);
#8150=ADVANCED_FACE('',(#7457),#11,.T.);
#8151=ADVANCED_FACE('',(#7458),#113,.T.);
#8152=ADVANCED_FACE('',(#7459),#12,.T.);
#8153=ADVANCED_FACE('',(#7460),#13,.T.);
#8154=ADVANCED_FACE('',(#7461),#114,.T.);
#8155=ADVANCED_FACE('',(#7462),#7663,.T.);
#8156=ADVANCED_FACE('',(#7463),#14,.T.);
#8157=ADVANCED_FACE('',(#7464),#15,.T.);
#8158=ADVANCED_FACE('',(#7465),#115,.T.);
#8159=ADVANCED_FACE('',(#7466),#16,.T.);
#8160=ADVANCED_FACE('',(#7467),#17,.T.);
#8161=ADVANCED_FACE('',(#7468),#116,.T.);
#8162=ADVANCED_FACE('',(#7469),#18,.T.);
#8163=ADVANCED_FACE('',(#7470),#19,.T.);
#8164=ADVANCED_FACE('',(#7471),#117,.T.);
#8165=ADVANCED_FACE('',(#7472),#20,.T.);
#8166=ADVANCED_FACE('',(#7473),#21,.T.);
#8167=ADVANCED_FACE('',(#7474),#118,.T.);
#8173=CLOSED_SHELL('',(#7913,#7914,#7915,#7916,#7917,#7918,#7919,#7920,
#7921,#7922,#7923,#7924,#7925,#7926,#7927,#7928,#7929,#7930,#7931,#7932,
#7933,#7934,#7935,#7936,#7937,#7938,#7939,#7940,#7941,#7942,#7943,#7944,
#7945,#7946,#7947,#7948,#7949,#7950,#7951,#7952,#7953,#7954,#7955,#7956,
#7957,#7958,#7959,#7960,#7961,#7962,#7963,#7964,#7965,#7966,#7967,#7968,
#7969,#7970,#7971,#7972,#7973,#7974,#7975,#7976,#7977,#7978,#7979,#7980,
#7981,#7982,#7983,#7984,#7985,#7986,#7987,#7988,#7989,#7990,#7991,#7992,
#7993,#7994,#7995,#7996,#7997,#7998,#7999,#8000,#8001,#8002,#8003,#8004,
#8005,#8006,#8007,#8008,#8009,#8010,#8011,#8012,#8013,#8014,#8015,#8016,
#8017,#8018,#8019,#8020,#8021,#8022,#8023,#8024,#8025,#8026,#8027,#8028,
#8029,#8030,#8031,#8032,#8033,#8034,#8035,#8036,#8037,#8038,#8039,#8040,
#8041,#8042,#8043,#8044,#8045,#8046,#8047,#8048,#8049,#8050,#8051,#8052,
#8053,#8054,#8055,#8056,#8057,#8058,#8059,#8060,#8061,#8062,#8063,#8064,
#8065,#8066,#8067,#8068,#8069,#8070,#8071,#8072,#8073,#8074,#8075,#8076,
#8077,#8078,#8079,#8080,#8081,#8082,#8083,#8084,#8085,#8086,#8087,#8088,
#8089,#8090,#8091,#8092,#8093,#8094,#8095,#8096,#8097,#8098,#8099,#8100,
#8101,#8102,#8103,#8104,#8105,#8106,#8107,#8108,#8109,#8110,#8111,#8112,
#8113,#8114,#8115,#8116,#8117,#8118,#8119,#8120,#8121,#8122,#8123,#8124,
#8125,#8126,#8127,#8128,#8129,#8130,#8131,#8132,#8133,#8134,#8135,#8136,
#8137,#8138,#8139,#8140,#8141,#8142,#8143,#8144,#8145,#8146,#8147,#8148,
#8149,#8150,#8151,#8152,#8153,#8154,#8155,#8156,#8157,#8158,#8159,#8160,
#8161,#8162,#8163,#8164,#8165,#8166,#8167));
#8179=STYLED_ITEM('',(#8185),#8224);
#8185=PRESENTATION_STYLE_ASSIGNMENT((#8191));
#8191=SURFACE_STYLE_USAGE(.BOTH.,#8197);
#8197=SURFACE_SIDE_STYLE('',(#8203));
#8203=SURFACE_STYLE_FILL_AREA(#8209);
#8209=FILL_AREA_STYLE('',(#8215));
#8215=FILL_AREA_STYLE_COLOUR('',#8218);
#8218=COLOUR_RGB('', 0.09019608, 0.27058824, 0.51372549);
#8224=MANIFOLD_SOLID_BREP('HubBody__ DE       35',#8173);
#8231=SHAPE_DEFINITION_REPRESENTATION(#18838,#8238);
#8238=SHAPE_REPRESENTATION('HubBody__ DE       35',(#8239),#18816);
#8239=AXIS2_PLACEMENT_3D('',#11098,#9192,#9193);
#8692=AXIS2_PLACEMENT_3D('',#13701,#10098,#10099);
#8693=AXIS2_PLACEMENT_3D('',#13702,#10100,#10101);
#8694=AXIS2_PLACEMENT_3D('',#13704,#10102,#10103);
#8695=AXIS2_PLACEMENT_3D('',#13706,#10104,#10105);
#8696=AXIS2_PLACEMENT_3D('',#13707,#10106,#10107);
#8697=AXIS2_PLACEMENT_3D('',#13709,#10108,#10109);
#8698=AXIS2_PLACEMENT_3D('',#13710,#10110,#10111);
#8699=AXIS2_PLACEMENT_3D('',#13712,#10112,#10113);
#8700=AXIS2_PLACEMENT_3D('',#13713,#10114,#10115);
#8701=AXIS2_PLACEMENT_3D('',#13715,#10116,#10117);
#8702=AXIS2_PLACEMENT_3D('',#13716,#10118,#10119);
#8703=AXIS2_PLACEMENT_3D('',#13718,#10120,#10121);
#8704=AXIS2_PLACEMENT_3D('',#13719,#10122,#10123);
#8705=AXIS2_PLACEMENT_3D('',#13721,#10124,#10125);
#8706=AXIS2_PLACEMENT_3D('',#13722,#10126,#10127);
#8707=AXIS2_PLACEMENT_3D('',#13724,#10128,#10129);
#8708=AXIS2_PLACEMENT_3D('',#13725,#10130,#10131);
#8709=AXIS2_PLACEMENT_3D('',#13727,#10132,#10133);
#8710=AXIS2_PLACEMENT_3D('',#13728,#10134,#10135);
#8711=AXIS2_PLACEMENT_3D('',#13730,#10136,#10137);
#8712=AXIS2_PLACEMENT_3D('',#13731,#10138,#10139);
#8713=AXIS2_PLACEMENT_3D('',#13733,#10140,#10141);
#8714=AXIS2_PLACEMENT_3D('',#13734,#10142,#10143);
#8715=AXIS2_PLACEMENT_3D('',#13736,#10144,#10145);
#8716=AXIS2_PLACEMENT_3D('',#13737,#10146,#10147);
#8717=AXIS2_PLACEMENT_3D('',#13739,#10148,#10149);
#8718=AXIS2_PLACEMENT_3D('',#13740,#10150,#10151);
#8719=AXIS2_PLACEMENT_3D('',#13742,#10152,#10153);
#8720=AXIS2_PLACEMENT_3D('',#13743,#10154,#10155);
#8721=AXIS2_PLACEMENT_3D('',#13745,#10156,#10157);
#8722=AXIS2_PLACEMENT_3D('',#13746,#10158,#10159);
#8723=AXIS2_PLACEMENT_3D('',#13748,#10160,#10161);
#8724=AXIS2_PLACEMENT_3D('',#13749,#10162,#10163);
#8725=AXIS2_PLACEMENT_3D('',#13751,#10164,#10165);
#8726=AXIS2_PLACEMENT_3D('',#13752,#10166,#10167);
#8727=AXIS2_PLACEMENT_3D('',#13754,#10168,#10169);
#8728=AXIS2_PLACEMENT_3D('',#13755,#10170,#10171);
#8729=AXIS2_PLACEMENT_3D('',#13757,#10172,#10173);
#8730=AXIS2_PLACEMENT_3D('',#13758,#10174,#10175);
#8731=AXIS2_PLACEMENT_3D('',#13760,#10176,#10177);
#8732=AXIS2_PLACEMENT_3D('',#13761,#10178,#10179);
#8733=AXIS2_PLACEMENT_3D('',#13763,#10180,#10181);
#8734=AXIS2_PLACEMENT_3D('',#13764,#10182,#10183);
#8735=AXIS2_PLACEMENT_3D('',#13766,#10184,#10185);
#8736=AXIS2_PLACEMENT_3D('',#13767,#10186,#10187);
#8737=AXIS2_PLACEMENT_3D('',#13769,#10188,#10189);
#8738=AXIS2_PLACEMENT_3D('',#13770,#10190,#10191);
#8739=AXIS2_PLACEMENT_3D('',#13772,#10192,#10193);
#8740=AXIS2_PLACEMENT_3D('',#13773,#10194,#10195);
#8741=AXIS2_PLACEMENT_3D('',#13775,#10196,#10197);
#8742=AXIS2_PLACEMENT_3D('',#13776,#10198,#10199);
#8743=AXIS2_PLACEMENT_3D('',#13778,#10200,#10201);
#8744=AXIS2_PLACEMENT_3D('',#13779,#10202,#10203);
#8745=AXIS2_PLACEMENT_3D('',#13781,#10204,#10205);
#8746=AXIS2_PLACEMENT_3D('',#13782,#10206,#10207);
#8747=AXIS2_PLACEMENT_3D('',#13784,#10208,#10209);
#8748=AXIS2_PLACEMENT_3D('',#13785,#10210,#10211);
#8749=AXIS2_PLACEMENT_3D('',#13787,#10212,#10213);
#8750=AXIS2_PLACEMENT_3D('',#13788,#10214,#10215);
#8751=AXIS2_PLACEMENT_3D('',#13790,#10216,#10217);
#8752=AXIS2_PLACEMENT_3D('',#13791,#10218,#10219);
#8753=AXIS2_PLACEMENT_3D('',#13793,#10220,#10221);
#8754=AXIS2_PLACEMENT_3D('',#13794,#10222,#10223);
#8755=AXIS2_PLACEMENT_3D('',#13796,#10224,#10225);
#8756=AXIS2_PLACEMENT_3D('',#13797,#10226,#10227);
#8757=AXIS2_PLACEMENT_3D('',#13799,#10228,#10229);
#8758=AXIS2_PLACEMENT_3D('',#13800,#10230,#10231);
#8759=AXIS2_PLACEMENT_3D('',#13802,#10232,#10233);
#8760=AXIS2_PLACEMENT_3D('',#13803,#10234,#10235);
#8761=AXIS2_PLACEMENT_3D('',#13805,#10236,#10237);
#8762=AXIS2_PLACEMENT_3D('',#13807,#10238,#10239);
#8763=AXIS2_PLACEMENT_3D('',#13809,#10240,#10241);
#8764=AXIS2_PLACEMENT_3D('',#13811,#10242,#10243);
#8765=AXIS2_PLACEMENT_3D('',#13813,#10244,#10245);
#8766=AXIS2_PLACEMENT_3D('',#13815,#10246,#10247);
#8767=AXIS2_PLACEMENT_3D('',#13817,#10248,#10249);
#8768=AXIS2_PLACEMENT_3D('',#13819,#10250,#10251);
#8769=AXIS2_PLACEMENT_3D('',#13821,#10252,#10253);
#8770=AXIS2_PLACEMENT_3D('',#13823,#10254,#10255);
#8771=AXIS2_PLACEMENT_3D('',#13825,#10256,#10257);
#8772=AXIS2_PLACEMENT_3D('',#13827,#10258,#10259);
#8773=AXIS2_PLACEMENT_3D('',#13829,#10260,#10261);
#8774=AXIS2_PLACEMENT_3D('',#13831,#10262,#10263);
#8775=AXIS2_PLACEMENT_3D('',#13833,#10264,#10265);
#8776=AXIS2_PLACEMENT_3D('',#13835,#10266,#10267);
#8777=AXIS2_PLACEMENT_3D('',#13837,#10268,#10269);
#8778=AXIS2_PLACEMENT_3D('',#13839,#10270,#10271);
#8779=AXIS2_PLACEMENT_3D('',#13841,#10272,#10273);
#8780=AXIS2_PLACEMENT_3D('',#13842,#10274,#10275);
#8781=AXIS2_PLACEMENT_3D('',#13844,#10276,#10277);
#8782=AXIS2_PLACEMENT_3D('',#13845,#10278,#10279);
#8783=AXIS2_PLACEMENT_3D('',#13847,#10280,#10281);
#8784=AXIS2_PLACEMENT_3D('',#13848,#10282,#10283);
#8785=AXIS2_PLACEMENT_3D('',#13850,#10284,#10285);
#8786=AXIS2_PLACEMENT_3D('',#13851,#10286,#10287);
#8787=AXIS2_PLACEMENT_3D('',#13853,#10288,#10289);
#8788=AXIS2_PLACEMENT_3D('',#13854,#10290,#10291);
#8789=AXIS2_PLACEMENT_3D('',#13856,#10292,#10293);
#8790=AXIS2_PLACEMENT_3D('',#13857,#10294,#10295);
#8791=AXIS2_PLACEMENT_3D('',#13859,#10296,#10297);
#8792=AXIS2_PLACEMENT_3D('',#13860,#10298,#10299);
#8793=AXIS2_PLACEMENT_3D('',#13862,#10300,#10301);
#8794=AXIS2_PLACEMENT_3D('',#13863,#10302,#10303);
#8795=AXIS2_PLACEMENT_3D('',#13865,#10304,#10305);
#8796=AXIS2_PLACEMENT_3D('',#13866,#10306,#10307);
#8797=AXIS2_PLACEMENT_3D('',#13868,#10308,#10309);
#8798=AXIS2_PLACEMENT_3D('',#13869,#10310,#10311);
#8799=AXIS2_PLACEMENT_3D('',#13871,#10312,#10313);
#8800=AXIS2_PLACEMENT_3D('',#13872,#10314,#10315);
#8801=AXIS2_PLACEMENT_3D('',#13874,#10316,#10317);
#8802=AXIS2_PLACEMENT_3D('',#13875,#10318,#10319);
#8803=AXIS2_PLACEMENT_3D('',#13877,#10320,#10321);
#8804=AXIS2_PLACEMENT_3D('',#13878,#10322,#10323);
#8805=AXIS2_PLACEMENT_3D('',#13880,#10324,#10325);
#8806=AXIS2_PLACEMENT_3D('',#13881,#10326,#10327);
#8807=AXIS2_PLACEMENT_3D('',#13883,#10328,#10329);
#8808=AXIS2_PLACEMENT_3D('',#13884,#10330,#10331);
#8809=AXIS2_PLACEMENT_3D('',#13886,#10332,#10333);
#8810=AXIS2_PLACEMENT_3D('',#13887,#10334,#10335);
#8811=AXIS2_PLACEMENT_3D('',#13889,#10336,#10337);
#8812=AXIS2_PLACEMENT_3D('',#13890,#10338,#10339);
#8813=AXIS2_PLACEMENT_3D('',#13892,#10340,#10341);
#8814=AXIS2_PLACEMENT_3D('',#13893,#10342,#10343);
#8815=AXIS2_PLACEMENT_3D('',#13895,#10344,#10345);
#8816=AXIS2_PLACEMENT_3D('',#13896,#10346,#10347);
#8817=AXIS2_PLACEMENT_3D('',#13898,#10348,#10349);
#8818=AXIS2_PLACEMENT_3D('',#13899,#10350,#10351);
#8819=AXIS2_PLACEMENT_3D('',#13913,#10352,#10353);
#8820=AXIS2_PLACEMENT_3D('',#13914,#10354,#10355);
#8821=AXIS2_PLACEMENT_3D('',#13928,#10356,#10357);
#8822=AXIS2_PLACEMENT_3D('',#13929,#10358,#10359);
#8823=AXIS2_PLACEMENT_3D('',#13931,#10360,#10361);
#8824=AXIS2_PLACEMENT_3D('',#13933,#10362,#10363);
#8825=AXIS2_PLACEMENT_3D('',#13947,#10364,#10365);
#8826=AXIS2_PLACEMENT_3D('',#13948,#10366,#10367);
#8827=AXIS2_PLACEMENT_3D('',#13949,#10368,#10369);
#8828=AXIS2_PLACEMENT_3D('',#13963,#10370,#10371);
#8829=AXIS2_PLACEMENT_3D('',#13988,#10372,#10373);
#8830=AXIS2_PLACEMENT_3D('',#13989,#10374,#10375);
#8831=AXIS2_PLACEMENT_3D('',#13990,#10376,#10377);
#8832=AXIS2_PLACEMENT_3D('',#13992,#10378,#10379);
#8833=AXIS2_PLACEMENT_3D('',#14006,#10380,#10381);
#8834=AXIS2_PLACEMENT_3D('',#14007,#10382,#10383);
#8835=AXIS2_PLACEMENT_3D('',#14008,#10384,#10385);
#8836=AXIS2_PLACEMENT_3D('',#14010,#10386,#10387);
#8837=AXIS2_PLACEMENT_3D('',#14016,#10388,#10389);
#8838=AXIS2_PLACEMENT_3D('',#14022,#10390,#10391);
#8839=AXIS2_PLACEMENT_3D('',#14034,#10392,#10393);
#8840=AXIS2_PLACEMENT_3D('',#14035,#10394,#10395);
#8841=AXIS2_PLACEMENT_3D('',#14049,#10396,#10397);
#8842=AXIS2_PLACEMENT_3D('',#14152,#10398,#10399);
#8843=AXIS2_PLACEMENT_3D('',#14202,#10400,#10401);
#8844=AXIS2_PLACEMENT_3D('',#14246,#10402,#10403);
#8845=AXIS2_PLACEMENT_3D('',#14247,#10404,#10405);
#8846=AXIS2_PLACEMENT_3D('',#14249,#10406,#10407);
#8847=AXIS2_PLACEMENT_3D('',#14250,#10408,#10409);
#8848=AXIS2_PLACEMENT_3D('',#14278,#10410,#10411);
#8849=AXIS2_PLACEMENT_3D('',#14289,#10412,#10413);
#8850=AXIS2_PLACEMENT_3D('',#14290,#10414,#10415);
#8851=AXIS2_PLACEMENT_3D('',#14297,#10416,#10417);
#8852=AXIS2_PLACEMENT_3D('',#14316,#10418,#10419);
#8853=AXIS2_PLACEMENT_3D('',#14334,#10420,#10421);
#8854=AXIS2_PLACEMENT_3D('',#14345,#10422,#10423);
#8855=AXIS2_PLACEMENT_3D('',#14346,#10424,#10425);
#8856=AXIS2_PLACEMENT_3D('',#14353,#10426,#10427);
#8857=AXIS2_PLACEMENT_3D('',#14372,#10428,#10429);
#8858=AXIS2_PLACEMENT_3D('',#14390,#10430,#10431);
#8859=AXIS2_PLACEMENT_3D('',#14401,#10432,#10433);
#8860=AXIS2_PLACEMENT_3D('',#14402,#10434,#10435);
#8861=AXIS2_PLACEMENT_3D('',#14409,#10436,#10437);
#8862=AXIS2_PLACEMENT_3D('',#14420,#10438,#10439);
#8863=AXIS2_PLACEMENT_3D('',#14426,#10440,#10441);
#8864=AXIS2_PLACEMENT_3D('',#14427,#10442,#10443);
#8865=AXIS2_PLACEMENT_3D('',#14438,#10444,#10445);
#8866=AXIS2_PLACEMENT_3D('',#14449,#10446,#10447);
#8867=AXIS2_PLACEMENT_3D('',#14450,#10448,#10449);
#8868=AXIS2_PLACEMENT_3D('',#14457,#10450,#10451);
#8869=AXIS2_PLACEMENT_3D('',#14468,#10452,#10453);
#8870=AXIS2_PLACEMENT_3D('',#14479,#10454,#10455);
#8871=AXIS2_PLACEMENT_3D('',#14490,#10456,#10457);
#8872=AXIS2_PLACEMENT_3D('',#14491,#10458,#10459);
#8873=AXIS2_PLACEMENT_3D('',#14498,#10460,#10461);
#8874=AXIS2_PLACEMENT_3D('',#14509,#10462,#10463);
#8875=AXIS2_PLACEMENT_3D('',#14520,#10464,#10465);
#8876=AXIS2_PLACEMENT_3D('',#14531,#10466,#10467);
#8877=AXIS2_PLACEMENT_3D('',#14532,#10468,#10469);
#8878=AXIS2_PLACEMENT_3D('',#14539,#10470,#10471);
#8879=AXIS2_PLACEMENT_3D('',#14544,#10472,#10473);
#8880=AXIS2_PLACEMENT_3D('',#14545,#10474,#10475);
#8881=AXIS2_PLACEMENT_3D('',#14547,#10476,#10477);
#8882=AXIS2_PLACEMENT_3D('',#14558,#10478,#10479);
#8883=AXIS2_PLACEMENT_3D('',#14559,#10480,#10481);
#8884=AXIS2_PLACEMENT_3D('',#14560,#10482,#10483);
#8885=AXIS2_PLACEMENT_3D('',#14567,#10484,#10485);
#8886=AXIS2_PLACEMENT_3D('',#14568,#10486,#10487);
#8887=AXIS2_PLACEMENT_3D('',#14569,#10488,#10489);
#8888=AXIS2_PLACEMENT_3D('',#14577,#10490,#10491);
#8889=AXIS2_PLACEMENT_3D('',#14578,#10492,#10493);
#8890=AXIS2_PLACEMENT_3D('',#14585,#10494,#10495);
#8891=AXIS2_PLACEMENT_3D('',#14587,#10496,#10497);
#8892=AXIS2_PLACEMENT_3D('',#14589,#10498,#10499);
#8893=AXIS2_PLACEMENT_3D('',#14596,#10500,#10501);
#8894=AXIS2_PLACEMENT_3D('',#14597,#10502,#10503);
#8895=AXIS2_PLACEMENT_3D('',#14604,#10504,#10505);
#8896=AXIS2_PLACEMENT_3D('',#14606,#10506,#10507);
#8897=AXIS2_PLACEMENT_3D('',#14608,#10508,#10509);
#8898=AXIS2_PLACEMENT_3D('',#14615,#10510,#10511);
#8899=AXIS2_PLACEMENT_3D('',#14621,#10512,#10513);
#8900=AXIS2_PLACEMENT_3D('',#14623,#10514,#10515);
#8901=AXIS2_PLACEMENT_3D('',#14625,#10516,#10517);
#8902=AXIS2_PLACEMENT_3D('',#14632,#10518,#10519);
#8903=AXIS2_PLACEMENT_3D('',#14633,#10520,#10521);
#8904=AXIS2_PLACEMENT_3D('',#14640,#10522,#10523);
#8905=AXIS2_PLACEMENT_3D('',#14642,#10524,#10525);
#8906=AXIS2_PLACEMENT_3D('',#14644,#10526,#10527);
#8907=AXIS2_PLACEMENT_3D('',#14651,#10528,#10529);
#8908=AXIS2_PLACEMENT_3D('',#14652,#10530,#10531);
#8909=AXIS2_PLACEMENT_3D('',#14659,#10532,#10533);
#8910=AXIS2_PLACEMENT_3D('',#14661,#10534,#10535);
#8911=AXIS2_PLACEMENT_3D('',#14663,#10536,#10537);
#8912=AXIS2_PLACEMENT_3D('',#14670,#10538,#10539);
#8913=AXIS2_PLACEMENT_3D('',#14671,#10540,#10541);
#8914=AXIS2_PLACEMENT_3D('',#14678,#10542,#10543);
#8915=AXIS2_PLACEMENT_3D('',#14680,#10544,#10545);
#8916=AXIS2_PLACEMENT_3D('',#14682,#10546,#10547);
#8917=AXIS2_PLACEMENT_3D('',#14683,#10548,#10549);
#8918=AXIS2_PLACEMENT_3D('',#14685,#10550,#10551);
#8919=AXIS2_PLACEMENT_3D('',#14687,#10552,#10553);
#8920=AXIS2_PLACEMENT_3D('',#14689,#10554,#10555);
#8921=AXIS2_PLACEMENT_3D('',#14691,#10556,#10557);
#8922=AXIS2_PLACEMENT_3D('',#14693,#10558,#10559);
#8923=AXIS2_PLACEMENT_3D('',#14695,#10560,#10561);
#8924=AXIS2_PLACEMENT_3D('',#14697,#10562,#10563);
#8925=AXIS2_PLACEMENT_3D('',#14699,#10564,#10565);
#8926=AXIS2_PLACEMENT_3D('',#14701,#10566,#10567);
#8927=AXIS2_PLACEMENT_3D('',#14703,#10568,#10569);
#8928=AXIS2_PLACEMENT_3D('',#14705,#10570,#10571);
#8929=AXIS2_PLACEMENT_3D('',#14707,#10572,#10573);
#8930=AXIS2_PLACEMENT_3D('',#14709,#10574,#10575);
#8931=AXIS2_PLACEMENT_3D('',#14711,#10576,#10577);
#8932=AXIS2_PLACEMENT_3D('',#14713,#10578,#10579);
#8933=AXIS2_PLACEMENT_3D('',#14715,#10580,#10581);
#8934=AXIS2_PLACEMENT_3D('',#14717,#10582,#10583);
#8935=AXIS2_PLACEMENT_3D('',#14719,#10584,#10585);
#8936=AXIS2_PLACEMENT_3D('',#14725,#10586,#10587);
#8937=AXIS2_PLACEMENT_3D('',#14731,#10588,#10589);
#8938=AXIS2_PLACEMENT_3D('',#14737,#10590,#10591);
#8939=AXIS2_PLACEMENT_3D('',#14738,#10592,#10593);
#8940=AXIS2_PLACEMENT_3D('',#14739,#10594,#10595);
#8941=AXIS2_PLACEMENT_3D('',#14745,#10596,#10597);
#8942=AXIS2_PLACEMENT_3D('',#14751,#10598,#10599);
#8943=AXIS2_PLACEMENT_3D('',#14757,#10600,#10601);
#8944=AXIS2_PLACEMENT_3D('',#14758,#10602,#10603);
#8945=AXIS2_PLACEMENT_3D('',#14764,#10604,#10605);
#8946=AXIS2_PLACEMENT_3D('',#14765,#10606,#10607);
#8947=AXIS2_PLACEMENT_3D('',#14771,#10608,#10609);
#8948=AXIS2_PLACEMENT_3D('',#14777,#10610,#10611);
#8949=AXIS2_PLACEMENT_3D('',#14783,#10612,#10613);
#8950=AXIS2_PLACEMENT_3D('',#14784,#10614,#10615);
#8951=AXIS2_PLACEMENT_3D('',#14790,#10616,#10617);
#8952=AXIS2_PLACEMENT_3D('',#14791,#10618,#10619);
#8953=AXIS2_PLACEMENT_3D('',#14797,#10620,#10621);
#8954=AXIS2_PLACEMENT_3D('',#14803,#10622,#10623);
#8955=AXIS2_PLACEMENT_3D('',#14809,#10624,#10625);
#8956=AXIS2_PLACEMENT_3D('',#14810,#10626,#10627);
#8957=AXIS2_PLACEMENT_3D('',#14816,#10628,#10629);
#8958=AXIS2_PLACEMENT_3D('',#14817,#10630,#10631);
#8959=AXIS2_PLACEMENT_3D('',#14823,#10632,#10633);
#8960=AXIS2_PLACEMENT_3D('',#14829,#10634,#10635);
#8961=AXIS2_PLACEMENT_3D('',#14835,#10636,#10637);
#8962=AXIS2_PLACEMENT_3D('',#14841,#10638,#10639);
#8963=AXIS2_PLACEMENT_3D('',#14842,#10640,#10641);
#8964=AXIS2_PLACEMENT_3D('',#14843,#10642,#10643);
#8965=AXIS2_PLACEMENT_3D('',#14849,#10644,#10645);
#8966=AXIS2_PLACEMENT_3D('',#14850,#10646,#10647);
#8967=AXIS2_PLACEMENT_3D('',#14856,#10648,#10649);
#8968=AXIS2_PLACEMENT_3D('',#14857,#10650,#10651);
#8969=AXIS2_PLACEMENT_3D('',#14871,#10652,#10653);
#8970=AXIS2_PLACEMENT_3D('',#14872,#10654,#10655);
#8971=AXIS2_PLACEMENT_3D('',#14874,#10656,#10657);
#8972=AXIS2_PLACEMENT_3D('',#14876,#10658,#10659);
#8973=AXIS2_PLACEMENT_3D('',#14888,#10660,#10661);
#8974=AXIS2_PLACEMENT_3D('',#14890,#10662,#10663);
#8975=AXIS2_PLACEMENT_3D('',#14896,#10664,#10665);
#8976=AXIS2_PLACEMENT_3D('',#14898,#10666,#10667);
#8977=AXIS2_PLACEMENT_3D('',#14900,#10668,#10669);
#8978=AXIS2_PLACEMENT_3D('',#14911,#10670,#10671);
#8979=AXIS2_PLACEMENT_3D('',#14913,#10672,#10673);
#8980=AXIS2_PLACEMENT_3D('',#14915,#10674,#10675);
#8981=AXIS2_PLACEMENT_3D('',#14926,#10676,#10677);
#8982=AXIS2_PLACEMENT_3D('',#14928,#10678,#10679);
#8983=AXIS2_PLACEMENT_3D('',#14930,#10680,#10681);
#8984=AXIS2_PLACEMENT_3D('',#14941,#10682,#10683);
#8985=AXIS2_PLACEMENT_3D('',#14943,#10684,#10685);
#8986=AXIS2_PLACEMENT_3D('',#14945,#10686,#10687);
#8987=AXIS2_PLACEMENT_3D('',#14951,#10688,#10689);
#8988=AXIS2_PLACEMENT_3D('',#14963,#10690,#10691);
#8989=AXIS2_PLACEMENT_3D('',#14965,#10692,#10693);
#8990=AXIS2_PLACEMENT_3D('',#14966,#10694,#10695);
#8991=AXIS2_PLACEMENT_3D('',#14968,#10696,#10697);
#8992=AXIS2_PLACEMENT_3D('',#14970,#10698,#10699);
#8993=AXIS2_PLACEMENT_3D('',#14972,#10700,#10701);
#8994=AXIS2_PLACEMENT_3D('',#14974,#10702,#10703);
#8995=AXIS2_PLACEMENT_3D('',#14976,#10704,#10705);
#8996=AXIS2_PLACEMENT_3D('',#14978,#10706,#10707);
#8997=AXIS2_PLACEMENT_3D('',#14980,#10708,#10709);
#8998=AXIS2_PLACEMENT_3D('',#14982,#10710,#10711);
#8999=AXIS2_PLACEMENT_3D('',#14984,#10712,#10713);
#9000=AXIS2_PLACEMENT_3D('',#14986,#10714,#10715);
#9001=AXIS2_PLACEMENT_3D('',#14988,#10716,#10717);
#9002=AXIS2_PLACEMENT_3D('',#14990,#10718,#10719);
#9003=AXIS2_PLACEMENT_3D('',#14992,#10720,#10721);
#9004=AXIS2_PLACEMENT_3D('',#14994,#10722,#10723);
#9005=AXIS2_PLACEMENT_3D('',#14996,#10724,#10725);
#9006=AXIS2_PLACEMENT_3D('',#14998,#10726,#10727);
#9007=AXIS2_PLACEMENT_3D('',#15000,#10728,#10729);
#9008=AXIS2_PLACEMENT_3D('',#15002,#10730,#10731);
#9009=AXIS2_PLACEMENT_3D('',#15007,#10732,#10733);
#9010=AXIS2_PLACEMENT_3D('',#15008,#10734,#10735);
#9011=AXIS2_PLACEMENT_3D('',#15009,#10736,#10737);
#9012=AXIS2_PLACEMENT_3D('',#15010,#10738,#10739);
#9013=AXIS2_PLACEMENT_3D('',#15011,#10740,#10741);
#9014=AXIS2_PLACEMENT_3D('',#15012,#10742,#10743);
#9015=AXIS2_PLACEMENT_3D('',#15013,#10744,#10745);
#9016=AXIS2_PLACEMENT_3D('',#15014,#10746,#10747);
#9017=AXIS2_PLACEMENT_3D('',#15015,#10748,#10749);
#9018=AXIS2_PLACEMENT_3D('',#15016,#10750,#10751);
#9019=AXIS2_PLACEMENT_3D('',#15017,#10752,#10753);
#9020=AXIS2_PLACEMENT_3D('',#15018,#10754,#10755);
#9021=AXIS2_PLACEMENT_3D('',#15019,#10756,#10757);
#9022=AXIS2_PLACEMENT_3D('',#15020,#10758,#10759);
#9023=AXIS2_PLACEMENT_3D('',#15021,#10760,#10761);
#9024=AXIS2_PLACEMENT_3D('',#15022,#10762,#10763);
#9025=AXIS2_PLACEMENT_3D('',#15023,#10764,#10765);
#9026=AXIS2_PLACEMENT_3D('',#15024,#10766,#10767);
#9027=AXIS2_PLACEMENT_3D('',#15025,#10768,#10769);
#9028=AXIS2_PLACEMENT_3D('',#15030,#10770,#10771);
#9029=AXIS2_PLACEMENT_3D('',#15035,#10772,#10773);
#9030=AXIS2_PLACEMENT_3D('',#15040,#10774,#10775);
#9031=AXIS2_PLACEMENT_3D('',#15045,#10776,#10777);
#9032=AXIS2_PLACEMENT_3D('',#15046,#10778,#10779);
#9033=AXIS2_PLACEMENT_3D('',#15051,#10780,#10781);
#9034=AXIS2_PLACEMENT_3D('',#15056,#10782,#10783);
#9035=AXIS2_PLACEMENT_3D('',#15061,#10784,#10785);
#9036=AXIS2_PLACEMENT_3D('',#15066,#10786,#10787);
#9037=AXIS2_PLACEMENT_3D('',#15067,#10788,#10789);
#9038=AXIS2_PLACEMENT_3D('',#15072,#10790,#10791);
#9039=AXIS2_PLACEMENT_3D('',#15077,#10792,#10793);
#9040=AXIS2_PLACEMENT_3D('',#15082,#10794,#10795);
#9041=AXIS2_PLACEMENT_3D('',#15083,#10796,#10797);
#9042=AXIS2_PLACEMENT_3D('',#15088,#10798,#10799);
#9043=AXIS2_PLACEMENT_3D('',#15093,#10800,#10801);
#9044=AXIS2_PLACEMENT_3D('',#15098,#10802,#10803);
#9045=AXIS2_PLACEMENT_3D('',#15103,#10804,#10805);
#9046=AXIS2_PLACEMENT_3D('',#15104,#10806,#10807);
#9047=AXIS2_PLACEMENT_3D('',#15109,#10808,#10809);
#9048=AXIS2_PLACEMENT_3D('',#15114,#10810,#10811);
#9049=AXIS2_PLACEMENT_3D('',#15119,#10812,#10813);
#9050=AXIS2_PLACEMENT_3D('',#15124,#10814,#10815);
#9051=AXIS2_PLACEMENT_3D('',#15125,#10816,#10817);
#9052=AXIS2_PLACEMENT_3D('',#15130,#10818,#10819);
#9053=AXIS2_PLACEMENT_3D('',#15135,#10820,#10821);
#9054=AXIS2_PLACEMENT_3D('',#15140,#10822,#10823);
#9055=AXIS2_PLACEMENT_3D('',#15145,#10824,#10825);
#9056=AXIS2_PLACEMENT_3D('',#15146,#10826,#10827);
#9057=AXIS2_PLACEMENT_3D('',#15147,#10828,#10829);
#9058=AXIS2_PLACEMENT_3D('',#15161,#10830,#10831);
#9059=AXIS2_PLACEMENT_3D('',#15162,#10832,#10833);
#9060=AXIS2_PLACEMENT_3D('',#15176,#10834,#10835);
#9061=AXIS2_PLACEMENT_3D('',#15177,#10836,#10837);
#9062=AXIS2_PLACEMENT_3D('',#15191,#10838,#10839);
#9063=AXIS2_PLACEMENT_3D('',#15192,#10840,#10841);
#9064=AXIS2_PLACEMENT_3D('',#15206,#10842,#10843);
#9065=AXIS2_PLACEMENT_3D('',#15207,#10844,#10845);
#9066=AXIS2_PLACEMENT_3D('',#15208,#10846,#10847);
#9067=AXIS2_PLACEMENT_3D('',#15210,#10848,#10849);
#9068=AXIS2_PLACEMENT_3D('',#15211,#10850,#10851);
#9069=AXIS2_PLACEMENT_3D('',#15225,#10852,#10853);
#9070=AXIS2_PLACEMENT_3D('',#15226,#10854,#10855);
#9071=AXIS2_PLACEMENT_3D('',#15234,#10856,#10857);
#9072=AXIS2_PLACEMENT_3D('',#15241,#10858,#10859);
#9073=AXIS2_PLACEMENT_3D('',#15248,#10860,#10861);
#9074=AXIS2_PLACEMENT_3D('',#15255,#10862,#10863);
#9075=AXIS2_PLACEMENT_3D('',#15262,#10864,#10865);
#9076=AXIS2_PLACEMENT_3D('',#15269,#10866,#10867);
#9077=AXIS2_PLACEMENT_3D('',#15276,#10868,#10869);
#9078=AXIS2_PLACEMENT_3D('',#15283,#10870,#10871);
#9079=AXIS2_PLACEMENT_3D('',#15290,#10872,#10873);
#9080=AXIS2_PLACEMENT_3D('',#15297,#10874,#10875);
#9081=AXIS2_PLACEMENT_3D('',#15304,#10876,#10877);
#9082=AXIS2_PLACEMENT_3D('',#15310,#10878,#10879);
#9083=AXIS2_PLACEMENT_3D('',#15312,#10880,#10881);
#9084=AXIS2_PLACEMENT_3D('',#15315,#10882,#10883);
#9085=AXIS2_PLACEMENT_3D('',#15316,#10884,#10885);
#9086=AXIS2_PLACEMENT_3D('',#15318,#10886,#10887);
#9087=AXIS2_PLACEMENT_3D('',#15320,#10888,#10889);
#9088=AXIS2_PLACEMENT_3D('',#15323,#10890,#10891);
#9089=AXIS2_PLACEMENT_3D('',#15324,#10892,#10893);
#9090=AXIS2_PLACEMENT_3D('',#15326,#10894,#10895);
#9091=AXIS2_PLACEMENT_3D('',#15327,#10896,#10897);
#9092=AXIS2_PLACEMENT_3D('',#15359,#10898,#10899);
#9093=AXIS2_PLACEMENT_3D('',#15391,#10900,#10901);
#9094=AXIS2_PLACEMENT_3D('',#15392,#10902,#10903);
#9095=AXIS2_PLACEMENT_3D('',#15457,#10904,#10905);
#9096=AXIS2_PLACEMENT_3D('',#15458,#10906,#10907);
#9097=AXIS2_PLACEMENT_3D('',#15466,#10908,#10909);
#9098=AXIS2_PLACEMENT_3D('',#15467,#10910,#10911);
#9099=AXIS2_PLACEMENT_3D('',#15478,#10912,#10913);
#9100=AXIS2_PLACEMENT_3D('',#15486,#10914,#10915);
#9101=AXIS2_PLACEMENT_3D('',#15493,#10916,#10917);
#9102=AXIS2_PLACEMENT_3D('',#15495,#10918,#10919);
#9103=AXIS2_PLACEMENT_3D('',#15496,#10920,#10921);
#9104=AXIS2_PLACEMENT_3D('',#15504,#10922,#10923);
#9105=AXIS2_PLACEMENT_3D('',#15506,#10924,#10925);
#9106=AXIS2_PLACEMENT_3D('',#15507,#10926,#10927);
#9107=AXIS2_PLACEMENT_3D('',#15508,#10928,#10929);
#9108=AXIS2_PLACEMENT_3D('',#15519,#10930,#10931);
#9109=AXIS2_PLACEMENT_3D('',#15520,#10932,#10933);
#9110=AXIS2_PLACEMENT_3D('',#15521,#10934,#10935);
#9111=AXIS2_PLACEMENT_3D('',#15529,#10936,#10937);
#9112=AXIS2_PLACEMENT_3D('',#15530,#10938,#10939);
#9113=AXIS2_PLACEMENT_3D('',#15549,#10940,#10941);
#9114=AXIS2_PLACEMENT_3D('',#15569,#10942,#10943);
#9115=AXIS2_PLACEMENT_3D('',#15583,#10944,#10945);
#9116=AXIS2_PLACEMENT_3D('',#15588,#10946,#10947);
#9117=AXIS2_PLACEMENT_3D('',#15603,#10948,#10949);
#9118=AXIS2_PLACEMENT_3D('',#15623,#10950,#10951);
#9119=AXIS2_PLACEMENT_3D('',#15637,#10952,#10953);
#9120=AXIS2_PLACEMENT_3D('',#15647,#10954,#10955);
#9121=AXIS2_PLACEMENT_3D('',#15653,#10956,#10957);
#9122=AXIS2_PLACEMENT_3D('',#15654,#10958,#10959);
#9123=AXIS2_PLACEMENT_3D('',#15655,#10960,#10961);
#9124=AXIS2_PLACEMENT_3D('',#15657,#10962,#10963);
#9125=AXIS2_PLACEMENT_3D('',#15668,#10964,#10965);
#9126=AXIS2_PLACEMENT_3D('',#15682,#10966,#10967);
#9127=AXIS2_PLACEMENT_3D('',#15687,#10968,#10969);
#9128=AXIS2_PLACEMENT_3D('',#15702,#10970,#10971);
#9129=AXIS2_PLACEMENT_3D('',#15722,#10972,#10973);
#9130=AXIS2_PLACEMENT_3D('',#15736,#10974,#10975);
#9131=AXIS2_PLACEMENT_3D('',#15741,#10976,#10977);
#9132=AXIS2_PLACEMENT_3D('',#15756,#10978,#10979);
#9133=AXIS2_PLACEMENT_3D('',#15776,#10980,#10981);
#9134=AXIS2_PLACEMENT_3D('',#15790,#10982,#10983);
#9135=AXIS2_PLACEMENT_3D('',#15795,#10984,#10985);
#9136=AXIS2_PLACEMENT_3D('',#15810,#10986,#10987);
#9137=AXIS2_PLACEMENT_3D('',#15830,#10988,#10989);
#9138=AXIS2_PLACEMENT_3D('',#15844,#10990,#10991);
#9139=AXIS2_PLACEMENT_3D('',#15845,#10992,#10993);
#9140=AXIS2_PLACEMENT_3D('',#15881,#10994,#10995);
#9141=AXIS2_PLACEMENT_3D('',#15887,#10996,#10997);
#9142=AXIS2_PLACEMENT_3D('',#15919,#10998,#10999);
#9143=AXIS2_PLACEMENT_3D('',#15924,#11000,#11001);
#9144=AXIS2_PLACEMENT_3D('',#15960,#11002,#11003);
#9145=AXIS2_PLACEMENT_3D('',#15996,#11004,#11005);
#9146=AXIS2_PLACEMENT_3D('',#16032,#11006,#11007);
#9147=AXIS2_PLACEMENT_3D('',#16068,#11008,#11009);
#9148=AXIS2_PLACEMENT_3D('',#16125,#11010,#11011);
#9149=AXIS2_PLACEMENT_3D('',#16182,#11012,#11013);
#9150=AXIS2_PLACEMENT_3D('',#16237,#11014,#11015);
#9151=AXIS2_PLACEMENT_3D('',#16294,#11016,#11017);
#9152=AXIS2_PLACEMENT_3D('',#16351,#11018,#11019);
#9153=AXIS2_PLACEMENT_3D('',#16406,#11020,#11021);
#9154=AXIS2_PLACEMENT_3D('',#16416,#11022,#11023);
#9155=AXIS2_PLACEMENT_3D('',#16426,#11024,#11025);
#9156=AXIS2_PLACEMENT_3D('',#16431,#11026,#11027);
#9157=AXIS2_PLACEMENT_3D('',#16441,#11028,#11029);
#9158=AXIS2_PLACEMENT_3D('',#16451,#11030,#11031);
#9159=AXIS2_PLACEMENT_3D('',#16456,#11032,#11033);
#9160=AXIS2_PLACEMENT_3D('',#16461,#11034,#11035);
#9161=AXIS2_PLACEMENT_3D('',#16471,#11036,#11037);
#9162=AXIS2_PLACEMENT_3D('',#16477,#11038,#11039);
#9163=AXIS2_PLACEMENT_3D('',#16478,#11040,#11041);
#9164=AXIS2_PLACEMENT_3D('',#16488,#11042,#11043);
#9165=AXIS2_PLACEMENT_3D('',#16498,#11044,#11045);
#9166=AXIS2_PLACEMENT_3D('',#16503,#11046,#11047);
#9167=AXIS2_PLACEMENT_3D('',#16513,#11048,#11049);
#9168=AXIS2_PLACEMENT_3D('',#16523,#11050,#11051);
#9169=AXIS2_PLACEMENT_3D('',#16528,#11052,#11053);
#9170=AXIS2_PLACEMENT_3D('',#16538,#11054,#11055);
#9171=AXIS2_PLACEMENT_3D('',#16548,#11056,#11057);
#9172=AXIS2_PLACEMENT_3D('',#16751,#11058,#11059);
#9173=AXIS2_PLACEMENT_3D('',#16752,#11060,#11061);
#9174=AXIS2_PLACEMENT_3D('',#16927,#11062,#11063);
#9175=AXIS2_PLACEMENT_3D('',#17126,#11064,#11065);
#9176=AXIS2_PLACEMENT_3D('',#17127,#11066,#11067);
#9177=AXIS2_PLACEMENT_3D('',#17302,#11068,#11069);
#9178=AXIS2_PLACEMENT_3D('',#17307,#11070,#11071);
#9179=AXIS2_PLACEMENT_3D('',#17506,#11072,#11073);
#9180=AXIS2_PLACEMENT_3D('',#17507,#11074,#11075);
#9181=AXIS2_PLACEMENT_3D('',#17682,#11076,#11077);
#9182=AXIS2_PLACEMENT_3D('',#17881,#11078,#11079);
#9183=AXIS2_PLACEMENT_3D('',#17882,#11080,#11081);
#9184=AXIS2_PLACEMENT_3D('',#18057,#11082,#11083);
#9185=AXIS2_PLACEMENT_3D('',#18256,#11084,#11085);
#9186=AXIS2_PLACEMENT_3D('',#18257,#11086,#11087);
#9187=AXIS2_PLACEMENT_3D('',#18432,#11088,#11089);
#9188=AXIS2_PLACEMENT_3D('',#18631,#11090,#11091);
#9189=AXIS2_PLACEMENT_3D('',#18632,#11092,#11093);
#9190=AXIS2_PLACEMENT_3D('',#18807,#11094,#11095);
#9192=DIRECTION('',(0.,0.,1.));
#9193=DIRECTION('',(1.,0.,0.));
#10098=DIRECTION('',(1.,0.,0.));
#10099=DIRECTION('',(0.,0.,-1.));
#10100=DIRECTION('',(1.,0.,0.));
#10101=DIRECTION('',(0.,0.,-1.));
#10102=DIRECTION('',(1.,0.,0.));
#10103=DIRECTION('',(0.,0.,-1.));
#10104=DIRECTION('',(1.,2.02801224290451E-16,-2.41603252256269E-16));
#10105=DIRECTION('',(-2.41603252256269E-16,0.,-1.));
#10106=DIRECTION('',(-1.,0.,0.));
#10107=DIRECTION('',(0.,0.,1.));
#10108=DIRECTION('',(-1.,0.,2.12198590438362E-17));
#10109=DIRECTION('',(2.12198590438362E-17,0.,1.));
#10110=DIRECTION('',(-1.,0.,0.));
#10111=DIRECTION('',(0.,0.,1.));
#10112=DIRECTION('',(-1.,0.,0.));
#10113=DIRECTION('',(0.,0.,1.));
#10114=DIRECTION('',(-1.,0.,0.));
#10115=DIRECTION('',(0.,0.,1.));
#10116=DIRECTION('',(-1.,0.,0.));
#10117=DIRECTION('',(0.,0.,1.));
#10118=DIRECTION('',(-1.,0.,0.));
#10119=DIRECTION('',(0.,0.,1.));
#10120=DIRECTION('',(-1.,-4.24397180875387E-17,-5.66873377313974E-17));
#10121=DIRECTION('',(-5.66873377313974E-17,0.,1.));
#10122=DIRECTION('',(1.,0.,0.));
#10123=DIRECTION('',(0.,0.,-1.));
#10124=DIRECTION('',(1.,1.03977309314787E-16,-1.08221281123575E-16));
#10125=DIRECTION('',(-1.08221281123575E-16,0.,-1.));
#10126=DIRECTION('',(1.,0.,0.));
#10127=DIRECTION('',(0.,0.,-1.));
#10128=DIRECTION('',(1.,0.,0.));
#10129=DIRECTION('',(0.,0.,-1.));
#10130=DIRECTION('',(1.,0.,0.));
#10131=DIRECTION('',(0.,0.,-1.));
#10132=DIRECTION('',(1.,0.,0.));
#10133=DIRECTION('',(0.,0.,-1.));
#10134=DIRECTION('',(1.,0.,0.));
#10135=DIRECTION('',(0.,0.,-1.));
#10136=DIRECTION('',(1.,5.72936194184529E-17,-1.22772041610769E-16));
#10137=DIRECTION('',(-1.22772041610769E-16,0.,-1.));
#10138=DIRECTION('',(-1.,0.,0.));
#10139=DIRECTION('',(0.,0.,1.));
#10140=DIRECTION('',(-1.,6.82066897833321E-18,2.57669716961208E-18));
#10141=DIRECTION('',(-6.82066897833321E-18,-1.,0.));
#10142=DIRECTION('',(-1.,0.,0.));
#10143=DIRECTION('',(0.,0.,1.));
#10144=DIRECTION('',(-1.,0.,0.));
#10145=DIRECTION('',(0.,0.,1.));
#10146=DIRECTION('',(-1.,0.,0.));
#10147=DIRECTION('',(0.,0.,1.));
#10148=DIRECTION('',(-1.,0.,0.));
#10149=DIRECTION('',(0.,0.,1.));
#10150=DIRECTION('',(-1.,0.,0.));
#10151=DIRECTION('',(0.,0.,1.));
#10152=DIRECTION('',(-1.,7.12380982182306E-18,-2.27355632612368E-18));
#10153=DIRECTION('',(-7.12380982182306E-18,-1.,0.));
#10154=DIRECTION('',(1.,0.,0.));
#10155=DIRECTION('',(0.,0.,-1.));
#10156=DIRECTION('',(1.,2.91015209743734E-17,4.57742673659912E-17));
#10157=DIRECTION('',(4.57742673659912E-17,0.,-1.));
#10158=DIRECTION('',(1.,0.,0.));
#10159=DIRECTION('',(0.,0.,-1.));
#10160=DIRECTION('',(1.,0.,0.));
#10161=DIRECTION('',(0.,0.,-1.));
#10162=DIRECTION('',(1.,0.,0.));
#10163=DIRECTION('',(0.,0.,-1.));
#10164=DIRECTION('',(1.,0.,0.));
#10165=DIRECTION('',(0.,0.,-1.));
#10166=DIRECTION('',(1.,0.,0.));
#10167=DIRECTION('',(0.,0.,-1.));
#10168=DIRECTION('',(1.,7.27538024359589E-17,-9.63987882277241E-17));
#10169=DIRECTION('',(-9.63987882277241E-17,0.,-1.));
#10170=DIRECTION('',(-1.,0.,0.));
#10171=DIRECTION('',(0.,0.,1.));
#10172=DIRECTION('',(-1.,-6.66909855658537E-18,-5.75967602618571E-18));
#10173=DIRECTION('',(6.66909855658537E-18,-1.,0.));
#10174=DIRECTION('',(-1.,0.,0.));
#10175=DIRECTION('',(0.,0.,1.));
#10176=DIRECTION('',(-1.,0.,0.));
#10177=DIRECTION('',(0.,0.,1.));
#10178=DIRECTION('',(-1.,0.,0.));
#10179=DIRECTION('',(0.,0.,1.));
#10180=DIRECTION('',(-1.,0.,0.));
#10181=DIRECTION('',(0.,0.,1.));
#10182=DIRECTION('',(-1.,0.,0.));
#10183=DIRECTION('',(0.,0.,1.));
#10184=DIRECTION('',(-1.,2.5009119587355E-17,1.22772041610769E-17));
#10185=DIRECTION('',(-2.5009119587355E-17,-1.,0.));
#10186=DIRECTION('',(1.,0.,0.));
#10187=DIRECTION('',(0.,0.,-1.));
#10188=DIRECTION('',(1.,2.4205796352152E-16,-2.29326048095192E-16));
#10189=DIRECTION('',(-2.4205796352152E-16,1.,0.));
#10190=DIRECTION('',(1.,0.,0.));
#10191=DIRECTION('',(0.,0.,-1.));
#10192=DIRECTION('',(1.,0.,0.));
#10193=DIRECTION('',(0.,0.,-1.));
#10194=DIRECTION('',(1.,0.,0.));
#10195=DIRECTION('',(0.,0.,-1.));
#10196=DIRECTION('',(1.,0.,0.));
#10197=DIRECTION('',(0.,0.,-1.));
#10198=DIRECTION('',(1.,0.,0.));
#10199=DIRECTION('',(0.,0.,-1.));
#10200=DIRECTION('',(1.,1.58886509469999E-16,-1.7842870047433E-16));
#10201=DIRECTION('',(-1.7842870047433E-16,0.,-1.));
#10202=DIRECTION('',(-1.,0.,0.));
#10203=DIRECTION('',(0.,0.,1.));
#10204=DIRECTION('',(1.,0.,0.));
#10205=DIRECTION('',(0.,0.,-1.));
#10206=DIRECTION('',(1.,0.,0.));
#10207=DIRECTION('',(0.,0.,-1.));
#10208=DIRECTION('',(-1.,0.,0.));
#10209=DIRECTION('',(0.,0.,1.));
#10210=DIRECTION('',(-1.,0.,0.));
#10211=DIRECTION('',(0.,0.,1.));
#10212=DIRECTION('',(1.,0.,0.));
#10213=DIRECTION('',(0.,0.,-1.));
#10214=DIRECTION('',(1.,0.,0.));
#10215=DIRECTION('',(0.,0.,-1.));
#10216=DIRECTION('',(-1.,-5.92083225297793E-17,-6.5638185609928E-17));
#10217=DIRECTION('',(-6.5638185609928E-17,0.,1.));
#10218=DIRECTION('',(-1.,0.,0.));
#10219=DIRECTION('',(0.,0.,1.));
#10220=DIRECTION('',(1.,2.03904353819831E-16,-2.22341986202179E-16));
#10221=DIRECTION('',(-2.22341986202179E-16,0.,-1.));
#10222=DIRECTION('',(1.,0.,0.));
#10223=DIRECTION('',(0.,0.,-1.));
#10224=DIRECTION('',(-1.,0.,0.));
#10225=DIRECTION('',(0.,0.,1.));
#10226=DIRECTION('',(-1.,0.,0.));
#10227=DIRECTION('',(0.,0.,1.));
#10228=DIRECTION('',(1.,0.,0.));
#10229=DIRECTION('',(0.,0.,-1.));
#10230=DIRECTION('',(-1.,0.,0.));
#10231=DIRECTION('',(0.,0.,1.));
#10232=DIRECTION('',(-1.,-8.42579974462088E-17,-9.46212805545689E-17));
#10233=DIRECTION('',(-9.46212805545689E-17,0.,1.));
#10234=DIRECTION('',(1.,-1.27665164684106E-12,-1.01285822605064E-16));
#10235=DIRECTION('',(1.27665164684106E-12,1.,0.));
#10236=DIRECTION('',(1.,0.,0.));
#10237=DIRECTION('',(0.,0.,-1.));
#10238=DIRECTION('',(1.,0.,0.));
#10239=DIRECTION('',(0.,0.,-1.));
#10240=DIRECTION('',(1.,0.,0.));
#10241=DIRECTION('',(0.,0.,-1.));
#10242=DIRECTION('',(1.,0.,0.));
#10243=DIRECTION('',(0.,0.,-1.));
#10244=DIRECTION('',(1.,0.,0.));
#10245=DIRECTION('',(0.,0.,-1.));
#10246=DIRECTION('',(1.,0.,0.));
#10247=DIRECTION('',(0.,0.,-1.));
#10248=DIRECTION('',(1.,0.,0.));
#10249=DIRECTION('',(0.,0.,-1.));
#10250=DIRECTION('',(1.,0.,0.));
#10251=DIRECTION('',(0.,0.,-1.));
#10252=DIRECTION('',(1.,0.,0.));
#10253=DIRECTION('',(0.,0.,-1.));
#10254=DIRECTION('',(1.,0.,0.));
#10255=DIRECTION('',(0.,0.,-1.));
#10256=DIRECTION('',(1.,0.,0.));
#10257=DIRECTION('',(0.,0.,-1.));
#10258=DIRECTION('',(1.,0.,0.));
#10259=DIRECTION('',(0.,0.,-1.));
#10260=DIRECTION('',(1.,0.,0.));
#10261=DIRECTION('',(0.,0.,-1.));
#10262=DIRECTION('',(1.,0.,0.));
#10263=DIRECTION('',(0.,0.,-1.));
#10264=DIRECTION('',(1.,0.,0.));
#10265=DIRECTION('',(0.,0.,-1.));
#10266=DIRECTION('',(1.,0.,0.));
#10267=DIRECTION('',(0.,0.,-1.));
#10268=DIRECTION('',(1.,0.,0.));
#10269=DIRECTION('',(0.,0.,-1.));
#10270=DIRECTION('',(1.,0.,0.));
#10271=DIRECTION('',(0.,0.,-1.));
#10272=DIRECTION('',(-1.,0.,0.));
#10273=DIRECTION('',(0.,0.,1.));
#10274=DIRECTION('',(1.,0.,0.));
#10275=DIRECTION('',(0.,0.,-1.));
#10276=DIRECTION('',(1.,0.,0.));
#10277=DIRECTION('',(0.,0.,-1.));
#10278=DIRECTION('',(1.,0.,0.));
#10279=DIRECTION('',(0.,0.,-1.));
#10280=DIRECTION('',(1.,0.,0.));
#10281=DIRECTION('',(0.,0.,-1.));
#10282=DIRECTION('',(1.,0.,0.));
#10283=DIRECTION('',(0.,0.,-1.));
#10284=DIRECTION('',(1.,0.,0.));
#10285=DIRECTION('',(0.,0.,-1.));
#10286=DIRECTION('',(1.,0.,0.));
#10287=DIRECTION('',(0.,0.,-1.));
#10288=DIRECTION('',(1.,0.,0.));
#10289=DIRECTION('',(0.,0.,-1.));
#10290=DIRECTION('',(1.,0.,0.));
#10291=DIRECTION('',(0.,0.,-1.));
#10292=DIRECTION('',(1.,0.,0.));
#10293=DIRECTION('',(0.,0.,-1.));
#10294=DIRECTION('',(1.,0.,0.));
#10295=DIRECTION('',(0.,0.,-1.));
#10296=DIRECTION('',(1.,0.,0.));
#10297=DIRECTION('',(0.,0.,-1.));
#10298=DIRECTION('',(1.,0.,0.));
#10299=DIRECTION('',(0.,0.,-1.));
#10300=DIRECTION('',(1.,0.,0.));
#10301=DIRECTION('',(0.,0.,-1.));
#10302=DIRECTION('',(1.,0.,0.));
#10303=DIRECTION('',(0.,0.,-1.));
#10304=DIRECTION('',(1.,0.,0.));
#10305=DIRECTION('',(0.,0.,-1.));
#10306=DIRECTION('',(1.,0.,0.));
#10307=DIRECTION('',(0.,0.,-1.));
#10308=DIRECTION('',(1.,0.,0.));
#10309=DIRECTION('',(0.,0.,-1.));
#10310=DIRECTION('',(1.,0.,0.));
#10311=DIRECTION('',(0.,0.,-1.));
#10312=DIRECTION('',(1.,0.,0.));
#10313=DIRECTION('',(0.,0.,-1.));
#10314=DIRECTION('',(1.,0.,0.));
#10315=DIRECTION('',(0.,0.,-1.));
#10316=DIRECTION('',(1.,0.,0.));
#10317=DIRECTION('',(0.,0.,-1.));
#10318=DIRECTION('',(1.,0.,0.));
#10319=DIRECTION('',(0.,0.,-1.));
#10320=DIRECTION('',(1.,0.,0.));
#10321=DIRECTION('',(0.,0.,-1.));
#10322=DIRECTION('',(1.,0.,0.));
#10323=DIRECTION('',(0.,0.,-1.));
#10324=DIRECTION('',(1.,0.,0.));
#10325=DIRECTION('',(0.,0.,-1.));
#10326=DIRECTION('',(1.,0.,0.));
#10327=DIRECTION('',(0.,0.,-1.));
#10328=DIRECTION('',(1.,0.,0.));
#10329=DIRECTION('',(0.,0.,-1.));
#10330=DIRECTION('',(1.,0.,0.));
#10331=DIRECTION('',(0.,0.,-1.));
#10332=DIRECTION('',(1.,0.,0.));
#10333=DIRECTION('',(0.,0.,-1.));
#10334=DIRECTION('',(1.,0.,0.));
#10335=DIRECTION('',(0.,0.,-1.));
#10336=DIRECTION('',(1.,0.,0.));
#10337=DIRECTION('',(0.,0.,-1.));
#10338=DIRECTION('',(1.,0.,0.));
#10339=DIRECTION('',(0.,0.,-1.));
#10340=DIRECTION('',(1.,0.,0.));
#10341=DIRECTION('',(0.,0.,-1.));
#10342=DIRECTION('',(1.,0.,0.));
#10343=DIRECTION('',(0.,0.,-1.));
#10344=DIRECTION('',(1.,0.,0.));
#10345=DIRECTION('',(0.,0.,-1.));
#10346=DIRECTION('',(1.,0.,0.));
#10347=DIRECTION('',(0.,0.,-1.));
#10348=DIRECTION('',(1.,-1.27665164684106E-12,-1.01285822605064E-16));
#10349=DIRECTION('',(1.27665164684106E-12,1.,0.));
#10350=DIRECTION('',(1.,1.27662876208615E-12,9.94459735806396E-17));
#10351=DIRECTION('',(-1.27662876208615E-12,1.,0.));
#10352=DIRECTION('',(1.,0.,0.));
#10353=DIRECTION('',(0.,0.,-1.));
#10354=DIRECTION('',(1.,0.,0.));
#10355=DIRECTION('',(0.,0.,-1.));
#10356=DIRECTION('',(1.,1.00478788398415E-16,-1.1970342952697E-16));
#10357=DIRECTION('',(-1.1970342952697E-16,0.,-1.));
#10358=DIRECTION('',(1.,1.27681490610412E-12,3.06367665504718E-17));
#10359=DIRECTION('',(-1.27681490610412E-12,1.,0.));
#10360=DIRECTION('',(-1.,0.,0.));
#10361=DIRECTION('',(0.,0.,1.));
#10362=DIRECTION('',(-1.,0.,0.));
#10363=DIRECTION('',(0.,0.,1.));
#10364=DIRECTION('',(-1.,0.,0.));
#10365=DIRECTION('',(0.,0.,1.));
#10366=DIRECTION('',(1.,0.,0.));
#10367=DIRECTION('',(0.,0.,-1.));
#10368=DIRECTION('',(1.,0.,0.));
#10369=DIRECTION('',(0.,0.,-1.));
#10370=DIRECTION('',(-1.,0.,0.));
#10371=DIRECTION('',(0.,0.,1.));
#10372=DIRECTION('',(1.,1.27681490610412E-12,3.06367665504718E-17));
#10373=DIRECTION('',(-1.27681490610412E-12,1.,0.));
#10374=DIRECTION('',(1.,0.,0.));
#10375=DIRECTION('',(0.,0.,-1.));
#10376=DIRECTION('',(1.,0.,0.));
#10377=DIRECTION('',(0.,0.,-1.));
#10378=DIRECTION('',(1.,0.,0.));
#10379=DIRECTION('',(0.,0.,-1.));
#10380=DIRECTION('',(1.,0.,0.));
#10381=DIRECTION('',(0.,0.,-1.));
#10382=DIRECTION('',(-1.,3.16611816286098E-16,2.99958470908511E-16));
#10383=DIRECTION('',(-3.16611816286098E-16,-1.,0.));
#10384=DIRECTION('',(1.,0.,0.));
#10385=DIRECTION('',(0.,0.,-1.));
#10386=DIRECTION('',(1.,-6.10766397547714E-11,6.58357325455797E-17));
#10387=DIRECTION('',(6.10766397547714E-11,1.,0.));
#10388=DIRECTION('',(-1.,0.,-2.21547530017009E-16));
#10389=DIRECTION('',(-2.21547530017009E-16,0.,1.));
#10390=DIRECTION('',(1.,6.10765954034213E-11,-7.15867759341588E-17));
#10391=DIRECTION('',(-6.10765954034213E-11,1.,0.));
#10392=DIRECTION('',(1.,0.,0.));
#10393=DIRECTION('',(0.,0.,-1.));
#10394=DIRECTION('',(1.,4.34750133448528E-12,-7.07356447213086E-17));
#10395=DIRECTION('',(-4.34750133448528E-12,1.,0.));
#10396=DIRECTION('',(-1.,0.,-2.21547530017009E-16));
#10397=DIRECTION('',(-2.21547530017009E-16,0.,1.));
#10398=DIRECTION('',(-1.,0.,-2.21547530017009E-16));
#10399=DIRECTION('',(-2.21547530017009E-16,0.,1.));
#10400=DIRECTION('',(-1.,0.,-2.21547530017009E-16));
#10401=DIRECTION('',(-2.21547530017009E-16,0.,1.));
#10402=DIRECTION('',(1.,4.34750133448528E-12,-7.07356447213086E-17));
#10403=DIRECTION('',(-4.34750133448528E-12,1.,0.));
#10404=DIRECTION('',(1.,4.34750133448528E-12,-7.07356447213086E-17));
#10405=DIRECTION('',(-4.34750133448528E-12,1.,0.));
#10406=DIRECTION('',(1.,1.75950681255562E-16,1.77784902179881E-11));
#10407=DIRECTION('',(1.77784902179881E-11,0.,-1.));
#10408=DIRECTION('',(-1.,0.,0.));
#10409=DIRECTION('',(0.,0.,1.));
#10410=DIRECTION('',(0.094639757655587,0.973920700489943,0.206208111935661));
#10411=DIRECTION('',(0.,-0.2071378324481,0.978311769513534));
#10412=DIRECTION('',(1.,8.1117015446827E-11,-1.3991198231814E-10));
#10413=DIRECTION('',(-1.3991198231814E-10,0.,-1.));
#10414=DIRECTION('',(1.,8.1117015446827E-11,-1.3991198231814E-10));
#10415=DIRECTION('',(-1.3991198231814E-10,0.,-1.));
#10416=DIRECTION('',(-0.0946398168959535,0.665538133586411,0.740339312612951));
#10417=DIRECTION('',(0.,-0.743677248769676,0.668538816870319));
#10418=DIRECTION('',(1.,-4.95011636935677E-10,2.85369859870056E-10));
#10419=DIRECTION('',(4.95011636935677E-10,1.,0.));
#10420=DIRECTION('',(0.0946397575924438,0.308378887082395,0.946544123791737));
#10421=DIRECTION('',(0.,-0.9508117613661,0.309769260011214));
#10422=DIRECTION('',(1.,1.17652320289254E-10,4.87112968899379E-16));
#10423=DIRECTION('',(-1.17652320289254E-10,1.,0.));
#10424=DIRECTION('',(1.,1.17652320289254E-10,4.87112968899379E-16));
#10425=DIRECTION('',(-1.17652320289254E-10,1.,0.));
#10426=DIRECTION('',(-0.0946398171021046,-0.308383585244705,0.946542587193256));
#10427=DIRECTION('',(0.,-0.950810223242973,-0.30977398111631));
#10428=DIRECTION('',(1.,-4.95007884417356E-10,-2.85368119247311E-10));
#10429=DIRECTION('',(4.95007884417356E-10,1.,0.));
#10430=DIRECTION('',(0.0946397579762018,-0.66554181379473,0.740336011754816));
#10431=DIRECTION('',(0.,-0.743673928844786,-0.668542509909848));
#10432=DIRECTION('',(1.,8.11172698461387E-11,1.39913973791465E-10));
#10433=DIRECTION('',(1.39913973791465E-10,0.,-1.));
#10434=DIRECTION('',(1.,8.11172698461387E-11,1.39913973791465E-10));
#10435=DIRECTION('',(1.39913973791465E-10,0.,-1.));
#10436=DIRECTION('',(0.094639816908078,0.973921718912833,-0.206203274672052));
#10437=DIRECTION('',(0.,0.20713297454698,0.978312798063748));
#10438=DIRECTION('',(1.,-4.74005497252645E-11,-6.27882181535306E-10));
#10439=DIRECTION('',(-6.27882181535306E-10,0.,-1.));
#10440=DIRECTION('',(-4.739727861225E-11,1.,-8.7405760717612E-11));
#10441=DIRECTION('',(0.,8.7405760717612E-11,1.));
#10442=DIRECTION('',(1.,4.73972785573744E-11,-6.27826053903067E-10));
#10443=DIRECTION('',(-6.27826053903067E-10,0.,-1.));
#10444=DIRECTION('',(-0.0946397577561541,0.973920700463518,0.206208112014312));
#10445=DIRECTION('',(0.,-0.207137832529095,0.978311769496385));
#10446=DIRECTION('',(1.,-8.11134369730464E-11,1.39906722256238E-10));
#10447=DIRECTION('',(1.39906722256238E-10,0.,-1.));
#10448=DIRECTION('',(1.,-8.11134369730464E-11,1.39906722256238E-10));
#10449=DIRECTION('',(1.39906722256238E-10,0.,-1.));
#10450=DIRECTION('',(0.094639817014141,0.665538133630341,0.740339312558352));
#10451=DIRECTION('',(0.,-0.743677248723224,0.668538816921992));
#10452=DIRECTION('',(1.,4.95010500146808E-10,-2.8536921183499E-10));
#10453=DIRECTION('',(-4.95010500146808E-10,1.,0.));
#10454=DIRECTION('',(-0.094639757574348,0.308378887070613,0.946544123797385));
#10455=DIRECTION('',(0.,-0.95081176137013,0.309769259998844));
#10456=DIRECTION('',(1.,-1.17647616855165E-10,2.02965890778723E-16));
#10457=DIRECTION('',(1.17647616855165E-10,1.,0.));
#10458=DIRECTION('',(1.,-1.17647616855165E-10,2.02965890778723E-16));
#10459=DIRECTION('',(1.17647616855165E-10,1.,0.));
#10460=DIRECTION('',(0.0946398171021004,-0.308383585244707,0.946542587193255));
#10461=DIRECTION('',(0.,-0.950810223242972,-0.309773981116312));
#10462=DIRECTION('',(1.,4.95008651459005E-10,2.85368745562457E-10));
#10463=DIRECTION('',(-4.95008651459005E-10,1.,0.));
#10464=DIRECTION('',(-0.094639757976208,-0.665541813794729,0.740336011754816));
#10465=DIRECTION('',(0.,-0.743673928844787,-0.668542509909848));
#10466=DIRECTION('',(1.,-8.11137982698219E-11,-1.3990738019364E-10));
#10467=DIRECTION('',(-1.3990738019364E-10,0.,-1.));
#10468=DIRECTION('',(1.,-8.11137982698219E-11,-1.3990738019364E-10));
#10469=DIRECTION('',(-1.3990738019364E-10,0.,-1.));
#10470=DIRECTION('',(-0.0946398169083375,0.973921718912779,-0.206203274672188));
#10471=DIRECTION('',(0.,0.207132974547121,0.978312798063718));
#10472=DIRECTION('',(1.,-6.96086070235072E-17,7.71679127636215E-17));
#10473=DIRECTION('',(7.71679127636215E-17,0.,-1.));
#10474=DIRECTION('',(1.,3.14873594454048E-12,1.4723392451601E-16));
#10475=DIRECTION('',(-3.14873594454048E-12,1.,0.));
#10476=DIRECTION('',(-1.,0.,0.));
#10477=DIRECTION('',(0.,0.,1.));
#10478=DIRECTION('',(-1.,0.,0.));
#10479=DIRECTION('',(0.,0.,1.));
#10480=DIRECTION('',(-1.,0.,0.));
#10481=DIRECTION('',(0.,0.,1.));
#10482=DIRECTION('',(-1.,0.,0.));
#10483=DIRECTION('',(0.,0.,1.));
#10484=DIRECTION('',(-1.,0.,0.));
#10485=DIRECTION('',(0.,0.,1.));
#10486=DIRECTION('',(-1.,1.1377082542873E-17,-4.88125653654854E-19));
#10487=DIRECTION('',(-1.1377082542873E-17,-1.,0.));
#10488=DIRECTION('',(1.,-1.27684531196004E-12,-3.07678549182519E-17));
#10489=DIRECTION('',(1.27684531196004E-12,1.,0.));
#10490=DIRECTION('',(-1.,0.,0.));
#10491=DIRECTION('',(0.,0.,1.));
#10492=DIRECTION('',(-1.,0.,0.));
#10493=DIRECTION('',(0.,0.,1.));
#10494=DIRECTION('',(-1.,0.,0.));
#10495=DIRECTION('',(0.,0.,1.));
#10496=DIRECTION('',(-1.,0.,0.));
#10497=DIRECTION('',(0.,0.,1.));
#10498=DIRECTION('',(-1.,0.,0.));
#10499=DIRECTION('',(0.,0.,1.));
#10500=DIRECTION('',(-1.,0.,0.));
#10501=DIRECTION('',(0.,0.,1.));
#10502=DIRECTION('',(-1.,0.,0.));
#10503=DIRECTION('',(0.,0.,1.));
#10504=DIRECTION('',(-1.,0.,0.));
#10505=DIRECTION('',(0.,0.,1.));
#10506=DIRECTION('',(-1.,0.,0.));
#10507=DIRECTION('',(0.,0.,1.));
#10508=DIRECTION('',(-1.,0.,0.));
#10509=DIRECTION('',(0.,0.,1.));
#10510=DIRECTION('',(-1.,0.,0.));
#10511=DIRECTION('',(0.,0.,1.));
#10512=DIRECTION('',(-1.,0.,0.));
#10513=DIRECTION('',(0.,0.,1.));
#10514=DIRECTION('',(-1.,0.,0.));
#10515=DIRECTION('',(0.,0.,1.));
#10516=DIRECTION('',(-1.,0.,0.));
#10517=DIRECTION('',(0.,0.,1.));
#10518=DIRECTION('',(-1.,0.,0.));
#10519=DIRECTION('',(0.,0.,1.));
#10520=DIRECTION('',(-1.,0.,0.));
#10521=DIRECTION('',(0.,0.,1.));
#10522=DIRECTION('',(-1.,0.,0.));
#10523=DIRECTION('',(0.,0.,1.));
#10524=DIRECTION('',(-1.,0.,0.));
#10525=DIRECTION('',(0.,0.,1.));
#10526=DIRECTION('',(-1.,0.,0.));
#10527=DIRECTION('',(0.,0.,1.));
#10528=DIRECTION('',(-1.,0.,0.));
#10529=DIRECTION('',(0.,0.,1.));
#10530=DIRECTION('',(-1.,0.,0.));
#10531=DIRECTION('',(0.,0.,1.));
#10532=DIRECTION('',(-1.,0.,0.));
#10533=DIRECTION('',(0.,0.,1.));
#10534=DIRECTION('',(-1.,0.,0.));
#10535=DIRECTION('',(0.,0.,1.));
#10536=DIRECTION('',(-1.,0.,0.));
#10537=DIRECTION('',(0.,0.,1.));
#10538=DIRECTION('',(-1.,0.,0.));
#10539=DIRECTION('',(0.,0.,1.));
#10540=DIRECTION('',(-1.,0.,0.));
#10541=DIRECTION('',(0.,0.,1.));
#10542=DIRECTION('',(-1.,0.,0.));
#10543=DIRECTION('',(0.,0.,1.));
#10544=DIRECTION('',(-1.,0.,0.));
#10545=DIRECTION('',(0.,0.,1.));
#10546=DIRECTION('',(-1.,0.,0.));
#10547=DIRECTION('',(0.,0.,1.));
#10548=DIRECTION('',(1.,0.,0.));
#10549=DIRECTION('',(0.,0.,-1.));
#10550=DIRECTION('',(1.,0.,0.));
#10551=DIRECTION('',(0.,0.,-1.));
#10552=DIRECTION('',(1.,0.,0.));
#10553=DIRECTION('',(0.,0.,-1.));
#10554=DIRECTION('',(1.,0.,0.));
#10555=DIRECTION('',(0.,0.,-1.));
#10556=DIRECTION('',(1.,0.,0.));
#10557=DIRECTION('',(0.,0.,-1.));
#10558=DIRECTION('',(1.,0.,0.));
#10559=DIRECTION('',(0.,0.,-1.));
#10560=DIRECTION('',(1.,0.,0.));
#10561=DIRECTION('',(0.,0.,-1.));
#10562=DIRECTION('',(1.,0.,0.));
#10563=DIRECTION('',(0.,0.,-1.));
#10564=DIRECTION('',(1.,0.,0.));
#10565=DIRECTION('',(0.,0.,-1.));
#10566=DIRECTION('',(1.,0.,0.));
#10567=DIRECTION('',(0.,0.,-1.));
#10568=DIRECTION('',(1.,0.,0.));
#10569=DIRECTION('',(0.,0.,-1.));
#10570=DIRECTION('',(1.,0.,0.));
#10571=DIRECTION('',(0.,0.,-1.));
#10572=DIRECTION('',(1.,0.,0.));
#10573=DIRECTION('',(0.,0.,-1.));
#10574=DIRECTION('',(1.,0.,0.));
#10575=DIRECTION('',(0.,0.,-1.));
#10576=DIRECTION('',(1.,0.,0.));
#10577=DIRECTION('',(0.,0.,-1.));
#10578=DIRECTION('',(1.,0.,0.));
#10579=DIRECTION('',(0.,0.,-1.));
#10580=DIRECTION('',(1.,0.,0.));
#10581=DIRECTION('',(0.,0.,-1.));
#10582=DIRECTION('',(1.,0.,0.));
#10583=DIRECTION('',(0.,0.,-1.));
#10584=DIRECTION('',(-1.,0.,0.));
#10585=DIRECTION('',(0.,0.,1.));
#10586=DIRECTION('',(-1.,0.,0.));
#10587=DIRECTION('',(0.,0.,1.));
#10588=DIRECTION('',(-1.,0.,0.));
#10589=DIRECTION('',(0.,0.,1.));
#10590=DIRECTION('',(-1.,0.,0.));
#10591=DIRECTION('',(0.,0.,1.));
#10592=DIRECTION('',(-1.,0.,0.));
#10593=DIRECTION('',(0.,0.,1.));
#10594=DIRECTION('',(-1.,0.,0.));
#10595=DIRECTION('',(0.,0.,1.));
#10596=DIRECTION('',(-1.,0.,0.));
#10597=DIRECTION('',(0.,0.,1.));
#10598=DIRECTION('',(-1.,0.,0.));
#10599=DIRECTION('',(0.,0.,1.));
#10600=DIRECTION('',(-1.,0.,0.));
#10601=DIRECTION('',(0.,0.,1.));
#10602=DIRECTION('',(-1.,0.,0.));
#10603=DIRECTION('',(0.,0.,1.));
#10604=DIRECTION('',(-1.,0.,0.));
#10605=DIRECTION('',(0.,0.,1.));
#10606=DIRECTION('',(-1.,0.,0.));
#10607=DIRECTION('',(0.,0.,1.));
#10608=DIRECTION('',(-1.,0.,0.));
#10609=DIRECTION('',(0.,0.,1.));
#10610=DIRECTION('',(-1.,0.,0.));
#10611=DIRECTION('',(0.,0.,1.));
#10612=DIRECTION('',(-1.,0.,0.));
#10613=DIRECTION('',(0.,0.,1.));
#10614=DIRECTION('',(-1.,0.,0.));
#10615=DIRECTION('',(0.,0.,1.));
#10616=DIRECTION('',(-1.,0.,0.));
#10617=DIRECTION('',(0.,0.,1.));
#10618=DIRECTION('',(-1.,0.,0.));
#10619=DIRECTION('',(0.,0.,1.));
#10620=DIRECTION('',(-1.,0.,0.));
#10621=DIRECTION('',(0.,0.,1.));
#10622=DIRECTION('',(-1.,0.,0.));
#10623=DIRECTION('',(0.,0.,1.));
#10624=DIRECTION('',(-1.,0.,0.));
#10625=DIRECTION('',(0.,0.,1.));
#10626=DIRECTION('',(-1.,0.,0.));
#10627=DIRECTION('',(0.,0.,1.));
#10628=DIRECTION('',(-1.,0.,0.));
#10629=DIRECTION('',(0.,0.,1.));
#10630=DIRECTION('',(-1.,0.,0.));
#10631=DIRECTION('',(0.,0.,1.));
#10632=DIRECTION('',(-1.,0.,0.));
#10633=DIRECTION('',(0.,0.,1.));
#10634=DIRECTION('',(-1.,0.,0.));
#10635=DIRECTION('',(0.,0.,1.));
#10636=DIRECTION('',(-1.,0.,0.));
#10637=DIRECTION('',(0.,0.,1.));
#10638=DIRECTION('',(-1.,0.,0.));
#10639=DIRECTION('',(0.,0.,1.));
#10640=DIRECTION('',(-1.,0.,0.));
#10641=DIRECTION('',(0.,0.,1.));
#10642=DIRECTION('',(-1.,0.,0.));
#10643=DIRECTION('',(0.,0.,1.));
#10644=DIRECTION('',(-1.,0.,0.));
#10645=DIRECTION('',(0.,0.,1.));
#10646=DIRECTION('',(-1.,0.,0.));
#10647=DIRECTION('',(0.,0.,1.));
#10648=DIRECTION('',(1.,3.14873594454048E-12,1.4723392451601E-16));
#10649=DIRECTION('',(-3.14873594454048E-12,1.,0.));
#10650=DIRECTION('',(1.,-3.14875882929539E-12,-1.47379671248562E-16));
#10651=DIRECTION('',(3.14875882929539E-12,1.,0.));
#10652=DIRECTION('',(1.,-1.30292001398524E-17,1.10016012708286E-17));
#10653=DIRECTION('',(1.30292001398524E-17,1.,0.));
#10654=DIRECTION('',(1.,1.276699066795E-12,-1.73643216677854E-17));
#10655=DIRECTION('',(-1.276699066795E-12,1.,0.));
#10656=DIRECTION('',(1.,-3.40640980091026E-12,4.52734012877115E-17));
#10657=DIRECTION('',(3.40640980091026E-12,1.,0.));
#10658=DIRECTION('',(-1.,0.,0.));
#10659=DIRECTION('',(0.,0.,1.));
#10660=DIRECTION('',(-1.,0.,0.));
#10661=DIRECTION('',(0.,0.,1.));
#10662=DIRECTION('',(-1.,0.,0.));
#10663=DIRECTION('',(0.,0.,1.));
#10664=DIRECTION('',(-1.,0.,0.));
#10665=DIRECTION('',(0.,0.,1.));
#10666=DIRECTION('',(-1.,0.,0.));
#10667=DIRECTION('',(0.,0.,1.));
#10668=DIRECTION('',(-1.,0.,0.));
#10669=DIRECTION('',(0.,0.,1.));
#10670=DIRECTION('',(-1.,0.,0.));
#10671=DIRECTION('',(0.,0.,1.));
#10672=DIRECTION('',(-1.,0.,0.));
#10673=DIRECTION('',(0.,0.,1.));
#10674=DIRECTION('',(-1.,0.,0.));
#10675=DIRECTION('',(0.,0.,1.));
#10676=DIRECTION('',(-1.,0.,0.));
#10677=DIRECTION('',(0.,0.,1.));
#10678=DIRECTION('',(-1.,0.,0.));
#10679=DIRECTION('',(0.,0.,1.));
#10680=DIRECTION('',(-1.,0.,0.));
#10681=DIRECTION('',(0.,0.,1.));
#10682=DIRECTION('',(-1.,0.,0.));
#10683=DIRECTION('',(0.,0.,1.));
#10684=DIRECTION('',(-1.,0.,0.));
#10685=DIRECTION('',(0.,0.,1.));
#10686=DIRECTION('',(-1.,0.,0.));
#10687=DIRECTION('',(0.,0.,1.));
#10688=DIRECTION('',(-1.,0.,0.));
#10689=DIRECTION('',(0.,0.,1.));
#10690=DIRECTION('',(-1.,0.,0.));
#10691=DIRECTION('',(0.,0.,1.));
#10692=DIRECTION('',(-1.,0.,0.));
#10693=DIRECTION('',(0.,0.,1.));
#10694=DIRECTION('',(1.,0.,0.));
#10695=DIRECTION('',(0.,0.,-1.));
#10696=DIRECTION('',(1.,0.,0.));
#10697=DIRECTION('',(0.,0.,-1.));
#10698=DIRECTION('',(1.,0.,0.));
#10699=DIRECTION('',(0.,0.,-1.));
#10700=DIRECTION('',(1.,0.,0.));
#10701=DIRECTION('',(0.,0.,-1.));
#10702=DIRECTION('',(1.,0.,0.));
#10703=DIRECTION('',(0.,0.,-1.));
#10704=DIRECTION('',(1.,0.,0.));
#10705=DIRECTION('',(0.,0.,-1.));
#10706=DIRECTION('',(1.,0.,0.));
#10707=DIRECTION('',(0.,0.,-1.));
#10708=DIRECTION('',(1.,0.,0.));
#10709=DIRECTION('',(0.,0.,-1.));
#10710=DIRECTION('',(1.,0.,0.));
#10711=DIRECTION('',(0.,0.,-1.));
#10712=DIRECTION('',(1.,0.,0.));
#10713=DIRECTION('',(0.,0.,-1.));
#10714=DIRECTION('',(1.,0.,0.));
#10715=DIRECTION('',(0.,0.,-1.));
#10716=DIRECTION('',(1.,0.,0.));
#10717=DIRECTION('',(0.,0.,-1.));
#10718=DIRECTION('',(1.,0.,0.));
#10719=DIRECTION('',(0.,0.,-1.));
#10720=DIRECTION('',(1.,0.,0.));
#10721=DIRECTION('',(0.,0.,-1.));
#10722=DIRECTION('',(1.,0.,0.));
#10723=DIRECTION('',(0.,0.,-1.));
#10724=DIRECTION('',(1.,0.,0.));
#10725=DIRECTION('',(0.,0.,-1.));
#10726=DIRECTION('',(1.,0.,0.));
#10727=DIRECTION('',(0.,0.,-1.));
#10728=DIRECTION('',(1.,0.,0.));
#10729=DIRECTION('',(0.,0.,-1.));
#10730=DIRECTION('',(-1.49022658150495E-16,0.707106781186547,0.707106781186548));
#10731=DIRECTION('',(0.,-0.707106781186548,0.707106781186547));
#10732=DIRECTION('',(1.,0.,0.));
#10733=DIRECTION('',(0.,0.,-1.));
#10734=DIRECTION('',(1.,0.,0.));
#10735=DIRECTION('',(0.,0.,-1.));
#10736=DIRECTION('',(1.,0.,0.));
#10737=DIRECTION('',(0.,0.,-1.));
#10738=DIRECTION('',(1.,0.,0.));
#10739=DIRECTION('',(0.,0.,-1.));
#10740=DIRECTION('',(1.,0.,0.));
#10741=DIRECTION('',(0.,0.,-1.));
#10742=DIRECTION('',(1.,0.,0.));
#10743=DIRECTION('',(0.,0.,-1.));
#10744=DIRECTION('',(1.,0.,0.));
#10745=DIRECTION('',(0.,0.,-1.));
#10746=DIRECTION('',(1.,0.,0.));
#10747=DIRECTION('',(0.,0.,-1.));
#10748=DIRECTION('',(1.,0.,0.));
#10749=DIRECTION('',(0.,0.,-1.));
#10750=DIRECTION('',(1.,0.,0.));
#10751=DIRECTION('',(0.,0.,-1.));
#10752=DIRECTION('',(1.,0.,0.));
#10753=DIRECTION('',(0.,0.,-1.));
#10754=DIRECTION('',(1.,0.,0.));
#10755=DIRECTION('',(0.,0.,-1.));
#10756=DIRECTION('',(1.,0.,0.));
#10757=DIRECTION('',(0.,0.,-1.));
#10758=DIRECTION('',(1.,0.,0.));
#10759=DIRECTION('',(0.,0.,-1.));
#10760=DIRECTION('',(1.,0.,0.));
#10761=DIRECTION('',(0.,0.,-1.));
#10762=DIRECTION('',(1.,0.,0.));
#10763=DIRECTION('',(0.,0.,-1.));
#10764=DIRECTION('',(1.,0.,0.));
#10765=DIRECTION('',(0.,0.,-1.));
#10766=DIRECTION('',(1.,0.,0.));
#10767=DIRECTION('',(0.,0.,-1.));
#10768=DIRECTION('',(-1.06924232066722E-17,-0.965925826292715,0.258819045088912));
#10769=DIRECTION('',(0.,-0.258819045088912,-0.965925826292715));
#10770=DIRECTION('',(-1.,0.,0.));
#10771=DIRECTION('',(0.,0.,1.));
#10772=DIRECTION('',(-1.,0.,0.));
#10773=DIRECTION('',(0.,0.,1.));
#10774=DIRECTION('',(-1.,0.,0.));
#10775=DIRECTION('',(0.,0.,1.));
#10776=DIRECTION('',(3.82310332191275E-18,-0.258819045142856,-0.965925826278261));
#10777=DIRECTION('',(0.,0.965925826278261,-0.258819045142856));
#10778=DIRECTION('',(-4.22965962259824E-18,-0.258819045142856,0.965925826278261));
#10779=DIRECTION('',(0.,-0.965925826278261,-0.258819045142856));
#10780=DIRECTION('',(-1.,0.,0.));
#10781=DIRECTION('',(0.,0.,1.));
#10782=DIRECTION('',(-1.,0.,0.));
#10783=DIRECTION('',(0.,0.,1.));
#10784=DIRECTION('',(-1.,0.,0.));
#10785=DIRECTION('',(0.,0.,1.));
#10786=DIRECTION('',(3.46708220525981E-18,-0.965925826292715,-0.258819045088912));
#10787=DIRECTION('',(0.,0.258819045088912,-0.965925826292715));
#10788=DIRECTION('',(-1.,0.,0.));
#10789=DIRECTION('',(0.,0.,1.));
#10790=DIRECTION('',(-1.,0.,0.));
#10791=DIRECTION('',(0.,0.,1.));
#10792=DIRECTION('',(-1.,0.,0.));
#10793=DIRECTION('',(0.,0.,1.));
#10794=DIRECTION('',(-1.37281479023486E-16,-0.707106781186547,0.707106781186548));
#10795=DIRECTION('',(0.,-0.707106781186548,-0.707106781186547));
#10796=DIRECTION('',(-1.06924232066722E-17,0.965925826292715,-0.258819045088912));
#10797=DIRECTION('',(0.,0.258819045088912,0.965925826292715));
#10798=DIRECTION('',(-1.,0.,0.));
#10799=DIRECTION('',(0.,0.,1.));
#10800=DIRECTION('',(-1.,0.,0.));
#10801=DIRECTION('',(0.,0.,1.));
#10802=DIRECTION('',(-1.,0.,0.));
#10803=DIRECTION('',(0.,0.,1.));
#10804=DIRECTION('',(3.82310332191275E-18,0.258819045142856,0.965925826278261));
#10805=DIRECTION('',(0.,-0.965925826278261,0.258819045142856));
#10806=DIRECTION('',(-4.22965962259824E-18,0.258819045142856,-0.965925826278261));
#10807=DIRECTION('',(0.,0.965925826278261,0.258819045142856));
#10808=DIRECTION('',(-1.,0.,0.));
#10809=DIRECTION('',(0.,0.,1.));
#10810=DIRECTION('',(-1.,0.,0.));
#10811=DIRECTION('',(0.,0.,1.));
#10812=DIRECTION('',(-1.,0.,0.));
#10813=DIRECTION('',(0.,0.,1.));
#10814=DIRECTION('',(3.46708220525981E-18,0.965925826292715,0.258819045088912));
#10815=DIRECTION('',(0.,-0.258819045088912,0.965925826292715));
#10816=DIRECTION('',(-1.49022658150495E-16,-0.707106781186547,-0.707106781186548));
#10817=DIRECTION('',(0.,0.707106781186548,-0.707106781186547));
#10818=DIRECTION('',(-1.,0.,0.));
#10819=DIRECTION('',(0.,0.,1.));
#10820=DIRECTION('',(-1.,0.,0.));
#10821=DIRECTION('',(0.,0.,1.));
#10822=DIRECTION('',(-1.,0.,0.));
#10823=DIRECTION('',(0.,0.,1.));
#10824=DIRECTION('',(-1.37281479023486E-16,0.707106781186547,-0.707106781186548));
#10825=DIRECTION('',(0.,0.707106781186548,0.707106781186547));
#10826=DIRECTION('',(1.,-1.27684531196004E-12,-3.07678549182519E-17));
#10827=DIRECTION('',(1.27684531196004E-12,1.,0.));
#10828=DIRECTION('',(1.,1.27682242720514E-12,2.98634303535282E-17));
#10829=DIRECTION('',(-1.27682242720514E-12,1.,0.));
#10830=DIRECTION('',(-1.,0.,0.));
#10831=DIRECTION('',(0.,0.,1.));
#10832=DIRECTION('',(-1.,0.,0.));
#10833=DIRECTION('',(0.,0.,1.));
#10834=DIRECTION('',(1.,-3.40640980091026E-12,4.52734012877115E-17));
#10835=DIRECTION('',(3.40640980091026E-12,1.,0.));
#10836=DIRECTION('',(-1.,0.,-2.21547530017009E-16));
#10837=DIRECTION('',(-2.21547530017009E-16,0.,1.));
#10838=DIRECTION('',(1.,1.276699066795E-12,-1.73643216677854E-17));
#10839=DIRECTION('',(-1.276699066795E-12,1.,0.));
#10840=DIRECTION('',(1.,-1.27672195154991E-12,1.17909395293212E-17));
#10841=DIRECTION('',(1.27672195154991E-12,1.,0.));
#10842=DIRECTION('',(-1.,0.,0.));
#10843=DIRECTION('',(0.,0.,1.));
#10844=DIRECTION('',(1.,3.40637471308767E-12,-2.04641749438355E-16));
#10845=DIRECTION('',(-3.40637471308767E-12,1.,0.));
#10846=DIRECTION('',(1.,3.40637471308767E-12,-2.04641749438355E-16));
#10847=DIRECTION('',(-3.40637471308767E-12,1.,0.));
#10848=DIRECTION('',(-1.,0.,-2.21547530017009E-16));
#10849=DIRECTION('',(-2.21547530017009E-16,0.,1.));
#10850=DIRECTION('',(-1.,0.,-2.21547530017009E-16));
#10851=DIRECTION('',(-2.21547530017009E-16,0.,1.));
#10852=DIRECTION('',(1.,-1.3591203195553E-17,3.38801252705614E-16));
#10853=DIRECTION('',(3.38801252705614E-16,0.,-1.));
#10854=DIRECTION('',(-1.,0.,0.));
#10855=DIRECTION('',(0.,0.,1.));
#10856=DIRECTION('',(1.,8.2405080686935E-11,-2.00999949487554E-10));
#10857=DIRECTION('',(-2.00999949487554E-10,0.,-1.));
#10858=DIRECTION('',(-1.,0.,0.));
#10859=DIRECTION('',(0.,0.,1.));
#10860=DIRECTION('',(1.,-8.24036101933253E-11,-2.00996350865422E-10));
#10861=DIRECTION('',(-2.00996350865422E-10,0.,-1.));
#10862=DIRECTION('',(-1.,0.,0.));
#10863=DIRECTION('',(0.,0.,1.));
#10864=DIRECTION('',(1.,-2.76226059390704E-10,9.08894019300185E-12));
#10865=DIRECTION('',(2.76226059390704E-10,1.,0.));
#10866=DIRECTION('',(-1.,0.,0.));
#10867=DIRECTION('',(0.,0.,1.));
#10868=DIRECTION('',(1.,-8.2415399410689E-11,2.0101199886441E-10));
#10869=DIRECTION('',(2.0101199886441E-10,0.,-1.));
#10870=DIRECTION('',(-1.,0.,0.));
#10871=DIRECTION('',(0.,0.,1.));
#10872=DIRECTION('',(1.,8.2377328281477E-11,2.00955368657685E-10));
#10873=DIRECTION('',(2.00955368657685E-10,0.,-1.));
#10874=DIRECTION('',(-1.,0.,0.));
#10875=DIRECTION('',(0.,0.,1.));
#10876=DIRECTION('',(1.,2.29382598029866E-10,3.48009873429896E-15));
#10877=DIRECTION('',(-2.29382598029866E-10,1.,0.));
#10878=DIRECTION('',(1.,-1.7553543294653E-16,2.21353907080645E-11));
#10879=DIRECTION('',(2.21353907080645E-11,0.,-1.));
#10880=DIRECTION('',(1.,-2.27117491928019E-11,-1.42033068007457E-15));
#10881=DIRECTION('',(2.27117491928019E-11,1.,0.));
#10882=DIRECTION('',(1.,2.27106160850224E-11,1.38950894359215E-15));
#10883=DIRECTION('',(-2.27106160850224E-11,1.,0.));
#10884=DIRECTION('',(1.,-3.69789685377355E-16,-2.21363853286448E-11));
#10885=DIRECTION('',(-2.21363853286448E-11,0.,-1.));
#10886=DIRECTION('',(1.,-7.05960696451627E-16,-2.21365946134359E-11));
#10887=DIRECTION('',(-2.21365946134359E-11,0.,-1.));
#10888=DIRECTION('',(1.,-2.27106389697773E-11,-1.43717553673992E-15));
#10889=DIRECTION('',(2.27106389697773E-11,1.,0.));
#10890=DIRECTION('',(1.,2.27103940404174E-11,1.44727788746658E-15));
#10891=DIRECTION('',(-2.27103940404174E-11,1.,0.));
#10892=DIRECTION('',(1.,-2.61658203503867E-15,2.2135315939631E-11));
#10893=DIRECTION('',(2.2135315939631E-11,0.,-1.));
#10894=DIRECTION('',(1.,-2.02663347171933E-11,-4.93824078287254E-17));
#10895=DIRECTION('',(2.02663347171933E-11,1.,0.));
#10896=DIRECTION('',(2.02663118324384E-11,-1.,-1.31076765045751E-12));
#10897=DIRECTION('',(1.,2.02663118324384E-11,0.));
#10898=DIRECTION('',(-1.,0.,-9.35772871761781E-16));
#10899=DIRECTION('',(-9.35772871761781E-16,0.,1.));
#10900=DIRECTION('',(-2.02663118324384E-11,1.,-2.64105976331828E-12));
#10901=DIRECTION('',(-1.,-2.02663118324384E-11,0.));
#10902=DIRECTION('',(1.,2.02663118324384E-11,4.37485396368513E-17));
#10903=DIRECTION('',(-2.02663118324384E-11,1.,0.));
#10904=DIRECTION('',(1.,-2.61658203503867E-15,2.2135315939631E-11));
#10905=DIRECTION('',(2.2135315939631E-11,0.,-1.));
#10906=DIRECTION('',(1.,-2.61658203503867E-15,2.2135315939631E-11));
#10907=DIRECTION('',(2.2135315939631E-11,0.,-1.));
#10908=DIRECTION('',(1.,2.27103940404174E-11,1.44727788746658E-15));
#10909=DIRECTION('',(-2.27103940404174E-11,1.,0.));
#10910=DIRECTION('',(1.,2.27103940404174E-11,1.44727788746658E-15));
#10911=DIRECTION('',(-2.27103940404174E-11,1.,0.));
#10912=DIRECTION('',(1.,-2.27106389697773E-11,-1.43717553673992E-15));
#10913=DIRECTION('',(2.27106389697773E-11,1.,0.));
#10914=DIRECTION('',(1.,-7.05960696451627E-16,-2.21365946134359E-11));
#10915=DIRECTION('',(-2.21365946134359E-11,0.,-1.));
#10916=DIRECTION('',(-1.,0.,0.));
#10917=DIRECTION('',(0.,0.,1.));
#10918=DIRECTION('',(1.,-7.05960696451627E-16,-2.21365946134359E-11));
#10919=DIRECTION('',(-2.21365946134359E-11,0.,-1.));
#10920=DIRECTION('',(1.,-3.69789685377355E-16,-2.21363853286448E-11));
#10921=DIRECTION('',(-2.21363853286448E-11,0.,-1.));
#10922=DIRECTION('',(-1.,0.,0.));
#10923=DIRECTION('',(0.,0.,1.));
#10924=DIRECTION('',(1.,-3.69789685377355E-16,-2.21363853286448E-11));
#10925=DIRECTION('',(-2.21363853286448E-11,0.,-1.));
#10926=DIRECTION('',(1.,2.27106160850224E-11,1.38950894359215E-15));
#10927=DIRECTION('',(-2.27106160850224E-11,1.,0.));
#10928=DIRECTION('',(1.,2.27106160850224E-11,1.38950894359215E-15));
#10929=DIRECTION('',(-2.27106160850224E-11,1.,0.));
#10930=DIRECTION('',(1.,-2.27117491928019E-11,-1.42033068007457E-15));
#10931=DIRECTION('',(2.27117491928019E-11,1.,0.));
#10932=DIRECTION('',(1.,-2.27117491928019E-11,-1.42033068007457E-15));
#10933=DIRECTION('',(2.27117491928019E-11,1.,0.));
#10934=DIRECTION('',(1.,-1.7553543294653E-16,2.21353907080645E-11));
#10935=DIRECTION('',(2.21353907080645E-11,0.,-1.));
#10936=DIRECTION('',(1.,-1.7553543294653E-16,2.21353907080645E-11));
#10937=DIRECTION('',(2.21353907080645E-11,0.,-1.));
#10938=DIRECTION('',(-3.57254169227789E-17,0.965925826285055,0.258819045117498));
#10939=DIRECTION('',(0.,-0.258819045117498,0.965925826285055));
#10940=DIRECTION('',(1.,8.2405080686935E-11,-2.00999949487554E-10));
#10941=DIRECTION('',(-2.00999949487554E-10,0.,-1.));
#10942=DIRECTION('',(-4.02472961092684E-18,-0.707106781124562,-0.707106781248533));
#10943=DIRECTION('',(0.,0.707106781248533,-0.707106781124562));
#10944=DIRECTION('',(-1.,0.,0.));
#10945=DIRECTION('',(0.,0.,1.));
#10946=DIRECTION('',(-1.17645942476586E-17,0.707106781124562,-0.707106781248533));
#10947=DIRECTION('',(0.,0.707106781248533,0.707106781124562));
#10948=DIRECTION('',(1.,-8.24036101933253E-11,-2.00996350865422E-10));
#10949=DIRECTION('',(-2.00996350865422E-10,0.,-1.));
#10950=DIRECTION('',(-3.26901987961688E-17,-0.965925826285055,0.258819045117498));
#10951=DIRECTION('',(0.,-0.258819045117498,-0.965925826285055));
#10952=DIRECTION('',(-1.,0.,0.));
#10953=DIRECTION('',(0.,0.,1.));
#10954=DIRECTION('',(0.,0.965925826289012,-0.258819045102731));
#10955=DIRECTION('',(0.,0.258819045102731,0.965925826289012));
#10956=DIRECTION('',(0.,0.965925826289012,-0.258819045102731));
#10957=DIRECTION('',(0.,0.258819045102731,0.965925826289012));
#10958=DIRECTION('',(1.,-2.76226059390704E-10,9.08894019300185E-12));
#10959=DIRECTION('',(2.76226059390704E-10,1.,0.));
#10960=DIRECTION('',(3.50383095897164E-11,0.0940884775756427,-0.995563839433463));
#10961=DIRECTION('',(0.,0.995563839433463,0.0940884775756427));
#10962=DIRECTION('',(1.,-2.76226059390704E-10,9.08894019300185E-12));
#10963=DIRECTION('',(2.76226059390704E-10,1.,0.));
#10964=DIRECTION('',(5.40788131399233E-18,-0.258819045117497,0.965925826285055));
#10965=DIRECTION('',(0.,-0.965925826285055,-0.258819045117497));
#10966=DIRECTION('',(-1.,0.,0.));
#10967=DIRECTION('',(0.,0.,1.));
#10968=DIRECTION('',(-3.57254169227789E-17,-0.965925826285055,-0.258819045117498));
#10969=DIRECTION('',(0.,0.258819045117498,-0.965925826285055));
#10970=DIRECTION('',(1.,-8.2415399410689E-11,2.0101199886441E-10));
#10971=DIRECTION('',(2.0101199886441E-10,0.,-1.));
#10972=DIRECTION('',(-4.02472961092684E-18,0.707106781124562,0.707106781248533));
#10973=DIRECTION('',(0.,-0.707106781248533,0.707106781124562));
#10974=DIRECTION('',(-1.,0.,0.));
#10975=DIRECTION('',(0.,0.,1.));
#10976=DIRECTION('',(-1.17645942476586E-17,-0.707106781124562,0.707106781248533));
#10977=DIRECTION('',(0.,-0.707106781248533,-0.707106781124562));
#10978=DIRECTION('',(1.,8.2377328281477E-11,2.00955368657685E-10));
#10979=DIRECTION('',(2.00955368657685E-10,0.,-1.));
#10980=DIRECTION('',(-3.26901987961688E-17,0.965925826285055,-0.258819045117498));
#10981=DIRECTION('',(0.,0.258819045117498,0.965925826285055));
#10982=DIRECTION('',(-1.,0.,0.));
#10983=DIRECTION('',(0.,0.,1.));
#10984=DIRECTION('',(-3.65658732528797E-18,0.258819045117497,0.965925826285055));
#10985=DIRECTION('',(0.,-0.965925826285055,0.258819045117497));
#10986=DIRECTION('',(1.,2.29382598029866E-10,3.48009873429896E-15));
#10987=DIRECTION('',(-2.29382598029866E-10,1.,0.));
#10988=DIRECTION('',(5.40788131399233E-18,0.258819045117497,-0.965925826285055));
#10989=DIRECTION('',(0.,0.965925826285055,0.258819045117497));
#10990=DIRECTION('',(-1.,0.,0.));
#10991=DIRECTION('',(0.,0.,1.));
#10992=DIRECTION('',(-1.,0.,-9.35772871761781E-16));
#10993=DIRECTION('',(-9.35772871761781E-16,0.,1.));
#10994=DIRECTION('',(-1.,0.,-9.35772871761781E-16));
#10995=DIRECTION('',(-9.35772871761781E-16,0.,1.));
#10996=DIRECTION('',(-1.,0.,-9.35772871761781E-16));
#10997=DIRECTION('',(-9.35772871761781E-16,0.,1.));
#10998=DIRECTION('',(-2.24403093282293E-19,-0.258819045117497,-0.965925826285055));
#10999=DIRECTION('',(0.,0.965925826285055,-0.258819045117497));
#11000=DIRECTION('',(-1.,0.,-9.35772871761781E-16));
#11001=DIRECTION('',(-9.35772871761781E-16,0.,1.));
#11002=DIRECTION('',(-1.,0.,-9.35772871761781E-16));
#11003=DIRECTION('',(-9.35772871761781E-16,0.,1.));
#11004=DIRECTION('',(-1.,0.,-9.35772871761781E-16));
#11005=DIRECTION('',(-9.35772871761781E-16,0.,1.));
#11006=DIRECTION('',(-1.,0.,-9.35772871761781E-16));
#11007=DIRECTION('',(-9.35772871761781E-16,0.,1.));
#11008=DIRECTION('',(-1.,0.,0.));
#11009=DIRECTION('',(0.,0.,1.));
#11010=DIRECTION('',(-1.,0.,0.));
#11011=DIRECTION('',(0.,0.,1.));
#11012=DIRECTION('',(-1.,0.,0.));
#11013=DIRECTION('',(0.,0.,1.));
#11014=DIRECTION('',(-1.,0.,0.));
#11015=DIRECTION('',(0.,0.,1.));
#11016=DIRECTION('',(-1.,0.,0.));
#11017=DIRECTION('',(0.,0.,1.));
#11018=DIRECTION('',(-1.,0.,0.));
#11019=DIRECTION('',(0.,0.,1.));
#11020=DIRECTION('',(-1.,0.,0.));
#11021=DIRECTION('',(0.,0.,1.));
#11022=DIRECTION('',(-1.,0.,0.));
#11023=DIRECTION('',(0.,0.,1.));
#11024=DIRECTION('',(-1.,0.,0.));
#11025=DIRECTION('',(0.,0.,1.));
#11026=DIRECTION('',(-1.,0.,0.));
#11027=DIRECTION('',(0.,0.,1.));
#11028=DIRECTION('',(-1.,0.,0.));
#11029=DIRECTION('',(0.,0.,1.));
#11030=DIRECTION('',(-1.,0.,0.));
#11031=DIRECTION('',(0.,0.,1.));
#11032=DIRECTION('',(-1.,0.,0.));
#11033=DIRECTION('',(0.,0.,1.));
#11034=DIRECTION('',(-1.,0.,0.));
#11035=DIRECTION('',(0.,0.,1.));
#11036=DIRECTION('',(-1.,0.,0.));
#11037=DIRECTION('',(0.,0.,1.));
#11038=DIRECTION('',(-1.,0.,0.));
#11039=DIRECTION('',(0.,0.,1.));
#11040=DIRECTION('',(-1.,0.,0.));
#11041=DIRECTION('',(0.,0.,1.));
#11042=DIRECTION('',(-1.,0.,0.));
#11043=DIRECTION('',(0.,0.,1.));
#11044=DIRECTION('',(-1.,0.,0.));
#11045=DIRECTION('',(0.,0.,1.));
#11046=DIRECTION('',(-1.,0.,0.));
#11047=DIRECTION('',(0.,0.,1.));
#11048=DIRECTION('',(-1.,0.,0.));
#11049=DIRECTION('',(0.,0.,1.));
#11050=DIRECTION('',(-1.,0.,0.));
#11051=DIRECTION('',(0.,0.,1.));
#11052=DIRECTION('',(-1.,0.,0.));
#11053=DIRECTION('',(0.,0.,1.));
#11054=DIRECTION('',(-1.,0.,0.));
#11055=DIRECTION('',(0.,0.,1.));
#11056=DIRECTION('',(-1.,0.,0.));
#11057=DIRECTION('',(0.,0.,1.));
#11058=DIRECTION('',(0.478873989006926,-0.264308029790248,0.83715050501149));
#11059=DIRECTION('',(-1.22147662529582E-10,-0.953600747871024,-0.301074099948542));
#11060=DIRECTION('',(0.497389500059933,-0.242860918363956,0.83283987630369));
#11061=DIRECTION('',(2.92636285103872E-10,0.960015711522541,0.279946126299096));
#11062=DIRECTION('',(1.,5.40052508211967E-11,-5.18934386003978E-11));
#11063=DIRECTION('',(-5.40052508211967E-11,1.,0.));
#11064=DIRECTION('',(0.478873988871033,-0.857147619266543,0.189677783539462));
#11065=DIRECTION('',(6.25680064193633E-10,-0.216062553694835,-0.976379522978061));
#11066=DIRECTION('',(0.497389497976556,-0.842690951126057,0.206096211010516));
#11067=DIRECTION('',(6.54476473210955E-10,0.237567395974056,0.971371058025771));
#11068=DIRECTION('',(1.,6.16564683748603E-10,-4.61139617844463E-15));
#11069=DIRECTION('',(-6.16564683748603E-10,1.,0.));
#11070=DIRECTION('',(-1.,0.,0.));
#11071=DIRECTION('',(0.,0.,1.));
#11072=DIRECTION('',(0.478873986714286,-0.592839591697574,-0.647472720169908));
#11073=DIRECTION('',(1.77654187437559E-9,0.737538191925152,-0.675305423828195));
#11074=DIRECTION('',(0.497389497799453,-0.599830031033446,-0.626743664785871));
#11075=DIRECTION('',(4.46702859689783E-10,-0.72244831369777,0.691424930151675));
#11076=DIRECTION('',(1.,5.40194019363879E-11,5.19075653119709E-11));
#11077=DIRECTION('',(-5.40194019363879E-11,1.,0.));
#11078=DIRECTION('',(0.478873989006939,0.264308029790259,-0.837150505011479));
#11079=DIRECTION('',(-1.22170792175962E-10,0.95360074787102,0.301074099948553));
#11080=DIRECTION('',(0.497389500059914,0.242860918363982,-0.832839876303695));
#11081=DIRECTION('',(2.92636285103876E-10,-0.960015711522533,-0.279946126299123));
#11082=DIRECTION('',(1.,-5.40325554069528E-11,5.19325882603181E-11));
#11083=DIRECTION('',(5.40325554069528E-11,1.,0.));
#11084=DIRECTION('',(0.478873988871033,0.857147619266543,-0.189677783539462));
#11085=DIRECTION('',(6.25680064193633E-10,0.216062553694835,0.976379522978061));
#11086=DIRECTION('',(0.497389497976556,0.842690951126057,-0.206096211010516));
#11087=DIRECTION('',(6.54476473210955E-10,-0.237567395974056,-0.971371058025771));
#11088=DIRECTION('',(1.,-6.16664743242366E-10,3.37120347294801E-15));
#11089=DIRECTION('',(6.16664743242366E-10,1.,0.));
#11090=DIRECTION('',(0.478873986714286,0.592839591697574,0.647472720169908));
#11091=DIRECTION('',(1.77654187437559E-9,-0.737538191925152,0.675305423828195));
#11092=DIRECTION('',(0.497389497799486,0.599830031033462,0.626743664785828));
#11093=DIRECTION('',(4.46656600397107E-10,0.722448313697753,-0.691424930151693));
#11094=DIRECTION('',(1.,-5.40666679703652E-11,-5.19980441369468E-11));
#11095=DIRECTION('',(5.40666679703652E-11,1.,0.));
#11098=CARTESIAN_POINT('',(0.,0.,0.));
#13701=CARTESIAN_POINT('',(0.035,0.,0.));
#13702=CARTESIAN_POINT('',(0.039,0.,0.));
#13703=CARTESIAN_POINT('',(0.039,0.,-0.016));
#13704=CARTESIAN_POINT('',(0.0385,0.,0.));
#13705=CARTESIAN_POINT('',(0.0385,0.,-0.016));
#13706=CARTESIAN_POINT('',(0.039,2.27769192395755E-17,1.36175792864179E-18));
#13707=CARTESIAN_POINT('',(0.039,0.,0.));
#13708=CARTESIAN_POINT('',(0.039,0.,0.01635));
#13709=CARTESIAN_POINT('',(0.0385,2.27769192395755E-17,-1.36175792864179E-18));
#13710=CARTESIAN_POINT('',(0.0385,0.,0.));
#13711=CARTESIAN_POINT('',(0.0385,0.,0.01635));
#13712=CARTESIAN_POINT('',(-2.34971638048196E-35,0.,0.));
#13713=CARTESIAN_POINT('',(0.0395,0.,0.));
#13714=CARTESIAN_POINT('',(0.0395,0.,0.01635));
#13715=CARTESIAN_POINT('',(-1.59983634253706E-35,0.,0.));
#13716=CARTESIAN_POINT('',(0.038,0.,0.));
#13717=CARTESIAN_POINT('',(0.038,0.,0.01635));
#13718=CARTESIAN_POINT('',(0.0395,2.27769192395755E-17,-1.36175792864179E-18));
#13719=CARTESIAN_POINT('',(0.0395,0.,0.));
#13720=CARTESIAN_POINT('',(0.0395,0.,-0.016));
#13721=CARTESIAN_POINT('',(0.038,2.27769192395755E-17,1.36175792864179E-18));
#13722=CARTESIAN_POINT('',(0.038,0.,0.));
#13723=CARTESIAN_POINT('',(0.038,0.,-0.016));
#13724=CARTESIAN_POINT('',(0.035,0.,0.));
#13725=CARTESIAN_POINT('',(0.04,0.,0.));
#13726=CARTESIAN_POINT('',(0.04,0.,-0.016));
#13727=CARTESIAN_POINT('',(0.035,0.,0.));
#13728=CARTESIAN_POINT('',(0.0375,0.,0.));
#13729=CARTESIAN_POINT('',(0.0375,0.,-0.016));
#13730=CARTESIAN_POINT('',(0.04,2.27769192395755E-17,1.36175792864179E-18));
#13731=CARTESIAN_POINT('',(0.04,0.,0.));
#13732=CARTESIAN_POINT('',(0.04,0.,0.01635));
#13733=CARTESIAN_POINT('',(0.0375,2.27769192395755E-17,-1.36175792864179E-18));
#13734=CARTESIAN_POINT('',(0.0375,0.,0.));
#13735=CARTESIAN_POINT('',(0.0375,0.,0.01635));
#13736=CARTESIAN_POINT('',(3.30786158221799E-36,0.,0.));
#13737=CARTESIAN_POINT('',(0.0405,0.,0.));
#13738=CARTESIAN_POINT('',(0.0405,0.,0.01635));
#13739=CARTESIAN_POINT('',(-1.05348069718484E-35,0.,0.));
#13740=CARTESIAN_POINT('',(0.037,0.,0.));
#13741=CARTESIAN_POINT('',(0.037,0.,0.01635));
#13742=CARTESIAN_POINT('',(0.0405,2.27769192395755E-17,-1.36175792864179E-18));
#13743=CARTESIAN_POINT('',(0.0405,0.,0.));
#13744=CARTESIAN_POINT('',(0.0405,0.,-0.016));
#13745=CARTESIAN_POINT('',(0.037,2.27769192395755E-17,1.36175792864179E-18));
#13746=CARTESIAN_POINT('',(0.037,0.,0.));
#13747=CARTESIAN_POINT('',(0.037,0.,-0.016));
#13748=CARTESIAN_POINT('',(0.035,0.,0.));
#13749=CARTESIAN_POINT('',(0.041,0.,0.));
#13750=CARTESIAN_POINT('',(0.041,0.,-0.016));
#13751=CARTESIAN_POINT('',(0.035,0.,0.));
#13752=CARTESIAN_POINT('',(0.0365,0.,0.));
#13753=CARTESIAN_POINT('',(0.0365,0.,-0.016));
#13754=CARTESIAN_POINT('',(0.041,2.27769192395755E-17,1.36175792864179E-18));
#13755=CARTESIAN_POINT('',(0.041,0.,0.));
#13756=CARTESIAN_POINT('',(0.041,0.,0.01635));
#13757=CARTESIAN_POINT('',(0.0365,2.27769192395755E-17,-1.36175792864179E-18));
#13758=CARTESIAN_POINT('',(0.0365,0.,0.));
#13759=CARTESIAN_POINT('',(0.0365,0.,0.01635));
#13760=CARTESIAN_POINT('',(-4.19093679253767E-36,0.,0.));
#13761=CARTESIAN_POINT('',(0.0415,0.,0.));
#13762=CARTESIAN_POINT('',(0.0415,0.,0.01635));
#13763=CARTESIAN_POINT('',(-3.03600664661662E-36,0.,0.));
#13764=CARTESIAN_POINT('',(0.036,0.,0.));
#13765=CARTESIAN_POINT('',(0.036,0.,0.01635));
#13766=CARTESIAN_POINT('',(0.0415,2.27769192395755E-17,-1.36175792864179E-18));
#13767=CARTESIAN_POINT('',(0.0415,0.,0.));
#13768=CARTESIAN_POINT('',(0.0415,0.,-0.016));
#13769=CARTESIAN_POINT('',(0.036,2.27769192395755E-17,1.36175792864179E-18));
#13770=CARTESIAN_POINT('',(0.036,0.,0.));
#13771=CARTESIAN_POINT('',(0.036,0.,-0.016));
#13772=CARTESIAN_POINT('',(0.035,0.,0.));
#13773=CARTESIAN_POINT('',(0.042,0.,0.));
#13774=CARTESIAN_POINT('',(0.042,0.,-0.016));
#13775=CARTESIAN_POINT('',(0.035,0.,0.));
#13776=CARTESIAN_POINT('',(0.035,0.,0.));
#13777=CARTESIAN_POINT('',(0.035,0.,-0.016));
#13778=CARTESIAN_POINT('',(0.042,-3.07046055247895E-18,0.));
#13779=CARTESIAN_POINT('',(0.042,0.,0.));
#13780=CARTESIAN_POINT('',(0.042,0.,0.0175));
#13781=CARTESIAN_POINT('',(0.035,-3.98986399474666E-19,1.35308431126191E-18));
#13782=CARTESIAN_POINT('',(0.035,0.,0.));
#13783=CARTESIAN_POINT('',(0.035,0.,-0.0125));
#13784=CARTESIAN_POINT('',(0.046000012,0.,0.));
#13785=CARTESIAN_POINT('',(0.046,0.,0.));
#13786=CARTESIAN_POINT('',(0.046,0.,0.0175));
#13787=CARTESIAN_POINT('',(0.028,0.,0.));
#13788=CARTESIAN_POINT('',(0.028,0.,0.));
#13789=CARTESIAN_POINT('',(0.028,0.,-0.0125));
#13790=CARTESIAN_POINT('',(0.046,-5.46437894932694E-19,-1.3010426069826E-18));
#13791=CARTESIAN_POINT('',(0.046,0.,0.));
#13792=CARTESIAN_POINT('',(0.046,0.,0.0185));
#13793=CARTESIAN_POINT('',(0.028,-5.20417042793042E-19,1.39645239816133E-18));
#13794=CARTESIAN_POINT('',(0.028,0.,0.));
#13795=CARTESIAN_POINT('',(0.028,0.,-0.0115));
#13796=CARTESIAN_POINT('',(-0.087860759494,0.,0.));
#13797=CARTESIAN_POINT('',(0.042,0.,0.));
#13798=CARTESIAN_POINT('',(0.042,0.,0.0185));
#13799=CARTESIAN_POINT('',(0.028,0.,0.));
#13800=CARTESIAN_POINT('',(0.0259999999999953,0.,0.));
#13801=CARTESIAN_POINT('',(0.0259999999999953,0.,0.0114999999999814));
#13802=CARTESIAN_POINT('',(0.042,-2.55351295663786E-17,-2.63677968348474E-18));
#13803=CARTESIAN_POINT('',(0.0419999999998646,-1.37313705098871E-13,-8.69099870562485E-19));
#13804=CARTESIAN_POINT('',(0.0419999999999067,0.0329999999999944,-8.69099870562485E-19));
#13805=CARTESIAN_POINT('',(0.042,0.027720932313,-0.010089594228));
#13806=CARTESIAN_POINT('',(0.042,0.027720932313,-0.011389594228));
#13807=CARTESIAN_POINT('',(0.042,0.022598311072,-0.018962234486));
#13808=CARTESIAN_POINT('',(0.042,0.022598311072,-0.020262234486));
#13809=CARTESIAN_POINT('',(0.042,0.01475,-0.025547749412));
#13810=CARTESIAN_POINT('',(0.042,0.01475,-0.026847749412));
#13811=CARTESIAN_POINT('',(0.042,0.005122621241,-0.029051828714));
#13812=CARTESIAN_POINT('',(0.042,0.005122621241,-0.030351828714));
#13813=CARTESIAN_POINT('',(0.042,-0.005122621241,-0.029051828714));
#13814=CARTESIAN_POINT('',(0.042,-0.005122621241,-0.030351828714));
#13815=CARTESIAN_POINT('',(0.042,-0.01475,-0.025547749412));
#13816=CARTESIAN_POINT('',(0.042,-0.01475,-0.026847749412));
#13817=CARTESIAN_POINT('',(0.042,-0.022598311072,-0.018962234486));
#13818=CARTESIAN_POINT('',(0.042,-0.022598311072,-0.020262234486));
#13819=CARTESIAN_POINT('',(0.042,-0.027720932313,-0.010089594228));
#13820=CARTESIAN_POINT('',(0.042,-0.027720932313,-0.011389594228));
#13821=CARTESIAN_POINT('',(0.042,-0.0295,0.));
#13822=CARTESIAN_POINT('',(0.042,-0.0295,-0.0013));
#13823=CARTESIAN_POINT('',(0.042,-0.027720932313,0.010089594228));
#13824=CARTESIAN_POINT('',(0.042,-0.027720932313,0.008789594228));
#13825=CARTESIAN_POINT('',(0.042,-0.022598311072,0.018962234486));
#13826=CARTESIAN_POINT('',(0.042,-0.022598311072,0.017662234486));
#13827=CARTESIAN_POINT('',(0.042,-0.01475,0.025547749412));
#13828=CARTESIAN_POINT('',(0.042,-0.01475,0.024247749412));
#13829=CARTESIAN_POINT('',(0.042,-0.005122621241,0.029051828714));
#13830=CARTESIAN_POINT('',(0.042,-0.005122621241,0.027751828714));
#13831=CARTESIAN_POINT('',(0.042,0.005122621241,0.029051828714));
#13832=CARTESIAN_POINT('',(0.042,0.005122621241,0.027751828714));
#13833=CARTESIAN_POINT('',(0.042,0.01475,0.025547749412));
#13834=CARTESIAN_POINT('',(0.042,0.01475,0.024247749412));
#13835=CARTESIAN_POINT('',(0.042,0.022598311072,0.018962234486));
#13836=CARTESIAN_POINT('',(0.042,0.022598311072,0.017662234486));
#13837=CARTESIAN_POINT('',(0.042,0.027720932313,0.010089594228));
#13838=CARTESIAN_POINT('',(0.042,0.027720932313,0.008789594228));
#13839=CARTESIAN_POINT('',(0.042,0.0295,0.));
#13840=CARTESIAN_POINT('',(0.042,0.0295,-0.0013));
#13841=CARTESIAN_POINT('',(0.071999999999921,0.,0.));
#13842=CARTESIAN_POINT('',(0.024,0.,0.));
#13843=CARTESIAN_POINT('',(0.024,0.,-0.012));
#13844=CARTESIAN_POINT('',(-0.046,0.0295,0.));
#13845=CARTESIAN_POINT('',(0.039,0.0295,0.));
#13846=CARTESIAN_POINT('',(0.039,0.0295,-0.0013));
#13847=CARTESIAN_POINT('',(-0.046,0.027720932313,0.010089594228));
#13848=CARTESIAN_POINT('',(0.039,0.027720932313,0.010089594228));
#13849=CARTESIAN_POINT('',(0.039,0.027720932313,0.008789594228));
#13850=CARTESIAN_POINT('',(-0.046,0.022598311072,0.018962234486));
#13851=CARTESIAN_POINT('',(0.039,0.022598311072,0.018962234486));
#13852=CARTESIAN_POINT('',(0.039,0.022598311072,0.017662234486));
#13853=CARTESIAN_POINT('',(-0.046,0.01475,0.025547749412));
#13854=CARTESIAN_POINT('',(0.039,0.01475,0.025547749412));
#13855=CARTESIAN_POINT('',(0.039,0.01475,0.024247749412));
#13856=CARTESIAN_POINT('',(-0.046,0.005122621241,0.029051828714));
#13857=CARTESIAN_POINT('',(0.039,0.005122621241,0.029051828714));
#13858=CARTESIAN_POINT('',(0.039,0.005122621241,0.027751828714));
#13859=CARTESIAN_POINT('',(-0.046,-0.005122621241,0.029051828714));
#13860=CARTESIAN_POINT('',(0.039,-0.005122621241,0.029051828714));
#13861=CARTESIAN_POINT('',(0.039,-0.005122621241,0.027751828714));
#13862=CARTESIAN_POINT('',(-0.046,-0.01475,0.025547749412));
#13863=CARTESIAN_POINT('',(0.039,-0.01475,0.025547749412));
#13864=CARTESIAN_POINT('',(0.039,-0.01475,0.024247749412));
#13865=CARTESIAN_POINT('',(-0.046,-0.022598311072,0.018962234486));
#13866=CARTESIAN_POINT('',(0.039,-0.022598311072,0.018962234486));
#13867=CARTESIAN_POINT('',(0.039,-0.022598311072,0.017662234486));
#13868=CARTESIAN_POINT('',(-0.046,-0.027720932313,0.010089594228));
#13869=CARTESIAN_POINT('',(0.039,-0.027720932313,0.010089594228));
#13870=CARTESIAN_POINT('',(0.039,-0.027720932313,0.008789594228));
#13871=CARTESIAN_POINT('',(-0.046,-0.0295,0.));
#13872=CARTESIAN_POINT('',(0.039,-0.0295,0.));
#13873=CARTESIAN_POINT('',(0.039,-0.0295,-0.0013));
#13874=CARTESIAN_POINT('',(-0.046,-0.027720932313,-0.010089594228));
#13875=CARTESIAN_POINT('',(0.039,-0.027720932313,-0.010089594228));
#13876=CARTESIAN_POINT('',(0.039,-0.027720932313,-0.011389594228));
#13877=CARTESIAN_POINT('',(-0.046,-0.022598311072,-0.018962234486));
#13878=CARTESIAN_POINT('',(0.039,-0.022598311072,-0.018962234486));
#13879=CARTESIAN_POINT('',(0.039,-0.022598311072,-0.020262234486));
#13880=CARTESIAN_POINT('',(-0.046,-0.01475,-0.025547749412));
#13881=CARTESIAN_POINT('',(0.039,-0.01475,-0.025547749412));
#13882=CARTESIAN_POINT('',(0.039,-0.01475,-0.026847749412));
#13883=CARTESIAN_POINT('',(-0.046,-0.005122621241,-0.029051828714));
#13884=CARTESIAN_POINT('',(0.039,-0.005122621241,-0.029051828714));
#13885=CARTESIAN_POINT('',(0.039,-0.005122621241,-0.030351828714));
#13886=CARTESIAN_POINT('',(-0.046,0.005122621241,-0.029051828714));
#13887=CARTESIAN_POINT('',(0.039,0.005122621241,-0.029051828714));
#13888=CARTESIAN_POINT('',(0.039,0.005122621241,-0.030351828714));
#13889=CARTESIAN_POINT('',(-0.046,0.01475,-0.025547749412));
#13890=CARTESIAN_POINT('',(0.039,0.01475,-0.025547749412));
#13891=CARTESIAN_POINT('',(0.039,0.01475,-0.026847749412));
#13892=CARTESIAN_POINT('',(-0.046,0.022598311072,-0.018962234486));
#13893=CARTESIAN_POINT('',(0.039,0.022598311072,-0.018962234486));
#13894=CARTESIAN_POINT('',(0.039,0.022598311072,-0.020262234486));
#13895=CARTESIAN_POINT('',(-0.046,0.027720932313,-0.010089594228));
#13896=CARTESIAN_POINT('',(0.039,0.027720932313,-0.010089594228));
#13897=CARTESIAN_POINT('',(0.039,0.027720932313,-0.011389594228));
#13898=CARTESIAN_POINT('',(0.0410000000000154,-1.36037053452222E-13,-7.67814047972691E-19));
#13899=CARTESIAN_POINT('',(0.0410000000001318,1.36039880532457E-13,1.32586349256442E-18));
#13900=CARTESIAN_POINT('',(0.0409999998753159,-6.97350952530812E-12,-0.0339999999999195));
#13901=CARTESIAN_POINT('',(0.0409999998750659,-1.9454455441122E-11,0.0339999999999195));
#13902=CARTESIAN_POINT('',(0.0410000000001318,-1.94544627178456E-11,0.0339999999998389));
#13903=CARTESIAN_POINT('',(0.0410000000001261,-0.00445058961092909,0.0339999999973102));
#13904=CARTESIAN_POINT('',(0.0410000000001147,-0.01334969402564,0.0322296836269298));
#13905=CARTESIAN_POINT('',(0.0410000000001003,-0.0246676067857547,0.02466753190434));
#13906=CARTESIAN_POINT('',(0.0410000000000906,-0.0322296622477484,0.0133499720628637));
#13907=CARTESIAN_POINT('',(0.0410000000000872,-0.0348851688773134,-6.40291906310467E-12));
#13908=CARTESIAN_POINT('',(0.0410000000000906,-0.0322296622428478,-0.0133499720746949));
#13909=CARTESIAN_POINT('',(0.0410000000001003,-0.0246676067766995,-0.0246675319133952));
#13910=CARTESIAN_POINT('',(0.0410000000001147,-0.0133496940138089,-0.0322296836318303));
#13911=CARTESIAN_POINT('',(0.0410000000001261,-0.00445058959844814,-0.0339999999989439));
#13912=CARTESIAN_POINT('',(0.0410000000001318,-6.97351966199401E-12,-0.0339999999998389));
#13913=CARTESIAN_POINT('',(0.028,0.,0.));
#13914=CARTESIAN_POINT('',(-0.0320000000000083,0.,0.));
#13915=CARTESIAN_POINT('',(-0.0319999999981381,-0.0119999999536082,-4.92248153054964E-12));
#13916=CARTESIAN_POINT('',(-0.0320000001856381,0.0119999999536082,3.42248023884155E-12));
#13917=CARTESIAN_POINT('',(-0.032,-0.012,-1.9225239339229E-12));
#13918=CARTESIAN_POINT('',(-0.032,-0.0120000000002517,0.00157079632480987));
#13919=CARTESIAN_POINT('',(-0.032,-0.0113751824597898,0.0047116567075861));
#13920=CARTESIAN_POINT('',(-0.032,-0.00870618773601581,0.00870621415482392));
#13921=CARTESIAN_POINT('',(-0.032,-0.00471175485132592,0.0113751749088022));
#13922=CARTESIAN_POINT('',(-0.032,-2.74207991250776E-12,0.0123124125450742));
#13923=CARTESIAN_POINT('',(-0.032,0.00471175484625923,0.0113751749109008));
#13924=CARTESIAN_POINT('',(-0.032,0.0087061877321379,0.00870621415870182));
#13925=CARTESIAN_POINT('',(-0.032,0.0113751824576911,0.00471165671265278));
#13926=CARTESIAN_POINT('',(-0.032,0.011999999999552,0.00157079633015488));
#13927=CARTESIAN_POINT('',(-0.032,0.012,3.42248023051021E-12));
#13928=CARTESIAN_POINT('',(0.039,-2.55351295663786E-17,2.63677968348474E-18));
#13929=CARTESIAN_POINT('',(0.0390000000001354,-1.37315511707168E-13,3.70144955568662E-19));
#13930=CARTESIAN_POINT('',(0.0390000000000933,0.0329999999999944,3.70144955568662E-19));
#13931=CARTESIAN_POINT('',(0.039,0.,0.));
#13932=CARTESIAN_POINT('',(0.039,0.,0.0195));
#13933=CARTESIAN_POINT('',(-0.087860759494,0.,0.));
#13934=CARTESIAN_POINT('',(0.04,-2.24470338423357E-11,-0.034));
#13935=CARTESIAN_POINT('',(0.04,-0.0044505896134887,-0.0339999999970617));
#13936=CARTESIAN_POINT('',(0.04,-0.0133496940271719,-0.0322296836262199));
#13937=CARTESIAN_POINT('',(0.04,-0.0246676067858995,-0.0246675319040342));
#13938=CARTESIAN_POINT('',(0.04,-0.03222966224722,-0.0133499720637649));
#13939=CARTESIAN_POINT('',(0.04,-0.0348851688771597,4.02261648685935E-12));
#13940=CARTESIAN_POINT('',(0.04,-0.0322296622441412,0.0133499720711977));
#13941=CARTESIAN_POINT('',(0.04,-0.0246676067802106,0.0246675319097231));
#13942=CARTESIAN_POINT('',(0.04,-0.0133496940197391,0.0322296836292986));
#13943=CARTESIAN_POINT('',(0.04,-0.0044505896056476,0.0339999999980881));
#13944=CARTESIAN_POINT('',(0.04,-1.46059372383807E-11,0.034));
#13945=CARTESIAN_POINT('',(0.04,-1.15529693224835E-11,0.034));
#13946=CARTESIAN_POINT('',(0.0400000003749341,-6.97351034698232E-12,-0.0339999999999195));
#13947=CARTESIAN_POINT('',(0.04,0.,0.));
#13948=CARTESIAN_POINT('',(-0.0800000000001418,0.,0.));
#13949=CARTESIAN_POINT('',(-0.034,0.,0.));
#13950=CARTESIAN_POINT('',(-0.0340000000018702,-0.0115000000464252,-4.71737817072462E-12));
#13951=CARTESIAN_POINT('',(-0.0340000001875042,0.0115000000000167,3.27988199461071E-12));
#13952=CARTESIAN_POINT('',(-0.0340000000000083,-0.0115000000000334,-1.84241877001479E-12));
#13953=CARTESIAN_POINT('',(-0.0340000000000083,-0.0115000000002745,0.00150534647794716));
#13954=CARTESIAN_POINT('',(-0.0340000000000083,-0.0109012165239968,0.00451533767811645));
#13955=CARTESIAN_POINT('',(-0.0340000000000083,-0.00834342991370603,0.00834345523173046));
#13956=CARTESIAN_POINT('',(-0.0340000000000083,-0.00451543173253378,0.0109012092876337));
#13957=CARTESIAN_POINT('',(-0.0340000000000083,-2.62782831866655E-12,0.0117993953557304));
#13958=CARTESIAN_POINT('',(-0.0340000000000083,0.00451543172767821,0.0109012092896449));
#13959=CARTESIAN_POINT('',(-0.0340000000000083,0.00834342990998969,0.0083434552354468));
#13960=CARTESIAN_POINT('',(-0.0340000000000083,0.0109012165219856,0.00451533768297201));
#13961=CARTESIAN_POINT('',(-0.0340000000000083,0.011499999999604,0.00150534648306946));
#13962=CARTESIAN_POINT('',(-0.0340000000000083,0.0115000000000334,3.27987688758181E-12));
#13963=CARTESIAN_POINT('',(-0.087860759494,0.,0.));
#13964=CARTESIAN_POINT('',(0.034,4.875E-12,0.0195));
#13965=CARTESIAN_POINT('',(0.034,0.00255254403584375,0.0194999999993619));
#13966=CARTESIAN_POINT('',(0.034,0.00765644215749575,0.0184846714939946));
#13967=CARTESIAN_POINT('',(0.034,0.014147598007525,0.0141475550651059));
#13968=CARTESIAN_POINT('',(0.034,0.0184846592300561,0.0076566016255824));
#13969=CARTESIAN_POINT('',(0.034,0.0200076703857572,-4.10364388936103E-12));
#13970=CARTESIAN_POINT('',(0.034,0.0184846592269153,-0.00765660163316493));
#13971=CARTESIAN_POINT('',(0.034,0.0141475980017216,-0.0141475550709093));
#13972=CARTESIAN_POINT('',(0.034,0.0076564421499132,-0.0184846714971353));
#13973=CARTESIAN_POINT('',(0.034,0.00255254402784472,-0.0195000000004089));
#13974=CARTESIAN_POINT('',(0.034,-3.12403330873861E-12,-0.0195));
#13975=CARTESIAN_POINT('',(0.0340000000083513,-5.99926878926874E-12,-0.0194999999687883));
#13976=CARTESIAN_POINT('',(0.0340000000083513,-2.8752398984365E-12,0.0194999999687883));
#13977=CARTESIAN_POINT('',(0.034,-1.28740341154572E-11,-0.0195));
#13978=CARTESIAN_POINT('',(0.034,-0.00255254404303028,-0.0194999999983148));
#13979=CARTESIAN_POINT('',(0.034,-0.00765644216264269,-0.0184846714915085));
#13980=CARTESIAN_POINT('',(0.034,-0.01414759800956,-0.0141475550626079));
#13981=CARTESIAN_POINT('',(0.034,-0.0184846592300232,-0.00765660162480633));
#13982=CARTESIAN_POINT('',(0.034,-0.0200076703854298,2.30708918532461E-12));
#13983=CARTESIAN_POINT('',(0.034,-0.0184846592282575,0.00765660162906927));
#13984=CARTESIAN_POINT('',(0.034,-0.0141475980062973,0.0141475550658706));
#13985=CARTESIAN_POINT('',(0.034,-0.00765644215837976,0.0184846714932742));
#13986=CARTESIAN_POINT('',(0.034,-0.00255254403853318,0.0194999999989035));
#13987=CARTESIAN_POINT('',(0.034,-8.37693459260071E-12,0.0195));
#13988=CARTESIAN_POINT('',(0.0399999999999847,-1.36038696801256E-13,4.00781722114515E-19));
#13989=CARTESIAN_POINT('',(0.028,0.,0.));
#13990=CARTESIAN_POINT('',(-0.036,0.,0.));
#13991=CARTESIAN_POINT('',(-0.036,0.,-0.0115));
#13992=CARTESIAN_POINT('',(0.000225009254313235,0.,0.));
#13993=CARTESIAN_POINT('',(0.0284641016149117,-7.00391101341243E-12,-0.016303847577153));
#13994=CARTESIAN_POINT('',(0.0284641016149117,-0.00213416866341332,-0.0163038475762362));
#13995=CARTESIAN_POINT('',(0.0284641016149117,-0.00640151107325889,-0.015454936745714));
#13996=CARTESIAN_POINT('',(0.0284641016149117,-0.0118287323830679,-0.011828696481542));
#13997=CARTESIAN_POINT('',(0.0284641016149117,-0.0154549264905978,-0.00640164440683067));
#13998=CARTESIAN_POINT('',(0.0284641016149117,-0.0167283081198615,-2.97447703265889E-12));
#13999=CARTESIAN_POINT('',(0.0284641016149117,-0.0154549264928743,0.00640164440133462));
#14000=CARTESIAN_POINT('',(0.0284641016149117,-0.0118287323872744,0.0118286964773355));
#14001=CARTESIAN_POINT('',(0.0284641016149117,-0.00640151107875499,0.0154549367434375));
#14002=CARTESIAN_POINT('',(0.0284641016149117,-0.0021341686692113,0.0163038475754773));
#14003=CARTESIAN_POINT('',(0.0284641016149117,-1.28018861790704E-11,0.016303847577153));
#14004=CARTESIAN_POINT('',(0.0284641017231648,-1.28018825845269E-11,0.016303847639653));
#14005=CARTESIAN_POINT('',(0.028464101723209,-5.53993719574163E-12,-0.0163038476395765));
#14006=CARTESIAN_POINT('',(0.0284641016149116,0.,0.));
#14007=CARTESIAN_POINT('',(-0.036,-5.20417042793042E-19,-1.39645239816133E-18));
#14008=CARTESIAN_POINT('',(-0.036,0.,0.));
#14009=CARTESIAN_POINT('',(-0.036,0.,-0.0125));
#14010=CARTESIAN_POINT('',(0.0274641016153175,3.0328372677955E-13,-6.78218228121713E-19));
#14011=CARTESIAN_POINT('',(0.0274641016157182,5.28701310234456E-17,-0.0160358983846333));
#14012=CARTESIAN_POINT('',(0.0278131674658368,3.8206405763144E-16,-0.0160358983847033));
#14013=CARTESIAN_POINT('',(0.0281618017210979,-1.01223191233354E-15,-0.016129314652066));
#14014=CARTESIAN_POINT('',(0.0284641016147314,-5.8446799695983E-17,-0.0163038475774072));
#14015=CARTESIAN_POINT('',(0.0274641014903591,-3.28901507865897E-12,-0.0160358983848167));
#14016=CARTESIAN_POINT('',(0.027464101615,0.,2.55499381282536E-17));
#14017=CARTESIAN_POINT('',(0.0274641014903591,-7.17767932656037E-19,0.0160358983848167));
#14018=CARTESIAN_POINT('',(0.0284641016147314,-3.99727831696944E-17,0.0163038475774072));
#14019=CARTESIAN_POINT('',(0.0281618017210979,-1.02050365731269E-15,0.016129314652066));
#14020=CARTESIAN_POINT('',(0.0278131674658368,3.48011082928235E-16,0.0160358983847033));
#14021=CARTESIAN_POINT('',(0.0274641016157182,-7.29453163667589E-18,0.0160358983846333));
#14022=CARTESIAN_POINT('',(0.0274641016153175,-3.0328373862405E-13,1.10406601067048E-18));
#14023=CARTESIAN_POINT('',(0.0274641016157182,-3.28902052244081E-12,-0.0160358983846333));
#14024=CARTESIAN_POINT('',(0.0274641016158464,-0.00209909419313044,-0.0160358983842425));
#14025=CARTESIAN_POINT('',(0.0274641016161028,-0.00629630402099476,-0.0152009391671627));
#14026=CARTESIAN_POINT('',(0.0274641016164288,-0.0116343304626701,-0.0116342951504423));
#14027=CARTESIAN_POINT('',(0.0274641016166466,-0.0152009290811225,-0.00629643516240151));
#14028=CARTESIAN_POINT('',(0.0274641016167231,-0.0164533830371665,1.68734400876107E-12));
#14029=CARTESIAN_POINT('',(0.0274641016166466,-0.0152009290798311,0.00629643516551926));
#14030=CARTESIAN_POINT('',(0.0274641016164288,-0.0116343304602839,0.0116342951528286));
#14031=CARTESIAN_POINT('',(0.0274641016161028,-0.00629630401787699,0.0152009391684541));
#14032=CARTESIAN_POINT('',(0.0274641016158464,-0.00209909418984144,0.016035898384673));
#14033=CARTESIAN_POINT('',(0.0274641016157182,-1.92389594726442E-17,0.0160358983846333));
#14034=CARTESIAN_POINT('',(-0.046,0.,0.));
#14035=CARTESIAN_POINT('',(-0.0457000000001119,3.50888490739562E-13,-3.07178390214567E-19));
#14036=CARTESIAN_POINT('',(-0.045699999875,-5.80991519208953E-12,-0.0125));
#14037=CARTESIAN_POINT('',(-0.0457000000000961,-7.2512874463399E-12,0.0124999999998023));
#14038=CARTESIAN_POINT('',(-0.0457,-5.80992227401315E-12,-0.0125));
#14039=CARTESIAN_POINT('',(-0.0457,-0.00163624617896867,-0.0124999999992395));
#14040=CARTESIAN_POINT('',(-0.0457,-0.00490797574291331,-0.0118491483929665));
#14041=CARTESIAN_POINT('',(-0.0457,-0.00906897308119405,-0.00906894555480054));
#14042=CARTESIAN_POINT('',(-0.0457,-0.0118491405310354,-0.00490807796708854));
#14043=CARTESIAN_POINT('',(-0.0457,-0.0128254297342425,-1.25315075420625E-12));
#14044=CARTESIAN_POINT('',(-0.0457,-0.0118491405319946,0.00490807796477308));
#14045=CARTESIAN_POINT('',(-0.0457,-0.00906897308296621,0.00906894555302836));
#14046=CARTESIAN_POINT('',(-0.0457,-0.0049079757452288,0.0118491483920074));
#14047=CARTESIAN_POINT('',(-0.0457,-0.00163624618141133,0.0124999999989197));
#14048=CARTESIAN_POINT('',(-0.0457,-8.25258597144694E-12,0.0125));
#14049=CARTESIAN_POINT('',(-0.087860759494,0.,5.07655879918927E-49));
#14050=CARTESIAN_POINT('',(-0.024585786438,-7.45336965029581E-12,0.016035898385));
#14051=CARTESIAN_POINT('',(-0.024585786438,0.000957895816119835,0.0160358983854452));
#14052=CARTESIAN_POINT('',(-0.024585786438,0.00191577520026407,0.015949840337913));
#14053=CARTESIAN_POINT('',(-0.024585786438,0.00285833127640244,0.0157790994460516));
#14054=CARTESIAN_POINT('',(-0.0245857915218893,0.00285875682645188,0.0157810768606755));
#14055=CARTESIAN_POINT('',(-0.024585786063,-7.45336965029578E-12,0.016035898385));
#14056=CARTESIAN_POINT('',(-0.024585786438,-0.00285833128348905,0.0157790994447679));
#14057=CARTESIAN_POINT('',(-0.024585786438,-0.00191577520995451,0.0159498403365949));
#14058=CARTESIAN_POINT('',(-0.024585786438,-0.00095789582845831,0.0160358983845548));
#14059=CARTESIAN_POINT('',(-0.024585786438,-7.45337161412695E-12,0.016035898385));
#14060=CARTESIAN_POINT('',(-0.0245857915247488,-0.00285875721875978,0.0157810777875231));
#14061=CARTESIAN_POINT('',(-0.0244999999986063,-0.0038308953218821,0.0155715855983528));
#14062=CARTESIAN_POINT('',(-0.0244999999986063,-0.00375675399330742,0.0155898257234191));
#14063=CARTESIAN_POINT('',(-0.0245092062752334,-0.00361121403183318,0.0156242768363253));
#14064=CARTESIAN_POINT('',(-0.0245230015373636,-0.00349407903633082,0.0156507180843297));
#14065=CARTESIAN_POINT('',(-0.0245385333070015,-0.00337456186848279,0.0156770044066975));
#14066=CARTESIAN_POINT('',(-0.024553360191519,-0.00326583388861101,0.0156998573759084));
#14067=CARTESIAN_POINT('',(-0.0245599200223058,-0.003216175379522,0.0157101139591801));
#14068=CARTESIAN_POINT('',(-0.0245794719072487,-0.00305592627035903,0.0157425438538854));
#14069=CARTESIAN_POINT('',(-0.024585786438,-0.0029347517273015,0.0157652561360282));
#14070=CARTESIAN_POINT('',(-0.024585786438,-0.00285833128348905,0.0157790994447679));
#14071=CARTESIAN_POINT('',(-0.0244999908748831,-0.00383146920545553,0.0155743307735512));
#14072=CARTESIAN_POINT('',(-0.0244999999986063,-0.0115699410488142,0.0111034454626035));
#14073=CARTESIAN_POINT('',(-0.0244999999986063,-0.00947974650797664,0.0132814565763153));
#14074=CARTESIAN_POINT('',(-0.0244999999986063,-0.0067622055462158,0.0148504295828361));
#14075=CARTESIAN_POINT('',(-0.0244999999986063,-0.0038308953218821,0.0155715855983528));
#14076=CARTESIAN_POINT('',(-0.024499990869348,-0.0115720326073917,0.0111053160311667));
#14077=CARTESIAN_POINT('',(-0.024585786438,-0.0122359353307441,0.01036493722103));
#14078=CARTESIAN_POINT('',(-0.024585786438,-0.0121857755381519,0.0104241514705014));
#14079=CARTESIAN_POINT('',(-0.0245794838708969,-0.0121055669343417,0.0105176812333229));
#14080=CARTESIAN_POINT('',(-0.0245599357702701,-0.0119973545564825,0.0106402513674701));
#14081=CARTESIAN_POINT('',(-0.0245533746790821,-0.0119636301855107,0.0106781433864587));
#14082=CARTESIAN_POINT('',(-0.0245385462358393,-0.0118894679802916,0.0107608868196226));
#14083=CARTESIAN_POINT('',(-0.0245230204403454,-0.0118069814705956,0.0108512096671411));
#14084=CARTESIAN_POINT('',(-0.0245092134847558,-0.011725477902448,0.0109394730212321));
#14085=CARTESIAN_POINT('',(-0.0244999999986063,-0.011622848024814,0.0110483156746966));
#14086=CARTESIAN_POINT('',(-0.0244999999986063,-0.0115699410488142,0.0111034454626035));
#14087=CARTESIAN_POINT('',(-0.0245857915218036,-0.0122374350471151,0.0103662944654208));
#14088=CARTESIAN_POINT('',(-0.024585786438,-0.0150942666086899,0.00541416222141845));
#14089=CARTESIAN_POINT('',(-0.024585786438,-0.0144474424338318,0.00721745812297648));
#14090=CARTESIAN_POINT('',(-0.024585786438,-0.0134742233042604,0.00890312310275038));
#14091=CARTESIAN_POINT('',(-0.024585786438,-0.0122359353307441,0.01036493722103));
#14092=CARTESIAN_POINT('',(-0.0245857915246625,-0.0150961928720038,0.00541478251987751));
#14093=CARTESIAN_POINT('',(-0.0244999999986063,-0.0154008363654399,0.00446814013421592));
#14094=CARTESIAN_POINT('',(-0.0244999999986063,-0.0153795621158588,0.00454146846026513));
#14095=CARTESIAN_POINT('',(-0.0245092062770903,-0.0153366276661337,0.00468473534680755));
#14096=CARTESIAN_POINT('',(-0.0245230015342683,-0.0153009589728398,0.00479939781420821));
#14097=CARTESIAN_POINT('',(-0.0245385333074752,-0.0152639650035507,0.0049160459052644));
#14098=CARTESIAN_POINT('',(-0.0245533601912854,-0.0152293922673203,0.00502163357681073));
#14099=CARTESIAN_POINT('',(-0.0245599200224393,-0.0152134454727527,0.00506976740392879));
#14100=CARTESIAN_POINT('',(-0.0245794719071485,-0.0151614060402287,0.00522476212260026));
#14101=CARTESIAN_POINT('',(-0.024585786438,-0.0151204881851425,0.00534105848907922));
#14102=CARTESIAN_POINT('',(-0.024585786438,-0.0150942666086899,0.00541416222141845));
#14103=CARTESIAN_POINT('',(-0.0244999908748826,-0.0154035006993891,0.00446901572194627));
#14104=CARTESIAN_POINT('',(-0.0244999999986063,-0.0154008363654352,-0.0044681401342319));
#14105=CARTESIAN_POINT('',(-0.0244999999986063,-0.0162419520486458,-0.00156897300599358));
#14106=CARTESIAN_POINT('',(-0.0244999999986063,-0.0162419520486474,0.00156897300597672));
#14107=CARTESIAN_POINT('',(-0.0244999999986063,-0.0154008363654399,0.00446814013421592));
#14108=CARTESIAN_POINT('',(-0.0244999908693475,-0.0154035021040441,-0.00446901619492932));
#14109=CARTESIAN_POINT('',(-0.024585786438,-0.0150942666084793,-0.00541416222200544));
#14110=CARTESIAN_POINT('',(-0.024585786438,-0.0151204677564812,-0.00534111544261991));
#14111=CARTESIAN_POINT('',(-0.024579483870953,-0.0151613626047746,-0.00522488787391248));
#14112=CARTESIAN_POINT('',(-0.0245599357701953,-0.0152134052666352,-0.00506988813579796));
#14113=CARTESIAN_POINT('',(-0.0245533746792129,-0.0152293585307658,-0.00502173596870886));
#14114=CARTESIAN_POINT('',(-0.0245385462343378,-0.0152639353408618,-0.00491613790530282));
#14115=CARTESIAN_POINT('',(-0.0245230204532045,-0.0153009139297729,-0.00479954118649679));
#14116=CARTESIAN_POINT('',(-0.0245092134770404,-0.0153366005165388,-0.00468482514492004));
#14117=CARTESIAN_POINT('',(-0.0244999999986063,-0.0153795460566674,-0.00454152381326889));
#14118=CARTESIAN_POINT('',(-0.0244999999986063,-0.0154008363654352,-0.0044681401342319));
#14119=CARTESIAN_POINT('',(-0.0245857915218038,-0.0150961918740712,-0.00541478239418764));
#14120=CARTESIAN_POINT('',(-0.024585786438,-0.0122359353199755,-0.0103649372337425));
#14121=CARTESIAN_POINT('',(-0.024585786438,-0.0134742232984657,-0.0089031231126705));
#14122=CARTESIAN_POINT('',(-0.024585786438,-0.0144474424317463,-0.00721745812857003));
#14123=CARTESIAN_POINT('',(-0.024585786438,-0.0150942666084793,-0.00541416222200544));
#14124=CARTESIAN_POINT('',(-0.0245857915246626,-0.012237435651537,-0.0103662952709461));
#14125=CARTESIAN_POINT('',(-0.0244999999986063,-0.0115699410488029,-0.0111034454626152));
#14126=CARTESIAN_POINT('',(-0.0244999999986063,-0.0116228081173456,-0.011048357258821));
#14127=CARTESIAN_POINT('',(-0.0245092062722935,-0.0117254136119208,-0.0109395415387983));
#14128=CARTESIAN_POINT('',(-0.0245230015422633,-0.0118068799584357,-0.0108513202198437));
#14129=CARTESIAN_POINT('',(-0.0245385333053876,-0.0118894031339274,-0.0107609585117453));
#14130=CARTESIAN_POINT('',(-0.0245533601934441,-0.0119635583919606,-0.01067822378554));
#14131=CARTESIAN_POINT('',(-0.0245599200212059,-0.0119972700774136,-0.0106403465813125));
#14132=CARTESIAN_POINT('',(-0.0245794719080736,-0.0121054797679643,-0.0105177817029997));
#14133=CARTESIAN_POINT('',(-0.024585786438,-0.0121857364257066,-0.0104241976430973));
#14134=CARTESIAN_POINT('',(-0.024585786438,-0.0122359353199755,-0.0103649372337425));
#14135=CARTESIAN_POINT('',(-0.024499990874883,-0.0115720314953153,-0.011105315051073));
#14136=CARTESIAN_POINT('',(-0.0244999999986063,-0.00383089532186528,-0.0155715855983569));
#14137=CARTESIAN_POINT('',(-0.0244999999986063,-0.0067622055462001,-0.0148504295828433));
#14138=CARTESIAN_POINT('',(-0.0244999999986063,-0.00947974650796292,-0.0132814565763252));
#14139=CARTESIAN_POINT('',(-0.0244999999986063,-0.0115699410488029,-0.0111034454626152));
#14140=CARTESIAN_POINT('',(-0.0244999908693477,-0.00383146949816682,-0.015574332226511));
#14141=CARTESIAN_POINT('',(-0.024585786438,-0.00285833128287572,-0.015779099444879));
#14142=CARTESIAN_POINT('',(-0.024585786438,-0.00293469221286251,-0.0157652669168736));
#14143=CARTESIAN_POINT('',(-0.0245794838828349,-0.00305579558471988,-0.0157425691269049));
#14144=CARTESIAN_POINT('',(-0.0245599357543528,-0.00321605083959362,-0.0157101394805771));
#14145=CARTESIAN_POINT('',(-0.0245533747069374,-0.00326572813265205,-0.0156998793996686));
#14146=CARTESIAN_POINT('',(-0.0245385462192562,-0.00337446747410242,-0.0156770246950493));
#14147=CARTESIAN_POINT('',(-0.0245230204503161,-0.00349393241722351,-0.0156507507466387));
#14148=CARTESIAN_POINT('',(-0.0245092134787734,-0.00361112264764015,-0.0156242982328882));
#14149=CARTESIAN_POINT('',(-0.0244999999986063,-0.00375669803694566,-0.0155898394897091));
#14150=CARTESIAN_POINT('',(-0.0244999999986063,-0.00383089532186528,-0.0155715855983569));
#14151=CARTESIAN_POINT('',(-0.0245857915217653,-0.00285875758549826,-0.0157810767208921));
#14152=CARTESIAN_POINT('',(-0.024585786438,0.,1.40184139924496E-17));
#14153=CARTESIAN_POINT('',(-0.024585786438,-2.56905698753516E-12,-0.0160358983849999));
#14154=CARTESIAN_POINT('',(-0.024585786438,0.00285833128996237,-0.0157790994435952));
#14155=CARTESIAN_POINT('',(-0.024585786438,0.00191577521105279,-0.0159498403367953));
#14156=CARTESIAN_POINT('',(-0.024585786438,0.000957895823969581,-0.0160358983851534));
#14157=CARTESIAN_POINT('',(-0.024585786438,-2.56906054821988E-12,-0.016035898385));
#14158=CARTESIAN_POINT('',(-0.0245857915246446,0.00285875722091595,-0.0157810777871251));
#14159=CARTESIAN_POINT('',(-0.0244999999986063,0.00383089532826959,-0.0155715855967813));
#14160=CARTESIAN_POINT('',(-0.0244999999986063,0.0037567539999507,-0.015589825721817));
#14161=CARTESIAN_POINT('',(-0.0245092062723273,0.00361121406795415,-0.0156242768282245));
#14162=CARTESIAN_POINT('',(-0.024523001542207,0.00349407899314799,-0.0156507180939493));
#14163=CARTESIAN_POINT('',(-0.0245385333055515,0.00337456186892705,-0.0156770044066164));
#14164=CARTESIAN_POINT('',(-0.0245533601931607,0.00326583386869777,-0.0156998573800514));
#14165=CARTESIAN_POINT('',(-0.0245599200213679,0.00321617540143936,-0.0157101139546529));
#14166=CARTESIAN_POINT('',(-0.0245794719079521,0.00305592626012084,-0.01574254385596));
#14167=CARTESIAN_POINT('',(-0.024585786438,0.00293475175703248,-0.0157652561306102));
#14168=CARTESIAN_POINT('',(-0.024585786438,0.00285833128996237,-0.0157790994435952));
#14169=CARTESIAN_POINT('',(-0.0244999908748829,0.00383146920758899,-0.0155743307730475));
#14170=CARTESIAN_POINT('',(-0.0244999999986063,0.0115699410422654,-0.0111034454694274));
#14171=CARTESIAN_POINT('',(-0.0244999999986063,0.00947974650384446,-0.0132814565780498));
#14172=CARTESIAN_POINT('',(-0.0244999999986063,0.00676220554711697,-0.0148504295813392));
#14173=CARTESIAN_POINT('',(-0.0244999999986063,0.00383089532826959,-0.0155715855967813));
#14174=CARTESIAN_POINT('',(-0.0244999908693478,0.01157203260522,-0.0111053160334516));
#14175=CARTESIAN_POINT('',(-0.024585786438,0.0122359353246303,-0.0103649372282474));
#14176=CARTESIAN_POINT('',(-0.024585786438,0.0121857755389782,-0.0104241514694551));
#14177=CARTESIAN_POINT('',(-0.024579483882876,0.01210556701272,-0.0105176811453351));
#14178=CARTESIAN_POINT('',(-0.0245599357542979,0.0119973544631023,-0.010640251472091));
#14179=CARTESIAN_POINT('',(-0.0245533747070335,0.0119636303288962,-0.0106781432259488));
#14180=CARTESIAN_POINT('',(-0.0245385462192108,0.011889467902065,-0.0107608869071751));
#14181=CARTESIAN_POINT('',(-0.0245230204502448,0.0118069815237895,-0.0108512096084395));
#14182=CARTESIAN_POINT('',(-0.0245092134788162,0.0117254778602576,-0.0109394730675282));
#14183=CARTESIAN_POINT('',(-0.0244999999986063,0.0116228480182091,-0.0110483156816441));
#14184=CARTESIAN_POINT('',(-0.0244999999986063,0.0115699410422654,-0.0111034454694274));
#14185=CARTESIAN_POINT('',(-0.0245857915217862,0.0122374350450725,-0.0103662944678227));
#14186=CARTESIAN_POINT('',(-0.024585786438,0.0150942666109112,-0.00541416221522574));
#14187=CARTESIAN_POINT('',(-0.024585786438,0.0144474424349879,-0.00721745812208117));
#14188=CARTESIAN_POINT('',(-0.024585786438,0.0134742233024643,-0.00890312310661903));
#14189=CARTESIAN_POINT('',(-0.024585786438,0.0122359353246303,-0.0103649372282474));
#14190=CARTESIAN_POINT('',(-0.024585791524644,0.0150961928727466,-0.00541478251781387));
#14191=CARTESIAN_POINT('',(-0.0244999999986063,0.0154008363672729,-0.00446814012789783));
#14192=CARTESIAN_POINT('',(-0.0244999999986063,0.0153795621147456,-0.00454146846421457));
#14193=CARTESIAN_POINT('',(-0.0245092062732926,0.0153366276777982,-0.00468473530997678));
#14194=CARTESIAN_POINT('',(-0.0245230015405982,0.0153009589595615,-0.00479939785541512));
#14195=CARTESIAN_POINT('',(-0.0245385332971209,0.0152639650254876,-0.00491604583880081));
#14196=CARTESIAN_POINT('',(-0.0245533602086576,0.0152293922217421,-0.00502163371519752));
#14197=CARTESIAN_POINT('',(-0.0245599200125125,0.0152134455028226,-0.00506976731277923));
#14198=CARTESIAN_POINT('',(-0.0245794719145936,0.0151614060119585,-0.00522476220778196));
#14199=CARTESIAN_POINT('',(-0.024585786438,0.0151204881837907,-0.0053410584927536));
#14200=CARTESIAN_POINT('',(-0.024585786438,0.0150942666109112,-0.00541416221522574));
#14201=CARTESIAN_POINT('',(-0.0244999908750048,0.0154035004811123,-0.0044690164683281));
#14202=CARTESIAN_POINT('',(-0.0244999999986063,0.,1.40374197662062E-17));
#14203=CARTESIAN_POINT('',(-0.0244999908694697,0.0154035018848601,0.00446901694447226));
#14204=CARTESIAN_POINT('',(-0.024585786438,0.0150942666116729,0.00541416221310206));
#14205=CARTESIAN_POINT('',(-0.024585786438,0.015120467756025,0.00534111544375616));
#14206=CARTESIAN_POINT('',(-0.0245794838828001,0.0151613625683128,0.00522488798407675));
#14207=CARTESIAN_POINT('',(-0.0245599357543992,0.0152134053098073,0.00506988800492372));
#14208=CARTESIAN_POINT('',(-0.0245533747068561,0.0152293584647529,0.00502173616910086));
#14209=CARTESIAN_POINT('',(-0.0245385462198197,0.0152639353795454,0.0049161377882726));
#14210=CARTESIAN_POINT('',(-0.0245230204456509,0.0153009139554188,0.004799541102855));
#14211=CARTESIAN_POINT('',(-0.0245092134815725,0.0153366004980514,0.00468482520515153));
#14212=CARTESIAN_POINT('',(-0.0244999999986063,0.0153795460547884,0.00454152381963283));
#14213=CARTESIAN_POINT('',(-0.0244999999986063,0.0154008363636023,0.00446814014054949));
#14214=CARTESIAN_POINT('',(-0.0245857915217865,0.015096191875143,0.00541478239122186));
#14215=CARTESIAN_POINT('',(-0.024585786438,0.0122359353260886,0.0103649372265259));
#14216=CARTESIAN_POINT('',(-0.024585786438,0.0134742233037169,0.0089031231047233));
#14217=CARTESIAN_POINT('',(-0.024585786438,0.0144474424360034,0.0072174581200485));
#14218=CARTESIAN_POINT('',(-0.024585786438,0.0150942666116729,0.00541416221310206));
#14219=CARTESIAN_POINT('',(-0.0245857915246441,0.0122374356535695,0.0103662952685353));
#14220=CARTESIAN_POINT('',(-0.0244999999986063,0.0115699410442475,0.011103445467362));
#14221=CARTESIAN_POINT('',(-0.0244999999986063,0.011622808120127,0.011048357255968));
#14222=CARTESIAN_POINT('',(-0.0245092062752789,0.011725413640156,0.0109395415081673));
#14223=CARTESIAN_POINT('',(-0.0245230015372877,0.0118068799297762,0.0108513202510711));
#14224=CARTESIAN_POINT('',(-0.0245385333071508,0.0118894031377654,0.0107609585074612));
#14225=CARTESIAN_POINT('',(-0.0245533601912659,0.0119635583775685,0.0106782238016603));
#14226=CARTESIAN_POINT('',(-0.0245599200224506,0.0119972700957928,0.0106403465606616));
#14227=CARTESIAN_POINT('',(-0.02457947190714,0.0121054797616445,0.0105177817101086));
#14228=CARTESIAN_POINT('',(-0.024585786438,0.0121857364476053,0.0104241976173165));
#14229=CARTESIAN_POINT('',(-0.024585786438,0.0122359353260886,0.0103649372265259));
#14230=CARTESIAN_POINT('',(-0.0244999908748826,0.0115720314937939,0.0111053150526529));
#14231=CARTESIAN_POINT('',(-0.0244999999986063,0.0038308953154777,0.0155715855999284));
#14232=CARTESIAN_POINT('',(-0.0244999999986063,0.00676220554010803,0.0148504295856173));
#14233=CARTESIAN_POINT('',(-0.0244999999986063,0.00947974650251419,0.0132814565802142));
#14234=CARTESIAN_POINT('',(-0.0244999999986063,0.0115699410442475,0.011103445467362));
#14235=CARTESIAN_POINT('',(-0.0244999908693481,0.00383146949603822,0.0155743322270386));
#14236=CARTESIAN_POINT('',(-0.024585786438,0.00285833127640243,0.0157790994460516));
#14237=CARTESIAN_POINT('',(-0.024585786438,0.00293469221702162,0.0157652669161526));
#14238=CARTESIAN_POINT('',(-0.024579483870863,0.00305579566977372,0.0157425691090143));
#14239=CARTESIAN_POINT('',(-0.0245599357703154,0.00321605070803771,0.0157101395079826));
#14240=CARTESIAN_POINT('',(-0.0245533746790029,0.00326572834549023,0.0156998793552969));
#14241=CARTESIAN_POINT('',(-0.0245385462358954,0.00337446736221416,0.0156770247183708));
#14242=CARTESIAN_POINT('',(-0.024523020440236,0.00349393249877838,0.0156507507289995));
#14243=CARTESIAN_POINT('',(-0.0245092134848215,0.00361112258835951,0.0156242982458343));
#14244=CARTESIAN_POINT('',(-0.0244999999986063,0.00375669803098476,0.0155898394911433));
#14245=CARTESIAN_POINT('',(-0.0244999999986063,0.0038308953154777,0.0155715855999284));
#14246=CARTESIAN_POINT('',(-0.0457000000001119,3.50888490739562E-13,-3.07178390214567E-19));
#14247=CARTESIAN_POINT('',(-0.0460000000003369,3.49584240338238E-13,-2.85957696782259E-19));
#14248=CARTESIAN_POINT('',(-0.0460000000003925,0.0128000000001574,-2.85957696782259E-19));
#14249=CARTESIAN_POINT('',(-0.0245857864382098,-1.06895708554224E-18,5.60523044629629E-12));
#14250=CARTESIAN_POINT('',(-0.026,0.,0.));
#14251=CARTESIAN_POINT('',(-0.0260046754559256,0.00303667233985881,-0.016761340881293));
#14252=CARTESIAN_POINT('',(-0.0260046753764207,-0.00303667205936906,-0.0167613409725091));
#14253=CARTESIAN_POINT('',(-0.0260093507668446,0.00303675796778517,-0.0167595980847489));
#14254=CARTESIAN_POINT('',(-0.0259634000228127,0.00301413112031303,-0.0166352153311787));
#14255=CARTESIAN_POINT('',(-0.0258372476659582,0.00296840214035727,-0.0163834477539786));
#14256=CARTESIAN_POINT('',(-0.0255181562604789,0.00291257308816476,-0.0160777814927587));
#14257=CARTESIAN_POINT('',(-0.0252574621306591,0.00288545817598874,-0.0159300603377363));
#14258=CARTESIAN_POINT('',(-0.0250772590166116,0.00287212279539721,-0.0158591127207493));
#14259=CARTESIAN_POINT('',(-0.0249296521814598,0.0028648507887674,-0.0158197682249595));
#14260=CARTESIAN_POINT('',(-0.0248141730419544,0.0028610453310314,-0.015798524952678));
#14261=CARTESIAN_POINT('',(-0.0247254103202069,0.00285940104998143,-0.0157878998711275));
#14262=CARTESIAN_POINT('',(-0.0246348999596275,0.00285892031357241,-0.0157837419929907));
#14263=CARTESIAN_POINT('',(-0.0246245061620364,0.00285915979859944,-0.0157829616407464));
#14264=CARTESIAN_POINT('',(-0.0245857965998287,0.00285917994845102,-0.0157830567238291));
#14265=CARTESIAN_POINT('',(-0.0245857965941096,-0.00285917916856927,-0.0157830548693243));
#14266=CARTESIAN_POINT('',(-0.024587878063756,-0.00285917808489342,-0.0157830497570209));
#14267=CARTESIAN_POINT('',(-0.0246336063425909,-0.00285921570671322,-0.0157832993187842));
#14268=CARTESIAN_POINT('',(-0.0246879782365064,-0.00285974198593955,-0.0157858384025746));
#14269=CARTESIAN_POINT('',(-0.0247977856685484,-0.00286161612201955,-0.015794835889566));
#14270=CARTESIAN_POINT('',(-0.0249386423726374,-0.0028668146759778,-0.0158199768626178));
#14271=CARTESIAN_POINT('',(-0.0250982101173787,-0.00287617118472857,-0.0158663273977922));
#14272=CARTESIAN_POINT('',(-0.0252906230360713,-0.00289175213210285,-0.0159453481174248));
#14273=CARTESIAN_POINT('',(-0.0254945146967682,-0.00291519894531635,-0.0160683151780273));
#14274=CARTESIAN_POINT('',(-0.0257437244060328,-0.00295515150038263,-0.0162871022461858));
#14275=CARTESIAN_POINT('',(-0.0259279713746338,-0.00300141820559167,-0.0165553620254441));
#14276=CARTESIAN_POINT('',(-0.0259895224206423,-0.00302699365645837,-0.0167059255721978));
#14277=CARTESIAN_POINT('',(-0.0260093506078345,-0.00303675740795554,-0.0167595982669723));
#14278=CARTESIAN_POINT('',(-0.0245415219088105,0.00366437443650513,-0.0171447580070949));
#14279=CARTESIAN_POINT('',(-0.0259961345404699,0.00418903800875609,-0.0170280171879218));
#14280=CARTESIAN_POINT('',(-0.0260208846843343,0.00385989161947845,-0.0167874634655829));
#14281=CARTESIAN_POINT('',(-0.0259763001860542,0.00343771689296902,-0.0166906660659931));
#14282=CARTESIAN_POINT('',(-0.0260105733383942,0.00303746425710906,-0.0167629249983474));
#14283=CARTESIAN_POINT('',(-0.0259980774508458,0.00418905033679694,-0.0170282004945628));
#14284=CARTESIAN_POINT('',(-0.0244999817389186,0.00383204629597067,-0.0155770751715398));
#14285=CARTESIAN_POINT('',(-0.024944756596428,0.00383234583080769,-0.0155784920383265));
#14286=CARTESIAN_POINT('',(-0.0257532661794538,0.00393609475349983,-0.0159769883169212));
#14287=CARTESIAN_POINT('',(-0.0259959930191986,0.00410791207526705,-0.0166992236842379));
#14288=CARTESIAN_POINT('',(-0.0259961548791011,0.00418887289593309,-0.0170282446560903));
#14289=CARTESIAN_POINT('',(-0.0244999999971406,5.18740924496995E-13,-1.35370767904267E-12));
#14290=CARTESIAN_POINT('',(-0.0259999999972629,3.97065401316842E-13,-1.14383970554836E-12));
#14291=CARTESIAN_POINT('',(-0.0259980767575597,0.0126523290853278,-0.0121419242115842));
#14292=CARTESIAN_POINT('',(-0.0259961534925062,0.0126524561027222,-0.012141792577423));
#14293=CARTESIAN_POINT('',(-0.0259959911366752,0.0124079921773759,-0.011907164237172));
#14294=CARTESIAN_POINT('',(-0.0257532552174247,0.0118684248901205,-0.0113972464272905));
#14295=CARTESIAN_POINT('',(-0.0249447500346905,0.0115751992386728,-0.0111081568807122));
#14296=CARTESIAN_POINT('',(-0.024499981727848,0.0115741218908241,-0.0111071889869984));
#14297=CARTESIAN_POINT('',(-0.0245418550974504,0.0130179595803562,-0.0117432056820992));
#14298=CARTESIAN_POINT('',(-0.02601057263116,0.0129983875047157,-0.0110119839056589));
#14299=CARTESIAN_POINT('',(-0.0259762684314703,0.0127354513023962,-0.0113227572395601));
#14300=CARTESIAN_POINT('',(-0.0260208848459058,0.0126084204264453,-0.0117364608404768));
#14301=CARTESIAN_POINT('',(-0.0259961329743928,0.012652176631433,-0.0121418218538705));
#14302=CARTESIAN_POINT('',(-0.0260046753581521,0.0129974109954827,-0.0110105057125223));
#14303=CARTESIAN_POINT('',(-0.0245857965941095,0.0122389368818809,-0.010367649228686));
#14304=CARTESIAN_POINT('',(-0.0245878780633656,0.0122389329963349,-0.010367645734044));
#14305=CARTESIAN_POINT('',(-0.0246336063426967,0.0122391303122479,-0.0103678030963753));
#14306=CARTESIAN_POINT('',(-0.0246879782359766,0.0122410660836794,-0.0103695284094339));
#14307=CARTESIAN_POINT('',(-0.0247977856677001,0.0122479210678728,-0.0103756502023255));
#14308=CARTESIAN_POINT('',(-0.0249386423710321,0.0122670945120445,-0.0103927227684832));
#14309=CARTESIAN_POINT('',(-0.0250982101152105,0.0123025569982902,-0.0104240010100732));
#14310=CARTESIAN_POINT('',(-0.0252906230333307,0.0123632004747365,-0.0104770048657271));
#14311=CARTESIAN_POINT('',(-0.0254945146937632,0.0124579696657952,-0.0105587939314027));
#14312=CARTESIAN_POINT('',(-0.025743724403319,0.0126274685465381,-0.0107027873925713));
#14313=CARTESIAN_POINT('',(-0.0259279713731207,0.0128366549775345,-0.0108769854243933));
#14314=CARTESIAN_POINT('',(-0.0259895224200857,0.0129542591096644,-0.0109744161890341));
#14315=CARTESIAN_POINT('',(-0.0260093506077098,0.0129958591519529,-0.0110097081940201));
#14316=CARTESIAN_POINT('',(-0.0245857864470955,-1.92527892165488E-11,1.05583470944414E-11));
#14317=CARTESIAN_POINT('',(-0.0259999999997638,0.0160355496840746,-0.00575178060268176));
#14318=CARTESIAN_POINT('',(-0.0259999999995772,0.0153483883918416,-0.00766753674812516));
#14319=CARTESIAN_POINT('',(-0.0259999999995979,0.0143144758044963,-0.00945832588025775));
#14320=CARTESIAN_POINT('',(-0.0259999999998258,0.0129989629613864,-0.0110113030887326));
#14321=CARTESIAN_POINT('',(-0.0260046754376191,0.0160340832140701,-0.00575083496141242));
#14322=CARTESIAN_POINT('',(-0.0260093507666748,0.0160326166820256,-0.0057498894970771));
#14323=CARTESIAN_POINT('',(-0.0259634000226623,0.0159135846340675,-0.00570729354502668));
#14324=CARTESIAN_POINT('',(-0.0258372476658943,0.0156726830266146,-0.0056210122147486));
#14325=CARTESIAN_POINT('',(-0.0255181562605256,0.0153800537532759,-0.00551652846150879));
#14326=CARTESIAN_POINT('',(-0.0252574621306131,0.0152385660242035,-0.00546615008668747));
#14327=CARTESIAN_POINT('',(-0.0250772590165566,0.015170455895241,-0.00544222505652501));
#14328=CARTESIAN_POINT('',(-0.0249296521813009,0.0151327465590608,-0.00542885055109215));
#14329=CARTESIAN_POINT('',(-0.0248141730419652,0.0151124466167295,-0.00542152453801596));
#14330=CARTESIAN_POINT('',(-0.0247254103195691,0.0151024228856639,-0.00541763598639992));
#14331=CARTESIAN_POINT('',(-0.0246348999602412,0.0150985816893586,-0.00541597337727203));
#14332=CARTESIAN_POINT('',(-0.0246245061600504,0.0150980256270173,-0.00541537580103899));
#14333=CARTESIAN_POINT('',(-0.0245857965998274,0.0150981180462985,-0.00541540589229385));
#14334=CARTESIAN_POINT('',(-0.0245415219086352,0.016679983194184,-0.00539893765273315));
#14335=CARTESIAN_POINT('',(-0.0259961345406099,0.016841214462651,-0.00488619526152227));
#14336=CARTESIAN_POINT('',(-0.0260209032736197,0.0164680355527262,-0.00505109129460865));
#14337=CARTESIAN_POINT('',(-0.0259762695508448,0.0161735222636546,-0.00536784066556917));
#14338=CARTESIAN_POINT('',(-0.0260105733315168,0.0160358510451588,-0.00575094121468224));
#14339=CARTESIAN_POINT('',(-0.0259980774508441,0.0168413793742882,-0.00488627623713676));
#14340=CARTESIAN_POINT('',(-0.0244999817389172,0.0154061659632965,-0.0044698881448101));
#14341=CARTESIAN_POINT('',(-0.024944756596149,0.015407542773384,-0.00447033717343805));
#14342=CARTESIAN_POINT('',(-0.0257532661791717,0.0158045251349,-0.00457973610997194));
#14343=CARTESIAN_POINT('',(-0.0259959930193616,0.016515907972029,-0.00479205562839269));
#14344=CARTESIAN_POINT('',(-0.0259961548791145,0.0168413289028734,-0.00488645198709862));
#14345=CARTESIAN_POINT('',(-0.0244999999984256,5.24925381567424E-13,-1.62634843653004E-18));
#14346=CARTESIAN_POINT('',(-0.0259999999979621,3.48446901188088E-13,-2.35701788965328E-18));
#14347=CARTESIAN_POINT('',(-0.0259980767574808,0.0168413793587563,0.00488627630154334));
#14348=CARTESIAN_POINT('',(-0.0259961534923684,0.0168413288714539,0.00488645211585265));
#14349=CARTESIAN_POINT('',(-0.025995991136632,0.0165159028049937,0.00479205431631923));
#14350=CARTESIAN_POINT('',(-0.0257532552166203,0.0158045173834629,0.0045797342436974));
#14351=CARTESIAN_POINT('',(-0.0249447500341456,0.0154075456671966,0.00447033815426907));
#14352=CARTESIAN_POINT('',(-0.0244999817278468,0.0154061687726843,0.00446988909050619));
#14353=CARTESIAN_POINT('',(-0.0245418550974137,0.0166788942327279,0.0054022808611622));
#14354=CARTESIAN_POINT('',(-0.026010572631153,0.0160358515601886,0.00575094183466721));
#14355=CARTESIAN_POINT('',(-0.0259762684314615,0.0161735210607565,0.00536784573762992));
#14356=CARTESIAN_POINT('',(-0.0260208848456387,0.0164682834499534,0.00505098197197986));
#14357=CARTESIAN_POINT('',(-0.0259961329744937,0.0168412144868518,0.00488619545012088));
#14358=CARTESIAN_POINT('',(-0.0260046753581802,0.0160340831528961,0.00575083524947786));
#14359=CARTESIAN_POINT('',(-0.02458579659411,0.0150981160505823,0.00541540564052657));
#14360=CARTESIAN_POINT('',(-0.024587878063626,0.0150981110813599,0.00541540402286574));
#14361=CARTESIAN_POINT('',(-0.0246336063429746,0.0150983460190976,0.00541549622229607));
#14362=CARTESIAN_POINT('',(-0.0246879782368823,0.0151008080697915,0.0054163099930172));
#14363=CARTESIAN_POINT('',(-0.0247977856693694,0.0151095371901899,0.00541918568707618));
#14364=CARTESIAN_POINT('',(-0.0249386423737795,0.0151339091886502,0.0054272540938625));
#14365=CARTESIAN_POINT('',(-0.025098210118899,0.015178728184201,0.00544232638726969));
#14366=CARTESIAN_POINT('',(-0.0252906230379044,0.0152549526088682,0.00546834325098496));
#14367=CARTESIAN_POINT('',(-0.0254945146987291,0.0153731686142176,0.00550952124559355));
#14368=CARTESIAN_POINT('',(-0.0257437244077353,0.0155826200512163,0.00558431485227158));
#14369=CARTESIAN_POINT('',(-0.025927971375513,0.0158380731871927,0.00567837659986637));
#14370=CARTESIAN_POINT('',(-0.0259895224208923,0.0159812527677868,0.00573150938270905));
#14371=CARTESIAN_POINT('',(-0.026009350607797,0.0160326165598783,0.00574989007298671));
#14372=CARTESIAN_POINT('',(-0.0245857864470954,-1.92531126805405E-11,-1.05585621839471E-11));
#14373=CARTESIAN_POINT('',(-0.0259999999998258,0.0129989629613864,0.0110113030887327));
#14374=CARTESIAN_POINT('',(-0.0259999999995978,0.0143144758044964,0.00945832588025777));
#14375=CARTESIAN_POINT('',(-0.0259999999995771,0.0153483883918416,0.0076675367481252));
#14376=CARTESIAN_POINT('',(-0.0259999999997637,0.0160355496840746,0.00575178060268182));
#14377=CARTESIAN_POINT('',(-0.0260046754377188,0.0129974107769544,0.0110105059089517));
#14378=CARTESIAN_POINT('',(-0.0260093507668433,0.0129958587141842,0.0110097085877143));
#14379=CARTESIAN_POINT('',(-0.0259634000227723,0.0128994535135814,0.0109279217861875));
#14380=CARTESIAN_POINT('',(-0.0258372476658195,0.0127042808859719,0.0107624355392352));
#14381=CARTESIAN_POINT('',(-0.0255181562605883,0.0124674806650552,0.010561253031256));
#14382=CARTESIAN_POINT('',(-0.0252574621306685,0.0123531078481989,0.0104639102508905));
#14383=CARTESIAN_POINT('',(-0.0250772590166089,0.0122983330998608,0.0104168876640103));
#14384=CARTESIAN_POINT('',(-0.0249296521813909,0.0122678957703277,0.0103909176736192));
#14385=CARTESIAN_POINT('',(-0.0248141730419693,0.0122514012857434,0.0103770004143958));
#14386=CARTESIAN_POINT('',(-0.0247254103198681,0.0122430218357319,0.0103702638844561));
#14387=CARTESIAN_POINT('',(-0.024634899959954,0.0122396613758421,0.01036776861544));
#14388=CARTESIAN_POINT('',(-0.024624506160968,0.0122388658284674,0.0103675858394394));
#14389=CARTESIAN_POINT('',(-0.0245857965998277,0.0122389380979025,0.0103676508312604));
#14390=CARTESIAN_POINT('',(-0.024541521908582,0.0130156087577948,0.0117458203544688));
#14391=CARTESIAN_POINT('',(-0.0259961345402911,0.012652176456026,0.0121418219274446));
#14392=CARTESIAN_POINT('',(-0.026020903273923,0.0126083911539356,0.0117361914938224));
#14393=CARTESIAN_POINT('',(-0.0259762695509608,0.0127354475114188,0.0113227608169304));
#14394=CARTESIAN_POINT('',(-0.0260105733318727,0.012998386710699,0.0110119837691248));
#14395=CARTESIAN_POINT('',(-0.0259980774508218,0.0126523290373502,0.012141924257479));
#14396=CARTESIAN_POINT('',(-0.024499981738918,0.0115741196668296,0.0111071870265766));
#14397=CARTESIAN_POINT('',(-0.0249447565976953,0.0115751969421456,0.0111081548648414));
#14398=CARTESIAN_POINT('',(-0.0257532661814006,0.0118684303832142,0.0113972522082632));
#14399=CARTESIAN_POINT('',(-0.0259959930192577,0.0124079958978922,0.0119071680565776));
#14400=CARTESIAN_POINT('',(-0.0259961548790503,0.0126524560069423,0.0121417926689943));
#14401=CARTESIAN_POINT('',(-0.0244999999971406,5.18764360779374E-13,1.35374416890873E-12));
#14402=CARTESIAN_POINT('',(-0.0259999999972628,3.97088456000253E-13,1.14387320820443E-12));
#14403=CARTESIAN_POINT('',(-0.0259980767575157,0.0041890502732224,0.0170282005132929));
#14404=CARTESIAN_POINT('',(-0.0259961534924216,0.00418887276872869,0.0170282446932658));
#14405=CARTESIAN_POINT('',(-0.0259959911365039,0.00410791062794049,0.0166992185530027));
#14406=CARTESIAN_POINT('',(-0.0257532552162604,0.00393609249381923,0.0159769806701362));
#14407=CARTESIAN_POINT('',(-0.0249447500340041,0.00383234642828381,0.0155784950348394));
#14408=CARTESIAN_POINT('',(-0.0244999817278479,0.00383204688165825,0.015577078077351));
#14409=CARTESIAN_POINT('',(-0.0245418550973269,0.00366093465259704,0.0171454865430141));
#14410=CARTESIAN_POINT('',(-0.0260105726312166,0.00303746405549769,0.0167629257403239));
#14411=CARTESIAN_POINT('',(-0.0259762684315379,0.00343806975865812,0.0166906029764942));
#14412=CARTESIAN_POINT('',(-0.0260208848459788,0.00385986302468689,0.0167874428113377));
#14413=CARTESIAN_POINT('',(-0.0259961329744237,0.00418903785749696,0.0170280173031582));
#14414=CARTESIAN_POINT('',(-0.0260046753582004,0.00303667215730485,0.0167613409619478));
#14415=CARTESIAN_POINT('',(-0.0245857965941096,0.00285917916856925,0.0157830548693242));
#14416=CARTESIAN_POINT('',(-0.025090940149948,0.00285891617560677,0.0157818141848353));
#14417=CARTESIAN_POINT('',(-0.0258263367235061,0.00295388482187573,0.0162565491158958));
#14418=CARTESIAN_POINT('',(-0.0259713996501372,0.00301806968242363,0.0166568692504878));
#14419=CARTESIAN_POINT('',(-0.0260093506078376,0.00303675740795713,0.0167595982669812));
#14420=CARTESIAN_POINT('',(-0.0245857864487112,1.42203703998203E-12,5.38366735710928E-12));
#14421=CARTESIAN_POINT('',(-0.0259999999997604,1.73586899341303E-17,0.0170358983844952));
#14422=CARTESIAN_POINT('',(-0.0259999999997042,0.00101763355997381,0.0170358983845614));
#14423=CARTESIAN_POINT('',(-0.0259999999997053,0.00203524965503534,0.0169444731601271));
#14424=CARTESIAN_POINT('',(-0.0259999999997637,0.00303658672267139,0.0167630836914287));
#14425=CARTESIAN_POINT('',(-0.0260000001248802,-1.15781674900619E-18,0.0170358983847476));
#14426=CARTESIAN_POINT('',(-0.0245857864377007,1.10730438962528E-13,0.0175358983847132));
#14427=CARTESIAN_POINT('',(-0.0245857864487102,-1.42200809927133E-12,5.38360248515839E-12));
#14428=CARTESIAN_POINT('',(-0.0259999999997637,-0.00303658672267143,0.0167630836914286));
#14429=CARTESIAN_POINT('',(-0.0259999999997053,-0.00203524965503538,0.0169444731601271));
#14430=CARTESIAN_POINT('',(-0.0259999999997041,-0.00101763355997385,0.0170358983845614));
#14431=CARTESIAN_POINT('',(-0.0259999999997604,-4.77083853987333E-17,0.0170358983844952));
#14432=CARTESIAN_POINT('',(-0.0260046754377279,-0.00303667243689323,0.0167613408708776));
#14433=CARTESIAN_POINT('',(-0.0260093507668927,-0.00303675796778805,0.0167595980847398));
#14434=CARTESIAN_POINT('',(-0.0259714110358408,-0.00301807586534209,0.0166569001128961));
#14435=CARTESIAN_POINT('',(-0.0258263830287078,-0.00295389696213839,0.0162566051611366));
#14436=CARTESIAN_POINT('',(-0.0250909731285228,-0.00285891698418111,0.0157818158485132));
#14437=CARTESIAN_POINT('',(-0.0245857965998287,-0.0028591799484582,0.0157830567238613));
#14438=CARTESIAN_POINT('',(-0.0245415219087568,-0.00366437443651449,0.0171447580071625));
#14439=CARTESIAN_POINT('',(-0.0259961345404462,-0.00418903800884105,0.0170280171879839));
#14440=CARTESIAN_POINT('',(-0.0260209032740159,-0.00385964439988298,0.0167872827872964));
#14441=CARTESIAN_POINT('',(-0.0259762695510075,-0.00343807475236031,0.0166906014821321));
#14442=CARTESIAN_POINT('',(-0.0260105733318218,-0.0030374643344677,0.0167629249843816));
#14443=CARTESIAN_POINT('',(-0.0259980774508371,-0.00418905033688052,0.0170282004946286));
#14444=CARTESIAN_POINT('',(-0.0244999817389183,-0.00383204629596097,0.0155770751714919));
#14445=CARTESIAN_POINT('',(-0.0249447565965779,-0.0038323458308052,0.0155784920383121));
#14446=CARTESIAN_POINT('',(-0.0257532661796553,-0.00393609475357222,0.015976988317185));
#14447=CARTESIAN_POINT('',(-0.0259959930191771,-0.0041079120753024,0.0166992236843931));
#14448=CARTESIAN_POINT('',(-0.0259961548790839,-0.0041888728959336,0.0170282446561009));
#14449=CARTESIAN_POINT('',(-0.0244999999971407,-5.18631834631121E-13,1.35352719870077E-12));
#14450=CARTESIAN_POINT('',(-0.025999999997263,-3.96961679161639E-13,1.14366711529932E-12));
#14451=CARTESIAN_POINT('',(-0.0259980767575473,-0.0126523290853398,0.0121419242116851));
#14452=CARTESIAN_POINT('',(-0.0259961534924817,-0.0126524561027242,0.012141792577421));
#14453=CARTESIAN_POINT('',(-0.0259959911366461,-0.012407992177481,0.0119071642372684));
#14454=CARTESIAN_POINT('',(-0.0257532552176058,-0.0118684248903005,0.011397246427474));
#14455=CARTESIAN_POINT('',(-0.0249447500348285,-0.0115751992386655,0.0111081568807063));
#14456=CARTESIAN_POINT('',(-0.0244999817278477,-0.011574121890793,0.011107188986971));
#14457=CARTESIAN_POINT('',(-0.0245418550974116,-0.0130179595803988,0.0117432056821331));
#14458=CARTESIAN_POINT('',(-0.0260105726312484,-0.0129983875048527,0.0110119839054969));
#14459=CARTESIAN_POINT('',(-0.0259762684314917,-0.0127354513024245,0.0113227572394375));
#14460=CARTESIAN_POINT('',(-0.0260208848459214,-0.0126084204264179,0.0117364608404772));
#14461=CARTESIAN_POINT('',(-0.0259961329743619,-0.0126521766314437,0.0121418218539703));
#14462=CARTESIAN_POINT('',(-0.0260046753581827,-0.0129974109956148,0.0110105057123484));
#14463=CARTESIAN_POINT('',(-0.0245857965941096,-0.0122389368819011,0.0103676492287045));
#14464=CARTESIAN_POINT('',(-0.0250909401471701,-0.0122379939140726,0.0103668011278518));
#14465=CARTESIAN_POINT('',(-0.0258263367195619,-0.0126016420976086,0.0106864138505677));
#14466=CARTESIAN_POINT('',(-0.0259713996491344,-0.01291623707483,0.010942159639068));
#14467=CARTESIAN_POINT('',(-0.0260093506077712,-0.0129958591519313,0.0110097081940098));
#14468=CARTESIAN_POINT('',(-0.0245857864470955,1.92530944572749E-11,-1.05585582240299E-11));
#14469=CARTESIAN_POINT('',(-0.0259999999997637,-0.0160355496840745,0.00575178060268177));
#14470=CARTESIAN_POINT('',(-0.0259999999995771,-0.0153483883918416,0.00766753674812515));
#14471=CARTESIAN_POINT('',(-0.0259999999995978,-0.0143144758044963,0.00945832588025774));
#14472=CARTESIAN_POINT('',(-0.0259999999998258,-0.0129989629613864,0.0110113030887326));
#14473=CARTESIAN_POINT('',(-0.0260046754376107,-0.0160340832137518,0.0057508349623088));
#14474=CARTESIAN_POINT('',(-0.0260093507666581,-0.0160326166820308,0.00574988949708065));
#14475=CARTESIAN_POINT('',(-0.025971411035752,-0.0159343365787225,0.0057147196865982));
#14476=CARTESIAN_POINT('',(-0.0258263830290665,-0.0155555815303819,0.00557015277131583));
#14477=CARTESIAN_POINT('',(-0.025090973128876,-0.015096911934659,0.00541501318838743));
#14478=CARTESIAN_POINT('',(-0.0245857965998274,-0.0150981180463038,0.00541540589229551));
#14479=CARTESIAN_POINT('',(-0.0245415219086213,-0.0166799831941954,0.00539893765274277));
#14480=CARTESIAN_POINT('',(-0.0259961345406086,-0.0168412144627859,0.00488619526146272));
#14481=CARTESIAN_POINT('',(-0.0260209032736532,-0.0164680355525104,0.00505109129466021));
#14482=CARTESIAN_POINT('',(-0.0259762695507925,-0.016173522263216,0.00536784066603291));
#14483=CARTESIAN_POINT('',(-0.0260105733315772,-0.0160358510448399,0.0057509412155698));
#14484=CARTESIAN_POINT('',(-0.0259980774508479,-0.0168413793744232,0.00488627623707682));
#14485=CARTESIAN_POINT('',(-0.0244999817389172,-0.0154061659632896,0.00446988814480776));
#14486=CARTESIAN_POINT('',(-0.024944756596158,-0.0154075427733792,0.00447033717343636));
#14487=CARTESIAN_POINT('',(-0.0257532661791859,-0.0158045251349107,0.0045797361099757));
#14488=CARTESIAN_POINT('',(-0.025995993019367,-0.0165159079720358,0.00479205562839404));
#14489=CARTESIAN_POINT('',(-0.0259961548791221,-0.0168413289028737,0.00488645198709787));
#14490=CARTESIAN_POINT('',(-0.0244999999984257,-5.24694626034855E-13,7.65719141414477E-19));
#14491=CARTESIAN_POINT('',(-0.0259999999979621,-3.48223200806651E-13,4.6127030534049E-19));
#14492=CARTESIAN_POINT('',(-0.0259980767574809,-0.0168413793586215,-0.00488627630160291));
#14493=CARTESIAN_POINT('',(-0.0259961534923684,-0.0168413288714539,-0.00488645211585266));
#14494=CARTESIAN_POINT('',(-0.025995991136632,-0.0165159028049937,-0.00479205431631923));
#14495=CARTESIAN_POINT('',(-0.0257532552166203,-0.0158045173834629,-0.00457973424369741));
#14496=CARTESIAN_POINT('',(-0.0249447500341456,-0.0154075456671966,-0.00447033815426907));
#14497=CARTESIAN_POINT('',(-0.0244999817278467,-0.0154061687726844,-0.00446988909050619));
#14498=CARTESIAN_POINT('',(-0.0245418550974135,-0.0166788942327286,-0.00540228086116028));
#14499=CARTESIAN_POINT('',(-0.0260105726311714,-0.0160358515601145,-0.00575094183487335));
#14500=CARTESIAN_POINT('',(-0.0259762684314567,-0.0161735210606341,-0.00536784573779487));
#14501=CARTESIAN_POINT('',(-0.0260208848456298,-0.0164682834498121,-0.00505098197208591));
#14502=CARTESIAN_POINT('',(-0.0259961329745026,-0.0168412144867175,-0.00488619545018022));
#14503=CARTESIAN_POINT('',(-0.0260046753581802,-0.0160340831528214,-0.00575083524968604));
#14504=CARTESIAN_POINT('',(-0.02458579659411,-0.0150981160505823,-0.00541540564052657));
#14505=CARTESIAN_POINT('',(-0.0250909401516257,-0.0150969100897713,-0.00541501305685423));
#14506=CARTESIAN_POINT('',(-0.0258263367258225,-0.015555526925824,-0.0055701352631442));
#14507=CARTESIAN_POINT('',(-0.0259713996506763,-0.0159343067607731,-0.00571470961034891));
#14508=CARTESIAN_POINT('',(-0.026009350607797,-0.0160326165598783,-0.00574989007298672));
#14509=CARTESIAN_POINT('',(-0.0245857864470955,1.92527724721921E-11,1.05583478911826E-11));
#14510=CARTESIAN_POINT('',(-0.0259999999998258,-0.0129989629613864,-0.0110113030887327));
#14511=CARTESIAN_POINT('',(-0.0259999999995979,-0.0143144758044963,-0.00945832588025778));
#14512=CARTESIAN_POINT('',(-0.0259999999995772,-0.0153483883918416,-0.00766753674812521));
#14513=CARTESIAN_POINT('',(-0.0259999999997638,-0.0160355496840745,-0.00575178060268184));
#14514=CARTESIAN_POINT('',(-0.0260046754377188,-0.0129974107760712,-0.0110105059099944));
#14515=CARTESIAN_POINT('',(-0.0260093507668434,-0.0129958587141842,-0.0110097085877143));
#14516=CARTESIAN_POINT('',(-0.0259714110351495,-0.0129162607116119,-0.0109421804253578));
#14517=CARTESIAN_POINT('',(-0.0258263830259916,-0.0126016845651491,-0.0106864523879323));
#14518=CARTESIAN_POINT('',(-0.0250909731266351,-0.0122379949504956,-0.0103668026598678));
#14519=CARTESIAN_POINT('',(-0.0245857965998277,-0.0122389380979025,-0.0103676508312604));
#14520=CARTESIAN_POINT('',(-0.0245415219085822,-0.0130156087577962,-0.0117458203544672));
#14521=CARTESIAN_POINT('',(-0.0259961345402822,-0.0126521764560418,-0.0121418219275906));
#14522=CARTESIAN_POINT('',(-0.0260209032739087,-0.0126083911539552,-0.0117361914943769));
#14523=CARTESIAN_POINT('',(-0.0259762695510121,-0.0127354475110793,-0.0113227608179002));
#14524=CARTESIAN_POINT('',(-0.0260105733317587,-0.0129983867098248,-0.011011983770158));
#14525=CARTESIAN_POINT('',(-0.0259980774508218,-0.012652329037366,-0.0121419242576256));
#14526=CARTESIAN_POINT('',(-0.024499981738918,-0.0115741196668296,-0.0111071870265765));
#14527=CARTESIAN_POINT('',(-0.0249447565976953,-0.0115751969421456,-0.0111081548648414));
#14528=CARTESIAN_POINT('',(-0.0257532661814006,-0.0118684303832142,-0.0113972522082632));
#14529=CARTESIAN_POINT('',(-0.0259959930192577,-0.0124079958978922,-0.0119071680565776));
#14530=CARTESIAN_POINT('',(-0.0259961548790503,-0.0126524560069422,-0.0121417926689943));
#14531=CARTESIAN_POINT('',(-0.0244999999971407,-5.18644711631284E-13,-1.35354294616328E-12));
#14532=CARTESIAN_POINT('',(-0.025999999997263,-3.9697401421664E-13,-1.14368187585572E-12));
#14533=CARTESIAN_POINT('',(-0.0259980767575158,-0.00418905027313784,-0.0170282005132274));
#14534=CARTESIAN_POINT('',(-0.0259961534924215,-0.00418887276872622,-0.0170282446932557));
#14535=CARTESIAN_POINT('',(-0.0259959911365014,-0.00410791062793844,-0.0166992185529941));
#14536=CARTESIAN_POINT('',(-0.0257532552162551,-0.00393609249381833,-0.0159769806701326));
#14537=CARTESIAN_POINT('',(-0.0249447500340021,-0.00383234642828381,-0.0155784950348394));
#14538=CARTESIAN_POINT('',(-0.0244999817278479,-0.00383204688165824,-0.015577078077351));
#14539=CARTESIAN_POINT('',(-0.0245418550973269,-0.00366093465259706,-0.0171454865430142));
#14540=CARTESIAN_POINT('',(-0.0260105726395446,-0.00303746395823507,-0.0167629257578844));
#14541=CARTESIAN_POINT('',(-0.0259762952739958,-0.00343775617407728,-0.0166906595617935));
#14542=CARTESIAN_POINT('',(-0.026020876834144,-0.00385996963576985,-0.0167875207162035));
#14543=CARTESIAN_POINT('',(-0.0259961329724585,-0.00418903788362998,-0.0170280173222573));
#14544=CARTESIAN_POINT('',(-0.046,4.85722573273506E-19,3.46944695195362E-20));
#14545=CARTESIAN_POINT('',(-0.0460000000004017,-1.91988200481306E-13,-2.26738972774339E-20));
#14546=CARTESIAN_POINT('',(-0.0460000000004512,0.0157358983848686,-2.26738972774339E-20));
#14547=CARTESIAN_POINT('',(-0.019,0.,0.));
#14548=CARTESIAN_POINT('',(-0.02600000025,0.00303658672694563,-0.016763083691069));
#14549=CARTESIAN_POINT('',(-0.027000000125,0.00303658672694563,-0.016763083691069));
#14550=CARTESIAN_POINT('',(-0.028,0.00303658672694563,-0.016763083691069));
#14551=CARTESIAN_POINT('',(-0.028999999875,0.00303658672694563,-0.016763083691069));
#14552=CARTESIAN_POINT('',(-0.028999999875,0.00303658672474891,-0.0167630836915008));
#14553=CARTESIAN_POINT('',(-0.029,-0.00303658672393521,-0.0167630836916143));
#14554=CARTESIAN_POINT('',(-0.0280000000833333,-0.00303658672393521,-0.0167630836916143));
#14555=CARTESIAN_POINT('',(-0.0270000001666667,-0.00303658672393521,-0.0167630836916143));
#14556=CARTESIAN_POINT('',(-0.02600000025,-0.00303658672393521,-0.0167630836916143));
#14557=CARTESIAN_POINT('',(-0.029,-0.00303658672114831,-0.016763083692153));
#14558=CARTESIAN_POINT('',(-0.029,0.,0.));
#14559=CARTESIAN_POINT('',(-0.019,0.003303956249,-0.018239062532));
#14560=CARTESIAN_POINT('',(-0.029,0.003303956249,-0.018239062532));
#14561=CARTESIAN_POINT('',(-0.0289999998749999,0.00436461653820612,-0.0171784024646543));
#14562=CARTESIAN_POINT('',(-0.02899999975,0.00436461642035826,-0.0171784023597986));
#14563=CARTESIAN_POINT('',(-0.0279999999166667,0.00436461642035826,-0.0171784023597986));
#14564=CARTESIAN_POINT('',(-0.0270000000833333,0.00436461642035826,-0.0171784023597986));
#14565=CARTESIAN_POINT('',(-0.02600000025,0.00436461642035826,-0.0171784023597986));
#14566=CARTESIAN_POINT('',(-0.026,0.00436461886889965,-0.0171784047953479));
#14567=CARTESIAN_POINT('',(-0.026,0.003303956249,-0.018239062532));
#14568=CARTESIAN_POINT('',(-0.026,-2.55351295663786E-17,-2.63677968348474E-18));
#14569=CARTESIAN_POINT('',(-0.0260000000001354,-1.37314950086772E-13,2.61821090022989E-18));
#14570=CARTESIAN_POINT('',(-0.0260000000000933,0.0329999999999944,2.61821090022989E-18));
#14571=CARTESIAN_POINT('',(-0.026,0.00436461672182346,0.0171784026352795));
#14572=CARTESIAN_POINT('',(-0.026,0.00545695029196146,0.0182707362276815));
#14573=CARTESIAN_POINT('',(-0.026,0.00654928386209946,0.0193630698200835));
#14574=CARTESIAN_POINT('',(-0.026,0.00764161743223745,0.0204554034124854));
#14575=CARTESIAN_POINT('',(-0.026000000125,0.00436461642085125,0.0171784023602916));
#14576=CARTESIAN_POINT('',(-0.0260000001249999,0.00764161753161064,0.0204554034909548));
#14577=CARTESIAN_POINT('',(-0.026,0.003303956249,0.018239062532));
#14578=CARTESIAN_POINT('',(-0.026,0.014143513369,0.011980841311));
#14579=CARTESIAN_POINT('',(-0.0260000001249999,0.0126946255340264,0.0123690732293488));
#14580=CARTESIAN_POINT('',(-0.026,0.0138940902881418,0.0168455365833053));
#14581=CARTESIAN_POINT('',(-0.026,0.0134942687055029,0.0153533821314328));
#14582=CARTESIAN_POINT('',(-0.026,0.0130944471228641,0.0138612276795603));
#14583=CARTESIAN_POINT('',(-0.026,0.0126946255402253,0.0123690732276878));
#14584=CARTESIAN_POINT('',(-0.026000000125,0.013894090320796,0.0168455367788748));
#14585=CARTESIAN_POINT('',(-0.026,0.01534297906,0.016457308211));
#14586=CARTESIAN_POINT('',(-0.026000000125,0.016365844330921,0.0175544620917123));
#14587=CARTESIAN_POINT('',(-0.026,0.,0.));
#14588=CARTESIAN_POINT('',(-0.026000000125,0.0233855322877997,0.00539600589483076));
#14589=CARTESIAN_POINT('',(-0.026,0.021923936519,0.00505875553));
#14590=CARTESIAN_POINT('',(-0.0260000001249999,0.0215357078290251,0.00360986683636835));
#14591=CARTESIAN_POINT('',(-0.026,0.0170592414781658,0.00480933239988356));
#14592=CARTESIAN_POINT('',(-0.026,0.0185513968874907,0.00440951056069614));
#14593=CARTESIAN_POINT('',(-0.026,0.0200435522968155,0.00400968872150873));
#14594=CARTESIAN_POINT('',(-0.026,0.0215357077061403,0.00360986688232132));
#14595=CARTESIAN_POINT('',(-0.026000000125,0.0170592410507286,0.00480933248146393));
#14596=CARTESIAN_POINT('',(-0.026,0.017447469618,0.006258221221));
#14597=CARTESIAN_POINT('',(-0.026,0.017447469618,-0.006258221221));
#14598=CARTESIAN_POINT('',(-0.0260000001249999,0.0170592444030468,-0.00480933159968851));
#14599=CARTESIAN_POINT('',(-0.026,0.0215357077103104,-0.00360986688120394));
#14600=CARTESIAN_POINT('',(-0.026,0.0200435532759288,-0.00400968845915609));
#14601=CARTESIAN_POINT('',(-0.026,0.0185513988415473,-0.00440951003710825));
#14602=CARTESIAN_POINT('',(-0.026,0.0170592444071657,-0.0048093316150604));
#14603=CARTESIAN_POINT('',(-0.026000000125,0.0215357079510786,-0.00360986679080852));
#14604=CARTESIAN_POINT('',(-0.026,0.021923936519,-0.00505875553));
#14605=CARTESIAN_POINT('',(-0.026000000125,0.0233855322869016,-0.00539600589872286));
#14606=CARTESIAN_POINT('',(-0.026,0.,0.));
#14607=CARTESIAN_POINT('',(-0.026000000125,0.0163658443295185,-0.0175544620930199));
#14608=CARTESIAN_POINT('',(-0.026,0.01534297906,-0.016457308211));
#14609=CARTESIAN_POINT('',(-0.0260000001249999,0.013894090297154,-0.0168455366541086));
#14610=CARTESIAN_POINT('',(-0.026,0.0126946247563403,-0.0123690703021891));
#14611=CARTESIAN_POINT('',(-0.026,0.0130944465955277,-0.013861225711514));
#14612=CARTESIAN_POINT('',(-0.026,0.0134942684347151,-0.015353381120839));
#14613=CARTESIAN_POINT('',(-0.026,0.0138940902739026,-0.0168455365301639));
#14614=CARTESIAN_POINT('',(-0.026000000125,0.012694624629357,-0.0123690698778722));
#14615=CARTESIAN_POINT('',(-0.026,0.014143513369,-0.011980841311));
#14616=CARTESIAN_POINT('',(-0.026,0.00764161743223745,-0.0204554034124855));
#14617=CARTESIAN_POINT('',(-0.026,0.00654928457995689,-0.0193630705379409));
#14618=CARTESIAN_POINT('',(-0.026,0.00545695172767632,-0.0182707376633963));
#14619=CARTESIAN_POINT('',(-0.026,0.00436461887539576,-0.0171784047888518));
#14620=CARTESIAN_POINT('',(-0.026000000125,0.00764161763081172,-0.0204554035695319));
#14621=CARTESIAN_POINT('',(-0.026,0.006580957459,-0.021516063741));
#14622=CARTESIAN_POINT('',(-0.026000000125,0.00701968795640335,-0.0229504679905696));
#14623=CARTESIAN_POINT('',(-0.026,0.,0.));
#14624=CARTESIAN_POINT('',(-0.026000000125,-0.00701968795550563,-0.0229504679908442));
#14625=CARTESIAN_POINT('',(-0.026,-0.006580957459,-0.021516063741));
#14626=CARTESIAN_POINT('',(-0.0260000001249999,-0.0076416175313931,-0.0204554034907373));
#14627=CARTESIAN_POINT('',(-0.026,-0.00436461672182347,-0.0171784026352795));
#14628=CARTESIAN_POINT('',(-0.026,-0.00545695029196146,-0.0182707362276815));
#14629=CARTESIAN_POINT('',(-0.026,-0.00654928386209946,-0.0193630698200835));
#14630=CARTESIAN_POINT('',(-0.026,-0.00764161743223745,-0.0204554034124855));
#14631=CARTESIAN_POINT('',(-0.026000000125,-0.00436461642041616,-0.0171784023598565));
#14632=CARTESIAN_POINT('',(-0.026,-0.003303956249,-0.018239062532));
#14633=CARTESIAN_POINT('',(-0.026,-0.014143513369,-0.011980841311));
#14634=CARTESIAN_POINT('',(-0.0260000001249999,-0.0126946255341409,-0.0123690732297761));
#14635=CARTESIAN_POINT('',(-0.026,-0.0138940902739026,-0.0168455365301639));
#14636=CARTESIAN_POINT('',(-0.026,-0.0134942686960483,-0.0153533820961476));
#14637=CARTESIAN_POINT('',(-0.026,-0.013094447118194,-0.0138612276621313));
#14638=CARTESIAN_POINT('',(-0.026,-0.0126946255403397,-0.0123690732281151));
#14639=CARTESIAN_POINT('',(-0.026000000125,-0.01389409032085,-0.0168455367790761));
#14640=CARTESIAN_POINT('',(-0.026,-0.01534297906,-0.016457308211));
#14641=CARTESIAN_POINT('',(-0.026000000125,-0.0163658443305974,-0.017554462092014));
#14642=CARTESIAN_POINT('',(-0.026,0.,0.));
#14643=CARTESIAN_POINT('',(-0.026000000125,-0.0233855322862084,-0.00539600590172708));
#14644=CARTESIAN_POINT('',(-0.026,-0.021923936519,-0.00505875553));
#14645=CARTESIAN_POINT('',(-0.0260000001249999,-0.0215357078306828,-0.00360986683592415));
#14646=CARTESIAN_POINT('',(-0.026,-0.0170592414781658,-0.00480933239988355));
#14647=CARTESIAN_POINT('',(-0.026,-0.0185513968888807,-0.00440951056032368));
#14648=CARTESIAN_POINT('',(-0.026,-0.0200435522995956,-0.00400968872076381));
#14649=CARTESIAN_POINT('',(-0.026,-0.0215357077103104,-0.00360986688120394));
#14650=CARTESIAN_POINT('',(-0.026000000125,-0.0170592410498741,-0.0048093324816929));
#14651=CARTESIAN_POINT('',(-0.026,-0.017447469618,-0.006258221221));
#14652=CARTESIAN_POINT('',(-0.026,-0.017447469618,0.006258221221));
#14653=CARTESIAN_POINT('',(-0.0260000001249999,-0.0170592444034741,0.00480933159957403));
#14654=CARTESIAN_POINT('',(-0.026,-0.0215357077061403,0.00360986688232132));
#14655=CARTESIAN_POINT('',(-0.026,-0.0200435532732912,0.00400968845986285));
#14656=CARTESIAN_POINT('',(-0.026,-0.0185513988404421,0.00440951003740437));
#14657=CARTESIAN_POINT('',(-0.026,-0.017059244407593,0.0048093316149459));
#14658=CARTESIAN_POINT('',(-0.026000000125,-0.0215357079515059,0.00360986679069403));
#14659=CARTESIAN_POINT('',(-0.026,-0.021923936519,0.00505875553));
#14660=CARTESIAN_POINT('',(-0.026000000125,-0.0233855322868325,0.00539600589902264));
#14661=CARTESIAN_POINT('',(-0.026,0.,0.));
#14662=CARTESIAN_POINT('',(-0.026000000125,-0.0163658443346953,0.0175544620881936));
#14663=CARTESIAN_POINT('',(-0.026,-0.01534297906,0.016457308211));
#14664=CARTESIAN_POINT('',(-0.0260000001249999,-0.0138940903043532,0.0168455366809765));
#14665=CARTESIAN_POINT('',(-0.026,-0.0126946247563402,0.0123690703021891));
#14666=CARTESIAN_POINT('',(-0.026,-0.0130944466002741,0.0138612257292278));
#14667=CARTESIAN_POINT('',(-0.026,-0.0134942684442079,0.0153533811562665));
#14668=CARTESIAN_POINT('',(-0.026,-0.0138940902881418,0.0168455365833052));
#14669=CARTESIAN_POINT('',(-0.026000000125,-0.0126946246295162,0.0123690698784665));
#14670=CARTESIAN_POINT('',(-0.026,-0.014143513369,0.011980841311));
#14671=CARTESIAN_POINT('',(-0.026,-0.003303956249,0.018239062532));
#14672=CARTESIAN_POINT('',(-0.0260000001249999,-0.00436461886924978,0.017178404795698));
#14673=CARTESIAN_POINT('',(-0.026,-0.00764161743223745,0.0204554034124854));
#14674=CARTESIAN_POINT('',(-0.026,-0.00654928458007359,0.0193630705380576));
#14675=CARTESIAN_POINT('',(-0.026,-0.00545695172790972,0.0182707376636298));
#14676=CARTESIAN_POINT('',(-0.026,-0.00436461887574586,0.0171784047892019));
#14677=CARTESIAN_POINT('',(-0.026000000125,-0.00764161763077926,0.0204554035694995));
#14678=CARTESIAN_POINT('',(-0.026,-0.006580957459,0.021516063741));
#14679=CARTESIAN_POINT('',(-0.026000000125,-0.00701968795610915,0.0229504679906597));
#14680=CARTESIAN_POINT('',(-0.026,0.,0.));
#14681=CARTESIAN_POINT('',(-0.026000000125,0.00701968795079842,0.022950467992284));
#14682=CARTESIAN_POINT('',(-0.026,0.006580957459,0.021516063741));
#14683=CARTESIAN_POINT('',(-0.026,0.027720932313,-0.010089594228));
#14684=CARTESIAN_POINT('',(-0.026,0.027720932313,-0.011389594228));
#14685=CARTESIAN_POINT('',(-0.026,0.022598311072,-0.018962234486));
#14686=CARTESIAN_POINT('',(-0.026,0.022598311072,-0.020262234486));
#14687=CARTESIAN_POINT('',(-0.026,0.01475,-0.025547749412));
#14688=CARTESIAN_POINT('',(-0.026,0.01475,-0.026847749412));
#14689=CARTESIAN_POINT('',(-0.026,0.005122621241,-0.029051828714));
#14690=CARTESIAN_POINT('',(-0.026,0.005122621241,-0.030351828714));
#14691=CARTESIAN_POINT('',(-0.026,-0.005122621241,-0.029051828714));
#14692=CARTESIAN_POINT('',(-0.026,-0.005122621241,-0.030351828714));
#14693=CARTESIAN_POINT('',(-0.026,-0.01475,-0.025547749412));
#14694=CARTESIAN_POINT('',(-0.026,-0.01475,-0.026847749412));
#14695=CARTESIAN_POINT('',(-0.026,-0.022598311072,-0.018962234486));
#14696=CARTESIAN_POINT('',(-0.026,-0.022598311072,-0.020262234486));
#14697=CARTESIAN_POINT('',(-0.026,-0.027720932313,-0.010089594228));
#14698=CARTESIAN_POINT('',(-0.026,-0.027720932313,-0.011389594228));
#14699=CARTESIAN_POINT('',(-0.026,-0.0295,0.));
#14700=CARTESIAN_POINT('',(-0.026,-0.0295,-0.0013));
#14701=CARTESIAN_POINT('',(-0.026,-0.027720932313,0.010089594228));
#14702=CARTESIAN_POINT('',(-0.026,-0.027720932313,0.008789594228));
#14703=CARTESIAN_POINT('',(-0.026,-0.022598311072,0.018962234486));
#14704=CARTESIAN_POINT('',(-0.026,-0.022598311072,0.017662234486));
#14705=CARTESIAN_POINT('',(-0.026,-0.01475,0.025547749412));
#14706=CARTESIAN_POINT('',(-0.026,-0.01475,0.024247749412));
#14707=CARTESIAN_POINT('',(-0.026,-0.005122621241,0.029051828714));
#14708=CARTESIAN_POINT('',(-0.026,-0.005122621241,0.027751828714));
#14709=CARTESIAN_POINT('',(-0.026,0.005122621241,0.029051828714));
#14710=CARTESIAN_POINT('',(-0.026,0.005122621241,0.027751828714));
#14711=CARTESIAN_POINT('',(-0.026,0.01475,0.025547749412));
#14712=CARTESIAN_POINT('',(-0.026,0.01475,0.024247749412));
#14713=CARTESIAN_POINT('',(-0.026,0.022598311072,0.018962234486));
#14714=CARTESIAN_POINT('',(-0.026,0.022598311072,0.017662234486));
#14715=CARTESIAN_POINT('',(-0.026,0.027720932313,0.010089594228));
#14716=CARTESIAN_POINT('',(-0.026,0.027720932313,0.008789594228));
#14717=CARTESIAN_POINT('',(-0.026,0.0295,0.));
#14718=CARTESIAN_POINT('',(-0.026,0.0295,-0.0013));
#14719=CARTESIAN_POINT('',(-0.019,0.014143513369,-0.011980841311));
#14720=CARTESIAN_POINT('',(-0.02600000025,0.0126946246294055,-0.0123690698780533));
#14721=CARTESIAN_POINT('',(-0.0270000000833333,0.0126946246294055,-0.0123690698780533));
#14722=CARTESIAN_POINT('',(-0.0279999999166667,0.0126946246294055,-0.0123690698780533));
#14723=CARTESIAN_POINT('',(-0.02899999975,0.0126946246294055,-0.0123690698780533));
#14724=CARTESIAN_POINT('',(-0.029,0.0126946246726379,-0.0123690700146031));
#14725=CARTESIAN_POINT('',(-0.029,0.014143513369,-0.011980841311));
#14726=CARTESIAN_POINT('',(-0.028999999875,0.012998962961142,-0.0110113030890252));
#14727=CARTESIAN_POINT('',(-0.028999999875,0.0129989629609766,-0.0110113030892194));
#14728=CARTESIAN_POINT('',(-0.028,0.0129989629609766,-0.0110113030892194));
#14729=CARTESIAN_POINT('',(-0.027000000125,0.0129989629609766,-0.0110113030892194));
#14730=CARTESIAN_POINT('',(-0.02600000025,0.0129989629609766,-0.0110113030892194));
#14731=CARTESIAN_POINT('',(-0.019,0.,0.));
#14732=CARTESIAN_POINT('',(-0.02600000025,0.0160355496845724,-0.00575178060235749));
#14733=CARTESIAN_POINT('',(-0.027000000125,0.0160355496845724,-0.00575178060235749));
#14734=CARTESIAN_POINT('',(-0.028,0.0160355496845724,-0.00575178060235749));
#14735=CARTESIAN_POINT('',(-0.028999999875,0.0160355496845724,-0.00575178060235749));
#14736=CARTESIAN_POINT('',(-0.028999999875,0.016035549684198,-0.00575178060272061));
#14737=CARTESIAN_POINT('',(-0.029,0.,0.));
#14738=CARTESIAN_POINT('',(-0.019,0.017447469618,-0.006258221221));
#14739=CARTESIAN_POINT('',(-0.029,0.017447469618,-0.006258221221));
#14740=CARTESIAN_POINT('',(-0.0289999998749999,0.0170592411886433,-0.00480933246098534));
#14741=CARTESIAN_POINT('',(-0.02899999975,0.017059241049795,-0.0048093324817141));
#14742=CARTESIAN_POINT('',(-0.0279999999166667,0.017059241049795,-0.0048093324817141));
#14743=CARTESIAN_POINT('',(-0.0270000000833333,0.017059241049795,-0.0048093324817141));
#14744=CARTESIAN_POINT('',(-0.02600000025,0.017059241049795,-0.0048093324817141));
#14745=CARTESIAN_POINT('',(-0.019,0.017447469618,0.006258221221));
#14746=CARTESIAN_POINT('',(-0.02600000025,0.0170592410509098,0.0048093324814154));
#14747=CARTESIAN_POINT('',(-0.0270000000833333,0.0170592410509098,0.0048093324814154));
#14748=CARTESIAN_POINT('',(-0.0279999999166667,0.0170592410509098,0.0048093324814154));
#14749=CARTESIAN_POINT('',(-0.02899999975,0.0170592410509098,0.0048093324814154));
#14750=CARTESIAN_POINT('',(-0.029,0.0170592411890195,0.00480933246088452));
#14751=CARTESIAN_POINT('',(-0.029,0.017447469618,0.006258221221));
#14752=CARTESIAN_POINT('',(-0.028999999875,0.0160355496840715,0.00575178060307333));
#14753=CARTESIAN_POINT('',(-0.028999999875,0.0160355496838868,0.00575178060290777));
#14754=CARTESIAN_POINT('',(-0.028,0.0160355496838868,0.00575178060290777));
#14755=CARTESIAN_POINT('',(-0.027000000125,0.0160355496838868,0.00575178060290777));
#14756=CARTESIAN_POINT('',(-0.02600000025,0.0160355496838868,0.00575178060290777));
#14757=CARTESIAN_POINT('',(-0.019,0.,0.));
#14758=CARTESIAN_POINT('',(-0.029,0.,0.));
#14759=CARTESIAN_POINT('',(-0.028999999875,0.0129989629621973,0.0110113030877919));
#14760=CARTESIAN_POINT('',(-0.02600000025,0.0129989629630871,0.0110113030867529));
#14761=CARTESIAN_POINT('',(-0.027000000125,0.0129989629630871,0.0110113030867529));
#14762=CARTESIAN_POINT('',(-0.028,0.0129989629630871,0.0110113030867529));
#14763=CARTESIAN_POINT('',(-0.028999999875,0.0129989629630871,0.0110113030867529));
#14764=CARTESIAN_POINT('',(-0.019,0.014143513369,0.011980841311));
#14765=CARTESIAN_POINT('',(-0.029,0.014143513369,0.011980841311));
#14766=CARTESIAN_POINT('',(-0.0289999998749999,0.0126946246727312,0.0123690700149513));
#14767=CARTESIAN_POINT('',(-0.02899999975,0.012694624629495,0.0123690698783874));
#14768=CARTESIAN_POINT('',(-0.0279999999166667,0.012694624629495,0.0123690698783874));
#14769=CARTESIAN_POINT('',(-0.0270000000833333,0.012694624629495,0.0123690698783874));
#14770=CARTESIAN_POINT('',(-0.02600000025,0.012694624629495,0.0123690698783874));
#14771=CARTESIAN_POINT('',(-0.019,0.003303956249,0.018239062532));
#14772=CARTESIAN_POINT('',(-0.02600000025,0.00436461642098383,0.0171784023604242));
#14773=CARTESIAN_POINT('',(-0.0270000000833333,0.00436461642098383,0.0171784023604242));
#14774=CARTESIAN_POINT('',(-0.0279999999166667,0.00436461642098383,0.0171784023604242));
#14775=CARTESIAN_POINT('',(-0.02899999975,0.00436461642098383,0.0171784023604242));
#14776=CARTESIAN_POINT('',(-0.029,0.00436461651612127,0.0171784024425695));
#14777=CARTESIAN_POINT('',(-0.029,0.003303956249,0.018239062532));
#14778=CARTESIAN_POINT('',(-0.028999999875,0.00303658672248485,0.0167630836919108));
#14779=CARTESIAN_POINT('',(-0.028999999875,0.00303658672242937,0.0167630836919547));
#14780=CARTESIAN_POINT('',(-0.028,0.00303658672242937,0.0167630836919547));
#14781=CARTESIAN_POINT('',(-0.027000000125,0.00303658672242937,0.0167630836919547));
#14782=CARTESIAN_POINT('',(-0.02600000025,0.00303658672242937,0.0167630836919547));
#14783=CARTESIAN_POINT('',(-0.019,0.,0.));
#14784=CARTESIAN_POINT('',(-0.029,0.,0.));
#14785=CARTESIAN_POINT('',(-0.028999999875,-0.00303658672131075,0.0167630836921236));
#14786=CARTESIAN_POINT('',(-0.02600000025,-0.0030365867200693,0.0167630836923146));
#14787=CARTESIAN_POINT('',(-0.027000000125,-0.0030365867200693,0.0167630836923146));
#14788=CARTESIAN_POINT('',(-0.028,-0.0030365867200693,0.0167630836923146));
#14789=CARTESIAN_POINT('',(-0.028999999875,-0.0030365867200693,0.0167630836923146));
#14790=CARTESIAN_POINT('',(-0.019,-0.003303956249,0.018239062532));
#14791=CARTESIAN_POINT('',(-0.029,-0.003303956249,0.018239062532));
#14792=CARTESIAN_POINT('',(-0.0289999998749999,-0.00436461651615862,0.0171784024426068));
#14793=CARTESIAN_POINT('',(-0.02899999975,-0.00436461642079335,0.0171784023602337));
#14794=CARTESIAN_POINT('',(-0.0279999999166667,-0.00436461642079335,0.0171784023602337));
#14795=CARTESIAN_POINT('',(-0.0270000000833333,-0.00436461642079335,0.0171784023602337));
#14796=CARTESIAN_POINT('',(-0.02600000025,-0.00436461642079335,0.0171784023602337));
#14797=CARTESIAN_POINT('',(-0.019,-0.014143513369,0.011980841311));
#14798=CARTESIAN_POINT('',(-0.02600000025,-0.0126946246295647,0.0123690698786476));
#14799=CARTESIAN_POINT('',(-0.0270000000833333,-0.0126946246295647,0.0123690698786476));
#14800=CARTESIAN_POINT('',(-0.0279999999166667,-0.0126946246295647,0.0123690698786476));
#14801=CARTESIAN_POINT('',(-0.02899999975,-0.0126946246295647,0.0123690698786476));
#14802=CARTESIAN_POINT('',(-0.029,-0.0126946246727175,0.0123690700149003));
#14803=CARTESIAN_POINT('',(-0.029,-0.014143513369,0.011980841311));
#14804=CARTESIAN_POINT('',(-0.028999999875,-0.0129989629614279,0.0110113030886876));
#14805=CARTESIAN_POINT('',(-0.028999999875,-0.0129989629615484,0.0110113030885444));
#14806=CARTESIAN_POINT('',(-0.028,-0.0129989629615484,0.0110113030885444));
#14807=CARTESIAN_POINT('',(-0.027000000125,-0.0129989629615484,0.0110113030885444));
#14808=CARTESIAN_POINT('',(-0.02600000025,-0.0129989629615484,0.0110113030885444));
#14809=CARTESIAN_POINT('',(-0.019,0.,0.));
#14810=CARTESIAN_POINT('',(-0.029,0.,0.));
#14811=CARTESIAN_POINT('',(-0.028999999875,-0.0160355496830183,0.00575178060600955));
#14812=CARTESIAN_POINT('',(-0.02600000025,-0.016035549682213,0.00575178060893538));
#14813=CARTESIAN_POINT('',(-0.027000000125,-0.016035549682213,0.00575178060893538));
#14814=CARTESIAN_POINT('',(-0.028,-0.016035549682213,0.00575178060893538));
#14815=CARTESIAN_POINT('',(-0.028999999875,-0.016035549682213,0.00575178060893538));
#14816=CARTESIAN_POINT('',(-0.019,-0.017447469618,0.006258221221));
#14817=CARTESIAN_POINT('',(-0.029,-0.017447469618,0.006258221221));
#14818=CARTESIAN_POINT('',(-0.0289999998749999,-0.0170592411890706,0.00480933246087085));
#14819=CARTESIAN_POINT('',(-0.02899999975,-0.0170592410506495,0.00480933248148512));
#14820=CARTESIAN_POINT('',(-0.0279999999166667,-0.0170592410506495,0.00480933248148512));
#14821=CARTESIAN_POINT('',(-0.0270000000833333,-0.0170592410506495,0.00480933248148512));
#14822=CARTESIAN_POINT('',(-0.02600000025,-0.0170592410506495,0.00480933248148512));
#14823=CARTESIAN_POINT('',(-0.019,-0.017447469618,-0.006258221221));
#14824=CARTESIAN_POINT('',(-0.02600000025,-0.0170592410500552,-0.00480933248164437));
#14825=CARTESIAN_POINT('',(-0.0270000000833333,-0.0170592410500552,-0.00480933248164437));
#14826=CARTESIAN_POINT('',(-0.0279999999166667,-0.0170592410500552,-0.00480933248164437));
#14827=CARTESIAN_POINT('',(-0.02899999975,-0.0170592410500552,-0.00480933248164437));
#14828=CARTESIAN_POINT('',(-0.029,-0.0170592411885923,-0.00480933246099901));
#14829=CARTESIAN_POINT('',(-0.029,-0.017447469618,-0.006258221221));
#14830=CARTESIAN_POINT('',(-0.028999999875,-0.0160355496839222,-0.0057517806034897));
#14831=CARTESIAN_POINT('',(-0.028999999875,-0.0160355496835881,-0.00575178060374051));
#14832=CARTESIAN_POINT('',(-0.028,-0.0160355496835881,-0.00575178060374051));
#14833=CARTESIAN_POINT('',(-0.027000000125,-0.0160355496835881,-0.00575178060374051));
#14834=CARTESIAN_POINT('',(-0.02600000025,-0.0160355496835881,-0.00575178060374051));
#14835=CARTESIAN_POINT('',(-0.019,0.,0.));
#14836=CARTESIAN_POINT('',(-0.02600000025,-0.0129989629565927,-0.0110113030944196));
#14837=CARTESIAN_POINT('',(-0.027000000125,-0.0129989629565927,-0.0110113030944196));
#14838=CARTESIAN_POINT('',(-0.028,-0.0129989629565927,-0.0110113030944196));
#14839=CARTESIAN_POINT('',(-0.028999999875,-0.0129989629565927,-0.0110113030944196));
#14840=CARTESIAN_POINT('',(-0.028999999875,-0.0129989629589501,-0.0110113030916253));
#14841=CARTESIAN_POINT('',(-0.029,0.,0.));
#14842=CARTESIAN_POINT('',(-0.019,-0.014143513369,-0.011980841311));
#14843=CARTESIAN_POINT('',(-0.029,-0.014143513369,-0.011980841311));
#14844=CARTESIAN_POINT('',(-0.0289999998749999,-0.0126946246728457,-0.0123690700153786));
#14845=CARTESIAN_POINT('',(-0.02899999975,-0.012694624629724,-0.012369069879242));
#14846=CARTESIAN_POINT('',(-0.0279999999166667,-0.012694624629724,-0.012369069879242));
#14847=CARTESIAN_POINT('',(-0.0270000000833333,-0.012694624629724,-0.012369069879242));
#14848=CARTESIAN_POINT('',(-0.02600000025,-0.012694624629724,-0.012369069879242));
#14849=CARTESIAN_POINT('',(-0.019,-0.003303956249,-0.018239062532));
#14850=CARTESIAN_POINT('',(-0.029,-0.003303956249,-0.018239062532));
#14851=CARTESIAN_POINT('',(-0.0289999998749999,-0.00436461653816879,-0.017178402464617));
#14852=CARTESIAN_POINT('',(-0.02600000025,-0.00436461642054874,-0.0171784023599891));
#14853=CARTESIAN_POINT('',(-0.0270000000833333,-0.00436461642054874,-0.0171784023599891));
#14854=CARTESIAN_POINT('',(-0.0279999999166667,-0.00436461642054874,-0.0171784023599891));
#14855=CARTESIAN_POINT('',(-0.02899999975,-0.00436461642054874,-0.0171784023599891));
#14856=CARTESIAN_POINT('',(-0.0457000000004547,-1.9104357969811E-13,2.14962800695782E-20));
#14857=CARTESIAN_POINT('',(-0.0457000000001921,1.91044680793333E-13,3.0529103015044E-19));
#14858=CARTESIAN_POINT('',(-0.0456999998751711,-1.43991496994606E-12,0.0160358983847874));
#14859=CARTESIAN_POINT('',(-0.0456999998750961,-1.19492304347938E-11,-0.0160358983847874));
#14860=CARTESIAN_POINT('',(-0.0457000000001922,-1.19492250689532E-11,-0.0160358983845747));
#14861=CARTESIAN_POINT('',(-0.0457000000001856,-0.00209909420135277,-0.0160358983830355));
#14862=CARTESIAN_POINT('',(-0.0457000000001723,-0.00629630402788561,-0.0152009391640093));
#14863=CARTESIAN_POINT('',(-0.0457000000001555,-0.0116343304668846,-0.0116342951457853));
#14864=CARTESIAN_POINT('',(-0.0457000000001443,-0.0152009290827189,-0.00629643515766662));
#14865=CARTESIAN_POINT('',(-0.0457000000001404,-0.0164533830368208,5.39146857913628E-12));
#14866=CARTESIAN_POINT('',(-0.0457000000001443,-0.0152009290785924,0.00629643516762871));
#14867=CARTESIAN_POINT('',(-0.0457000000001555,-0.0116343304592599,0.01163429515341));
#14868=CARTESIAN_POINT('',(-0.0457000000001724,-0.00629630401792351,0.0152009391681357));
#14869=CARTESIAN_POINT('',(-0.0457000000001856,-0.00209909419084346,0.0160358983844112));
#14870=CARTESIAN_POINT('',(-0.0457000000001922,-1.4399100356034E-12,0.0160358983845747));
#14871=CARTESIAN_POINT('',(-0.029,-2.55351295663786E-17,2.63677968348474E-18));
#14872=CARTESIAN_POINT('',(-0.0289999999998646,-1.37316647958235E-13,2.1453454169561E-18));
#14873=CARTESIAN_POINT('',(-0.0289999999999067,0.0329999999999944,2.1453454169561E-18));
#14874=CARTESIAN_POINT('',(-0.0289999999996631,3.49860794609214E-13,-3.47956526835693E-19));
#14875=CARTESIAN_POINT('',(-0.0289999999996075,0.0163358983851577,-3.47956526835693E-19));
#14876=CARTESIAN_POINT('',(-0.029,0.021923936519,-0.00505875553));
#14877=CARTESIAN_POINT('',(-0.029,0.021535705976621,-0.00360986733288895));
#14878=CARTESIAN_POINT('',(-0.028999999875,0.0233855322869173,-0.00539600589872648));
#14879=CARTESIAN_POINT('',(-0.029,0.0170592413274916,-0.00480933244025659));
#14880=CARTESIAN_POINT('',(-0.029,0.0185513962116061,-0.00440951074179888));
#14881=CARTESIAN_POINT('',(-0.029,0.0200435510957205,-0.00400968904334117));
#14882=CARTESIAN_POINT('',(-0.029,0.0215357059798349,-0.00360986734488346));
#14883=CARTESIAN_POINT('',(-0.029,0.0138940902739026,-0.0168455365301639));
#14884=CARTESIAN_POINT('',(-0.029,0.0134942684212575,-0.0153533810706144));
#14885=CARTESIAN_POINT('',(-0.029,0.0130944465686124,-0.0138612256110648));
#14886=CARTESIAN_POINT('',(-0.029,0.0126946247159673,-0.0123690701515153));
#14887=CARTESIAN_POINT('',(-0.02899999975,0.013894090320454,-0.0168455367782344));
#14888=CARTESIAN_POINT('',(-0.029,0.01534297906,-0.016457308211));
#14889=CARTESIAN_POINT('',(-0.028999999875,0.0163658443296136,-0.0175544620931219));
#14890=CARTESIAN_POINT('',(-0.029,0.,0.));
#14891=CARTESIAN_POINT('',(-0.029,0.0215357077061403,0.00360986688232131));
#14892=CARTESIAN_POINT('',(-0.029,0.0200435522465908,0.0040096887349664));
#14893=CARTESIAN_POINT('',(-0.029,0.0185513967870412,0.00440951058761149));
#14894=CARTESIAN_POINT('',(-0.029,0.0170592413274916,0.00480933244025658));
#14895=CARTESIAN_POINT('',(-0.02899999975,0.0215357079520908,0.00360986679036687));
#14896=CARTESIAN_POINT('',(-0.029,0.021923936519,0.00505875553));
#14897=CARTESIAN_POINT('',(-0.028999999875,0.0233855322877841,0.00539600589482715));
#14898=CARTESIAN_POINT('',(-0.029,0.,0.));
#14899=CARTESIAN_POINT('',(-0.028999999875,0.0163658443308259,0.0175544620916103));
#14900=CARTESIAN_POINT('',(-0.029,0.01534297906,0.016457308211));
#14901=CARTESIAN_POINT('',(-0.029,0.0138940903045709,0.0168455366811526));
#14902=CARTESIAN_POINT('',(-0.029,0.0126946247159673,0.0123690701515152));
#14903=CARTESIAN_POINT('',(-0.029,0.0130944465733588,0.0138612256287786));
#14904=CARTESIAN_POINT('',(-0.029,0.0134942684307503,0.0153533811060419));
#14905=CARTESIAN_POINT('',(-0.029,0.0138940902881418,0.0168455365833053));
#14906=CARTESIAN_POINT('',(-0.029,0.00764161743223745,0.0204554034124855));
#14907=CARTESIAN_POINT('',(-0.029,0.00654928382533293,0.0193630697833169));
#14908=CARTESIAN_POINT('',(-0.029,0.0054569502184284,0.0182707361541484));
#14909=CARTESIAN_POINT('',(-0.029,0.00436461661152387,0.0171784025249799));
#14910=CARTESIAN_POINT('',(-0.02899999975,0.00764161763111642,0.0204554035695568));
#14911=CARTESIAN_POINT('',(-0.029,0.006580957459,0.021516063741));
#14912=CARTESIAN_POINT('',(-0.028999999875,0.0070196879508506,0.0229504679924546));
#14913=CARTESIAN_POINT('',(-0.029,0.,0.));
#14914=CARTESIAN_POINT('',(-0.028999999875,-0.00701968795605696,0.022950467990489));
#14915=CARTESIAN_POINT('',(-0.029,-0.006580957459,0.021516063741));
#14916=CARTESIAN_POINT('',(-0.029,-0.00764161753161873,0.0204554034912427));
#14917=CARTESIAN_POINT('',(-0.029,-0.00436461661152388,0.0171784025249799));
#14918=CARTESIAN_POINT('',(-0.029,-0.00545695021842841,0.0182707361541484));
#14919=CARTESIAN_POINT('',(-0.029,-0.00654928382533293,0.0193630697833169));
#14920=CARTESIAN_POINT('',(-0.029,-0.00764161743223745,0.0204554034124855));
#14921=CARTESIAN_POINT('',(-0.029,-0.0138940902881418,0.0168455365833053));
#14922=CARTESIAN_POINT('',(-0.029,-0.0134942684307503,0.0153533811060419));
#14923=CARTESIAN_POINT('',(-0.029,-0.0130944465733588,0.0138612256287786));
#14924=CARTESIAN_POINT('',(-0.029,-0.0126946247159673,0.0123690701515152));
#14925=CARTESIAN_POINT('',(-0.02899999975,-0.0138940903206133,0.0168455367788287));
#14926=CARTESIAN_POINT('',(-0.029,-0.01534297906,0.016457308211));
#14927=CARTESIAN_POINT('',(-0.028999999875,-0.0163658443347904,0.0175544620882956));
#14928=CARTESIAN_POINT('',(-0.029,0.,0.));
#14929=CARTESIAN_POINT('',(-0.028999999875,-0.0233855322868481,0.00539600589902625));
#14930=CARTESIAN_POINT('',(-0.029,-0.021923936519,0.00505875553));
#14931=CARTESIAN_POINT('',(-0.029,-0.0215357078285702,0.00360986683666066));
#14932=CARTESIAN_POINT('',(-0.029,-0.0170592413274916,0.00480933244025658));
#14933=CARTESIAN_POINT('',(-0.029,-0.0185513967870412,0.00440951058761149));
#14934=CARTESIAN_POINT('',(-0.029,-0.0200435522465908,0.0040096887349664));
#14935=CARTESIAN_POINT('',(-0.029,-0.0215357077061403,0.00360986688232131));
#14936=CARTESIAN_POINT('',(-0.029,-0.0215357077103104,-0.00360986688120393));
#14937=CARTESIAN_POINT('',(-0.029,-0.0200435522493708,-0.00400968873422149));
#14938=CARTESIAN_POINT('',(-0.029,-0.0185513967884312,-0.00440951058723904));
#14939=CARTESIAN_POINT('',(-0.029,-0.0170592413274916,-0.0048093324402566));
#14940=CARTESIAN_POINT('',(-0.02899999975,-0.0215357079512363,-0.00360986679059585));
#14941=CARTESIAN_POINT('',(-0.029,-0.021923936519,-0.00505875553));
#14942=CARTESIAN_POINT('',(-0.028999999875,-0.0233855322861928,-0.00539600590172346));
#14943=CARTESIAN_POINT('',(-0.029,0.,0.));
#14944=CARTESIAN_POINT('',(-0.028999999875,-0.0163658443305024,-0.017554462091912));
#14945=CARTESIAN_POINT('',(-0.029,-0.01534297906,-0.016457308211));
#14946=CARTESIAN_POINT('',(-0.029,-0.0138940902974513,-0.0168455366545819));
#14947=CARTESIAN_POINT('',(-0.029,-0.0126946247159673,-0.0123690701515153));
#14948=CARTESIAN_POINT('',(-0.029,-0.0130944465686124,-0.0138612256110648));
#14949=CARTESIAN_POINT('',(-0.029,-0.0134942684212575,-0.0153533810706144));
#14950=CARTESIAN_POINT('',(-0.029,-0.0138940902739026,-0.0168455365301639));
#14951=CARTESIAN_POINT('',(-0.029,0.006580957459,-0.021516063741));
#14952=CARTESIAN_POINT('',(-0.029,0.00764161753161873,-0.0204554034912427));
#14953=CARTESIAN_POINT('',(-0.028999999875,0.00701968795635117,-0.022950467990399));
#14954=CARTESIAN_POINT('',(-0.029,0.00436461665605399,-0.01717840256951));
#14955=CARTESIAN_POINT('',(-0.029,0.00545695024811515,-0.0182707361838351));
#14956=CARTESIAN_POINT('',(-0.029,0.0065492838401763,-0.0193630697981603));
#14957=CARTESIAN_POINT('',(-0.029,0.00764161743223745,-0.0204554034124854));
#14958=CARTESIAN_POINT('',(-0.029,-0.00764161743223745,-0.0204554034124854));
#14959=CARTESIAN_POINT('',(-0.029,-0.0065492838401763,-0.0193630697981603));
#14960=CARTESIAN_POINT('',(-0.029,-0.00545695024811515,-0.0182707361838351));
#14961=CARTESIAN_POINT('',(-0.029,-0.004364616656054,-0.01717840256951));
#14962=CARTESIAN_POINT('',(-0.02899999975,-0.00764161763068133,-0.0204554035691217));
#14963=CARTESIAN_POINT('',(-0.029,-0.006580957459,-0.021516063741));
#14964=CARTESIAN_POINT('',(-0.028999999875,-0.00701968795555781,-0.0229504679910148));
#14965=CARTESIAN_POINT('',(-0.029,0.,0.));
#14966=CARTESIAN_POINT('',(-0.029,0.027720932313,-0.010089594228));
#14967=CARTESIAN_POINT('',(-0.029,0.027720932313,-0.011389594228));
#14968=CARTESIAN_POINT('',(-0.029,0.022598311072,-0.018962234486));
#14969=CARTESIAN_POINT('',(-0.029,0.022598311072,-0.020262234486));
#14970=CARTESIAN_POINT('',(-0.029,0.01475,-0.025547749412));
#14971=CARTESIAN_POINT('',(-0.029,0.01475,-0.026847749412));
#14972=CARTESIAN_POINT('',(-0.029,0.005122621241,-0.029051828714));
#14973=CARTESIAN_POINT('',(-0.029,0.005122621241,-0.030351828714));
#14974=CARTESIAN_POINT('',(-0.029,-0.005122621241,-0.029051828714));
#14975=CARTESIAN_POINT('',(-0.029,-0.005122621241,-0.030351828714));
#14976=CARTESIAN_POINT('',(-0.029,-0.01475,-0.025547749412));
#14977=CARTESIAN_POINT('',(-0.029,-0.01475,-0.026847749412));
#14978=CARTESIAN_POINT('',(-0.029,-0.022598311072,-0.018962234486));
#14979=CARTESIAN_POINT('',(-0.029,-0.022598311072,-0.020262234486));
#14980=CARTESIAN_POINT('',(-0.029,-0.027720932313,-0.010089594228));
#14981=CARTESIAN_POINT('',(-0.029,-0.027720932313,-0.011389594228));
#14982=CARTESIAN_POINT('',(-0.029,-0.0295,0.));
#14983=CARTESIAN_POINT('',(-0.029,-0.0295,-0.0013));
#14984=CARTESIAN_POINT('',(-0.029,-0.027720932313,0.010089594228));
#14985=CARTESIAN_POINT('',(-0.029,-0.027720932313,0.008789594228));
#14986=CARTESIAN_POINT('',(-0.029,-0.022598311072,0.018962234486));
#14987=CARTESIAN_POINT('',(-0.029,-0.022598311072,0.017662234486));
#14988=CARTESIAN_POINT('',(-0.029,-0.01475,0.025547749412));
#14989=CARTESIAN_POINT('',(-0.029,-0.01475,0.024247749412));
#14990=CARTESIAN_POINT('',(-0.029,-0.005122621241,0.029051828714));
#14991=CARTESIAN_POINT('',(-0.029,-0.005122621241,0.027751828714));
#14992=CARTESIAN_POINT('',(-0.029,0.005122621241,0.029051828714));
#14993=CARTESIAN_POINT('',(-0.029,0.005122621241,0.027751828714));
#14994=CARTESIAN_POINT('',(-0.029,0.01475,0.025547749412));
#14995=CARTESIAN_POINT('',(-0.029,0.01475,0.024247749412));
#14996=CARTESIAN_POINT('',(-0.029,0.022598311072,0.018962234486));
#14997=CARTESIAN_POINT('',(-0.029,0.022598311072,0.017662234486));
#14998=CARTESIAN_POINT('',(-0.029,0.027720932313,0.010089594228));
#14999=CARTESIAN_POINT('',(-0.029,0.027720932313,0.008789594228));
#15000=CARTESIAN_POINT('',(-0.029,0.0295,0.));
#15001=CARTESIAN_POINT('',(-0.029,0.0295,-0.0013));
#15002=CARTESIAN_POINT('',(-0.0275,0.006003117026,-0.018816902965));
#15003=CARTESIAN_POINT('',(-0.026000000125,0.007641617631,-0.02045540357));
#15004=CARTESIAN_POINT('',(-0.0270000000833333,0.007641617631,-0.02045540357));
#15005=CARTESIAN_POINT('',(-0.0280000000416667,0.007641617631,-0.02045540357));
#15006=CARTESIAN_POINT('',(-0.029,0.007641617631,-0.02045540357));
#15007=CARTESIAN_POINT('',(-0.046,0.0295,0.));
#15008=CARTESIAN_POINT('',(-0.046,0.027720932313,0.010089594228));
#15009=CARTESIAN_POINT('',(-0.046,0.022598311072,0.018962234486));
#15010=CARTESIAN_POINT('',(-0.046,0.01475,0.025547749412));
#15011=CARTESIAN_POINT('',(-0.046,0.005122621241,0.029051828714));
#15012=CARTESIAN_POINT('',(-0.046,-0.005122621241,0.029051828714));
#15013=CARTESIAN_POINT('',(-0.046,-0.01475,0.025547749412));
#15014=CARTESIAN_POINT('',(-0.046,-0.022598311072,0.018962234486));
#15015=CARTESIAN_POINT('',(-0.046,-0.027720932313,0.010089594228));
#15016=CARTESIAN_POINT('',(-0.046,-0.0295,0.));
#15017=CARTESIAN_POINT('',(-0.046,-0.027720932313,-0.010089594228));
#15018=CARTESIAN_POINT('',(-0.046,-0.022598311072,-0.018962234486));
#15019=CARTESIAN_POINT('',(-0.046,-0.01475,-0.025547749412));
#15020=CARTESIAN_POINT('',(-0.046,-0.005122621241,-0.029051828714));
#15021=CARTESIAN_POINT('',(-0.046,0.005122621241,-0.029051828714));
#15022=CARTESIAN_POINT('',(-0.046,0.01475,-0.025547749412));
#15023=CARTESIAN_POINT('',(-0.046,0.022598311072,-0.018962234486));
#15024=CARTESIAN_POINT('',(-0.046,0.027720932313,-0.010089594228));
#15025=CARTESIAN_POINT('',(-0.0275,0.0132943574755,0.0146073033285));
#15026=CARTESIAN_POINT('',(-0.026000000125,0.013894090321,0.016845536779));
#15027=CARTESIAN_POINT('',(-0.0270000000833333,0.013894090321,0.016845536779));
#15028=CARTESIAN_POINT('',(-0.0280000000416667,0.013894090321,0.016845536779));
#15029=CARTESIAN_POINT('',(-0.029,0.013894090321,0.016845536779));
#15030=CARTESIAN_POINT('',(-0.019,0.01534297906,0.016457308211));
#15031=CARTESIAN_POINT('',(-0.02899999975,0.0163658443309724,0.0175544620914737));
#15032=CARTESIAN_POINT('',(-0.0279999999166667,0.0163658443309724,0.0175544620914737));
#15033=CARTESIAN_POINT('',(-0.0270000000833333,0.0163658443309724,0.0175544620914737));
#15034=CARTESIAN_POINT('',(-0.02600000025,0.0163658443309724,0.0175544620914737));
#15035=CARTESIAN_POINT('',(-0.019,0.,0.));
#15036=CARTESIAN_POINT('',(-0.02899999975,0.0233855322886682,0.00539600589099533));
#15037=CARTESIAN_POINT('',(-0.0279999999166667,0.0233855322886682,0.00539600589099533));
#15038=CARTESIAN_POINT('',(-0.0270000000833333,0.0233855322886682,0.00539600589099533));
#15039=CARTESIAN_POINT('',(-0.02600000025,0.0233855322886682,0.00539600589099533));
#15040=CARTESIAN_POINT('',(-0.019,0.021923936519,0.00505875553));
#15041=CARTESIAN_POINT('',(-0.02899999975,0.0215357079519098,0.0036098667904154));
#15042=CARTESIAN_POINT('',(-0.0279999999166667,0.0215357079519098,0.0036098667904154));
#15043=CARTESIAN_POINT('',(-0.0270000000833333,0.0215357079519098,0.0036098667904154));
#15044=CARTESIAN_POINT('',(-0.02600000025,0.0215357079519098,0.0036098667904154));
#15045=CARTESIAN_POINT('',(-0.0275,0.019297474501,0.00420959963649999));
#15046=CARTESIAN_POINT('',(-0.0275,0.019297474501,-0.00420959963649999));
#15047=CARTESIAN_POINT('',(-0.026000000125,0.021535707951,-0.00360986679099999));
#15048=CARTESIAN_POINT('',(-0.0270000000833333,0.021535707951,-0.00360986679099999));
#15049=CARTESIAN_POINT('',(-0.0280000000416667,0.021535707951,-0.00360986679099999));
#15050=CARTESIAN_POINT('',(-0.029,0.021535707951,-0.00360986679099999));
#15051=CARTESIAN_POINT('',(-0.019,0.021923936519,-0.00505875553));
#15052=CARTESIAN_POINT('',(-0.02899999975,0.0233855322869034,-0.00539600589878677));
#15053=CARTESIAN_POINT('',(-0.0279999999166667,0.0233855322869034,-0.00539600589878677));
#15054=CARTESIAN_POINT('',(-0.0270000000833333,0.0233855322869034,-0.00539600589878677));
#15055=CARTESIAN_POINT('',(-0.02600000025,0.0233855322869034,-0.00539600589878677));
#15056=CARTESIAN_POINT('',(-0.019,0.,0.));
#15057=CARTESIAN_POINT('',(-0.02899999975,0.0163658443283577,-0.0175544620942928));
#15058=CARTESIAN_POINT('',(-0.0279999999166667,0.0163658443283577,-0.0175544620942928));
#15059=CARTESIAN_POINT('',(-0.0270000000833333,0.0163658443283577,-0.0175544620942928));
#15060=CARTESIAN_POINT('',(-0.02600000025,0.0163658443283577,-0.0175544620942928));
#15061=CARTESIAN_POINT('',(-0.019,0.01534297906,-0.016457308211));
#15062=CARTESIAN_POINT('',(-0.02899999975,0.0138940903204055,-0.0168455367780533));
#15063=CARTESIAN_POINT('',(-0.0279999999166667,0.0138940903204055,-0.0168455367780533));
#15064=CARTESIAN_POINT('',(-0.0270000000833333,0.0138940903204055,-0.0168455367780533));
#15065=CARTESIAN_POINT('',(-0.02600000025,0.0138940903204055,-0.0168455367780533));
#15066=CARTESIAN_POINT('',(-0.0275,0.0132943574755,-0.0146073033285));
#15067=CARTESIAN_POINT('',(-0.019,0.006580957459,-0.021516063741));
#15068=CARTESIAN_POINT('',(-0.02899999975,0.0070196879564287,-0.0229504679903753));
#15069=CARTESIAN_POINT('',(-0.0279999999166667,0.0070196879564287,-0.0229504679903753));
#15070=CARTESIAN_POINT('',(-0.0270000000833333,0.0070196879564287,-0.0229504679903753));
#15071=CARTESIAN_POINT('',(-0.02600000025,0.0070196879564287,-0.0229504679903753));
#15072=CARTESIAN_POINT('',(-0.019,0.,0.));
#15073=CARTESIAN_POINT('',(-0.02899999975,-0.00701968795473764,-0.0229504679912657));
#15074=CARTESIAN_POINT('',(-0.0279999999166667,-0.00701968795473764,-0.0229504679912657));
#15075=CARTESIAN_POINT('',(-0.0270000000833333,-0.00701968795473764,-0.0229504679912657));
#15076=CARTESIAN_POINT('',(-0.02600000025,-0.00701968795473764,-0.0229504679912657));
#15077=CARTESIAN_POINT('',(-0.019,-0.006580957459,-0.021516063741));
#15078=CARTESIAN_POINT('',(-0.02899999975,-0.00764161763054874,-0.0204554035689891));
#15079=CARTESIAN_POINT('',(-0.0279999999166667,-0.00764161763054874,-0.0204554035689891));
#15080=CARTESIAN_POINT('',(-0.0270000000833333,-0.00764161763054874,-0.0204554035689891));
#15081=CARTESIAN_POINT('',(-0.02600000025,-0.00764161763054874,-0.0204554035689891));
#15082=CARTESIAN_POINT('',(-0.0275,-0.006003117026,-0.018816902965));
#15083=CARTESIAN_POINT('',(-0.0275,-0.0132943574755,-0.0146073033285));
#15084=CARTESIAN_POINT('',(-0.026000000125,-0.013894090321,-0.016845536779));
#15085=CARTESIAN_POINT('',(-0.0270000000833333,-0.013894090321,-0.016845536779));
#15086=CARTESIAN_POINT('',(-0.0280000000416667,-0.013894090321,-0.016845536779));
#15087=CARTESIAN_POINT('',(-0.029,-0.013894090321,-0.016845536779));
#15088=CARTESIAN_POINT('',(-0.019,-0.01534297906,-0.016457308211));
#15089=CARTESIAN_POINT('',(-0.02899999975,-0.0163658443303253,-0.017554462092077));
#15090=CARTESIAN_POINT('',(-0.0279999999166667,-0.0163658443303253,-0.017554462092077));
#15091=CARTESIAN_POINT('',(-0.0270000000833333,-0.0163658443303253,-0.017554462092077));
#15092=CARTESIAN_POINT('',(-0.02600000025,-0.0163658443303253,-0.017554462092077));
#15093=CARTESIAN_POINT('',(-0.019,0.,0.));
#15094=CARTESIAN_POINT('',(-0.02899999975,-0.0233855322854857,-0.00539600590478796));
#15095=CARTESIAN_POINT('',(-0.0279999999166667,-0.0233855322854857,-0.00539600590478796));
#15096=CARTESIAN_POINT('',(-0.0270000000833333,-0.0233855322854857,-0.00539600590478796));
#15097=CARTESIAN_POINT('',(-0.02600000025,-0.0233855322854857,-0.00539600590478796));
#15098=CARTESIAN_POINT('',(-0.019,-0.021923936519,-0.00505875553));
#15099=CARTESIAN_POINT('',(-0.02899999975,-0.0215357079510552,-0.00360986679064437));
#15100=CARTESIAN_POINT('',(-0.0279999999166667,-0.0215357079510552,-0.00360986679064437));
#15101=CARTESIAN_POINT('',(-0.0270000000833333,-0.0215357079510552,-0.00360986679064437));
#15102=CARTESIAN_POINT('',(-0.02600000025,-0.0215357079510552,-0.00360986679064437));
#15103=CARTESIAN_POINT('',(-0.0275,-0.019297474501,-0.00420959963649999));
#15104=CARTESIAN_POINT('',(-0.0275,-0.019297474501,0.00420959963649999));
#15105=CARTESIAN_POINT('',(-0.026000000125,-0.021535707951,0.00360986679099999));
#15106=CARTESIAN_POINT('',(-0.0270000000833333,-0.021535707951,0.00360986679099999));
#15107=CARTESIAN_POINT('',(-0.0280000000416667,-0.021535707951,0.00360986679099999));
#15108=CARTESIAN_POINT('',(-0.029,-0.021535707951,0.00360986679099999));
#15109=CARTESIAN_POINT('',(-0.019,-0.021923936519,0.00505875553));
#15110=CARTESIAN_POINT('',(-0.02899999975,-0.0233855322867651,0.00539600589938632));
#15111=CARTESIAN_POINT('',(-0.0279999999166667,-0.0233855322867651,0.00539600589938632));
#15112=CARTESIAN_POINT('',(-0.0270000000833333,-0.0233855322867651,0.00539600589938632));
#15113=CARTESIAN_POINT('',(-0.02600000025,-0.0233855322867651,0.00539600589938632));
#15114=CARTESIAN_POINT('',(-0.019,0.,0.));
#15115=CARTESIAN_POINT('',(-0.02899999975,-0.0163658443387112,0.0175544620846403));
#15116=CARTESIAN_POINT('',(-0.0279999999166667,-0.0163658443387112,0.0175544620846403));
#15117=CARTESIAN_POINT('',(-0.0270000000833333,-0.0163658443387112,0.0175544620846403));
#15118=CARTESIAN_POINT('',(-0.02600000025,-0.0163658443387112,0.0175544620846403));
#15119=CARTESIAN_POINT('',(-0.019,-0.01534297906,0.016457308211));
#15120=CARTESIAN_POINT('',(-0.02899999975,-0.0138940903205647,0.0168455367786476));
#15121=CARTESIAN_POINT('',(-0.0279999999166667,-0.0138940903205647,0.0168455367786476));
#15122=CARTESIAN_POINT('',(-0.0270000000833333,-0.0138940903205647,0.0168455367786476));
#15123=CARTESIAN_POINT('',(-0.02600000025,-0.0138940903205647,0.0168455367786476));
#15124=CARTESIAN_POINT('',(-0.0275,-0.0132943574755,0.0146073033285));
#15125=CARTESIAN_POINT('',(-0.0275,-0.006003117026,0.018816902965));
#15126=CARTESIAN_POINT('',(-0.026000000125,-0.007641617631,0.02045540357));
#15127=CARTESIAN_POINT('',(-0.0270000000833333,-0.007641617631,0.02045540357));
#15128=CARTESIAN_POINT('',(-0.0280000000416667,-0.007641617631,0.02045540357));
#15129=CARTESIAN_POINT('',(-0.029,-0.007641617631,0.02045540357));
#15130=CARTESIAN_POINT('',(-0.019,-0.006580957459,0.021516063741));
#15131=CARTESIAN_POINT('',(-0.02899999975,-0.0070196879558403,0.0229504679905553));
#15132=CARTESIAN_POINT('',(-0.0279999999166667,-0.0070196879558403,0.0229504679905553));
#15133=CARTESIAN_POINT('',(-0.0270000000833333,-0.0070196879558403,0.0229504679905553));
#15134=CARTESIAN_POINT('',(-0.02600000025,-0.0070196879558403,0.0229504679905553));
#15135=CARTESIAN_POINT('',(-0.019,0.,0.));
#15136=CARTESIAN_POINT('',(-0.02899999975,0.00701968794532321,0.0229504679941452));
#15137=CARTESIAN_POINT('',(-0.0279999999166667,0.00701968794532321,0.0229504679941452));
#15138=CARTESIAN_POINT('',(-0.0270000000833333,0.00701968794532321,0.0229504679941452));
#15139=CARTESIAN_POINT('',(-0.02600000025,0.00701968794532321,0.0229504679941452));
#15140=CARTESIAN_POINT('',(-0.019,0.006580957459,0.021516063741));
#15141=CARTESIAN_POINT('',(-0.02899999975,0.00764161763098383,0.0204554035694242));
#15142=CARTESIAN_POINT('',(-0.0279999999166667,0.00764161763098383,0.0204554035694242));
#15143=CARTESIAN_POINT('',(-0.0270000000833333,0.00764161763098383,0.0204554035694242));
#15144=CARTESIAN_POINT('',(-0.02600000025,0.00764161763098383,0.0204554035694242));
#15145=CARTESIAN_POINT('',(-0.0275,0.006003117026,0.018816902965));
#15146=CARTESIAN_POINT('',(-0.0269999999999846,-1.36038104775004E-13,2.6489787551435E-18));
#15147=CARTESIAN_POINT('',(-0.0269999999998682,1.36039743730353E-13,-2.59930748974073E-18));
#15148=CARTESIAN_POINT('',(-0.0270000001246841,-6.97351005096951E-12,-0.0339999999999195));
#15149=CARTESIAN_POINT('',(-0.0270000001249341,-1.94544521920252E-11,0.0339999999999195));
#15150=CARTESIAN_POINT('',(-0.0269999999998682,-1.94544562196518E-11,0.0339999999998389));
#15151=CARTESIAN_POINT('',(-0.0269999999998739,-0.00445058961092908,0.0339999999973102));
#15152=CARTESIAN_POINT('',(-0.0269999999998853,-0.01334969402564,0.0322296836269298));
#15153=CARTESIAN_POINT('',(-0.0269999999998997,-0.0246676067857547,0.0246675319043401));
#15154=CARTESIAN_POINT('',(-0.0269999999999094,-0.0322296622477484,0.0133499720628638));
#15155=CARTESIAN_POINT('',(-0.0269999999999128,-0.0348851688773134,-6.40291627412936E-12));
#15156=CARTESIAN_POINT('',(-0.0269999999999094,-0.0322296622428478,-0.0133499720746949));
#15157=CARTESIAN_POINT('',(-0.0269999999998997,-0.0246676067766996,-0.0246675319133952));
#15158=CARTESIAN_POINT('',(-0.0269999999998853,-0.0133496940138089,-0.0322296836318303));
#15159=CARTESIAN_POINT('',(-0.0269999999998739,-0.00445058959844815,-0.0339999999989439));
#15160=CARTESIAN_POINT('',(-0.0269999999998682,-6.97352071331679E-12,-0.0339999999998389));
#15161=CARTESIAN_POINT('',(-0.087860759494,0.,0.));
#15162=CARTESIAN_POINT('',(-0.0448,0.,0.));
#15163=CARTESIAN_POINT('',(-0.0448000003749039,-1.43991482401222E-12,0.0160358983848022));
#15164=CARTESIAN_POINT('',(-0.044799999999904,-9.30247185607308E-12,-0.0160358983848022));
#15165=CARTESIAN_POINT('',(-0.0448,-6.88880368742238E-12,0.016035898385));
#15166=CARTESIAN_POINT('',(-0.0448,-0.00209909419616183,0.0160358983840983));
#15167=CARTESIAN_POINT('',(-0.0448,-0.00629630402268758,0.0152009391664744));
#15168=CARTESIAN_POINT('',(-0.0448,-0.0116343304626057,0.0116342951503842));
#15169=CARTESIAN_POINT('',(-0.0448,-0.0152009290802918,0.00629643516400925));
#15170=CARTESIAN_POINT('',(-0.0448,-0.0164533830369911,1.89724333662342E-12));
#15171=CARTESIAN_POINT('',(-0.0448,-0.0152009290817439,-0.0062964351605036));
#15172=CARTESIAN_POINT('',(-0.0448,-0.0116343304652888,-0.0116342951477011));
#15173=CARTESIAN_POINT('',(-0.0448,-0.00629630402619322,-0.0152009391650224));
#15174=CARTESIAN_POINT('',(-0.0448,-0.00209909419986004,-0.0160358983836142));
#15175=CARTESIAN_POINT('',(-0.0448,-1.0587010404128E-11,-0.016035898385));
#15176=CARTESIAN_POINT('',(-0.0292999999998881,3.50882717550253E-13,-3.61538547232193E-19));
#15177=CARTESIAN_POINT('',(-0.0293,0.,1.29739916218158E-17));
#15178=CARTESIAN_POINT('',(-0.0293000001249039,-4.18441562143595E-12,0.0160358983848022));
#15179=CARTESIAN_POINT('',(-0.0293000001249039,-5.46894785937705E-12,-0.0160358983848022));
#15180=CARTESIAN_POINT('',(-0.0292999999998079,-5.46895656244816E-12,-0.0160358983846046));
#15181=CARTESIAN_POINT('',(-0.0292999999998007,-0.00209909419504539,-0.0160358983839346));
#15182=CARTESIAN_POINT('',(-0.0292999999997864,-0.00629630402226934,-0.0152009391665087));
#15183=CARTESIAN_POINT('',(-0.0292999999997682,-0.0116343304630323,-0.0116342951499371));
#15184=CARTESIAN_POINT('',(-0.0292999999997561,-0.0152009290809598,-0.00629643516255718));
#15185=CARTESIAN_POINT('',(-0.0292999999997518,-0.0164533830370793,6.59004884789626E-13));
#15186=CARTESIAN_POINT('',(-0.0292999999997561,-0.0152009290804555,0.00629643516377478));
#15187=CARTESIAN_POINT('',(-0.0292999999997682,-0.0116343304621004,0.011634295150869));
#15188=CARTESIAN_POINT('',(-0.0292999999997864,-0.0062963040210517,0.015200939167013));
#15189=CARTESIAN_POINT('',(-0.0292999999998007,-0.00209909419376085,0.0160358983841027));
#15190=CARTESIAN_POINT('',(-0.0292999999998079,-4.18441069673782E-12,0.0160358983846046));
#15191=CARTESIAN_POINT('',(-0.0280000000000153,-1.36039948891632E-13,2.12798109529093E-18));
#15192=CARTESIAN_POINT('',(-0.0280000000001317,1.36035990293993E-13,-2.40331363620194E-18));
#15193=CARTESIAN_POINT('',(-0.0279999998753159,-3.05296983152609E-12,0.0339999999999195));
#15194=CARTESIAN_POINT('',(-0.0279999998750659,-2.53352639798974E-11,-0.0339999999999195));
#15195=CARTESIAN_POINT('',(-0.0280000000001317,-2.53352755643033E-11,-0.033999999999839));
#15196=CARTESIAN_POINT('',(-0.0280000000001261,-0.00445058961672823,-0.0339999999965404));
#15197=CARTESIAN_POINT('',(-0.0280000000001147,-0.0133496940309697,-0.0322296836246866));
#15198=CARTESIAN_POINT('',(-0.0280000000001003,-0.0246676067896425,-0.0246675319004057));
#15199=CARTESIAN_POINT('',(-0.0280000000000906,-0.0322296622497385,-0.0133499720579734));
#15200=CARTESIAN_POINT('',(-0.0280000000000872,-0.0348851688772805,1.14312184329868E-11));
#15201=CARTESIAN_POINT('',(-0.0280000000000906,-0.0322296622409894,0.0133499720790955));
#15202=CARTESIAN_POINT('',(-0.0280000000001003,-0.0246676067734763,0.0246675319165719));
#15203=CARTESIAN_POINT('',(-0.0280000000001147,-0.0133496940098477,0.0322296836334355));
#15204=CARTESIAN_POINT('',(-0.0280000000001261,-0.00445058959444593,0.0339999999994571));
#15205=CARTESIAN_POINT('',(-0.0280000000001317,-3.05298233072731E-12,0.033999999999839));
#15206=CARTESIAN_POINT('',(-0.087860759494,0.,0.));
#15207=CARTESIAN_POINT('',(-0.0447999999998881,-3.50878864290858E-13,1.27902351783967E-19));
#15208=CARTESIAN_POINT('',(-0.0444999999996631,-3.49856951876166E-13,6.65098269064164E-20));
#15209=CARTESIAN_POINT('',(-0.0444999999997187,0.016335898384458,6.65098269064164E-20));
#15210=CARTESIAN_POINT('',(-0.087860759494,0.,2.74627544186333E-49));
#15211=CARTESIAN_POINT('',(-0.033133974596,0.,1.21245840199241E-17));
#15212=CARTESIAN_POINT('',(-0.0331339745961753,-9.30247461674151E-12,-0.01603589838493));
#15213=CARTESIAN_POINT('',(-0.033133974471,-7.45337677166523E-12,0.016035898385));
#15214=CARTESIAN_POINT('',(-0.033133974596,-1.0587010404128E-11,-0.016035898385));
#15215=CARTESIAN_POINT('',(-0.033133974596,-0.00209909419983651,-0.0160358983836142));
#15216=CARTESIAN_POINT('',(-0.033133974596,-0.0062963040261227,-0.0152009391650413));
#15217=CARTESIAN_POINT('',(-0.033133974596,-0.0116343304651797,-0.0116342951477968));
#15218=CARTESIAN_POINT('',(-0.033133974596,-0.015200929081652,-0.00629643516070066));
#15219=CARTESIAN_POINT('',(-0.033133974596,-0.0164533830369816,1.60761173666999E-12));
#15220=CARTESIAN_POINT('',(-0.033133974596,-0.0152009290804216,0.00629643516367116));
#15221=CARTESIAN_POINT('',(-0.033133974596,-0.0116343304629062,0.0116342951500703));
#15222=CARTESIAN_POINT('',(-0.033133974596,-0.00629630402315223,0.0152009391662717));
#15223=CARTESIAN_POINT('',(-0.033133974596,-0.00209909419670289,0.0160358983840244));
#15224=CARTESIAN_POINT('',(-0.033133974596,-7.45338585686584E-12,0.016035898385));
#15225=CARTESIAN_POINT('',(-0.0445,3.78301144317866E-6,1.64798730217797E-19));
#15226=CARTESIAN_POINT('',(-0.0445,0.,0.));
#15227=CARTESIAN_POINT('',(-0.0445,-0.0119306429063121,0.0114497029323385));
#15228=CARTESIAN_POINT('',(-0.044499999875,-0.0158810549881622,0.00460738839930129));
#15229=CARTESIAN_POINT('',(-0.0445,-0.013988882352324,0.0191311570514775));
#15230=CARTESIAN_POINT('',(-0.0445,-0.0133028025302656,0.016570672323168));
#15231=CARTESIAN_POINT('',(-0.0445,-0.0126167227082072,0.0140101875948586));
#15232=CARTESIAN_POINT('',(-0.0445,-0.0119306428861488,0.0114497028665492));
#15233=CARTESIAN_POINT('',(-0.0445000000004407,-0.01398888233812,0.0191311570560501));
#15234=CARTESIAN_POINT('',(-0.0445000000054389,-1.31298894547398E-11,2.57689317088404E-11));
#15235=CARTESIAN_POINT('',(-0.044500000000146,-0.00957362679562088,0.021680305939673));
#15236=CARTESIAN_POINT('',(-0.0445,-0.00395041209800161,0.0160570912714795));
#15237=CARTESIAN_POINT('',(-0.0445,-0.00582481702234961,0.0179314961816983));
#15238=CARTESIAN_POINT('',(-0.0445,-0.0076992219466976,0.019805901091917));
#15239=CARTESIAN_POINT('',(-0.0445,-0.0095736268710456,0.0216803060021358));
#15240=CARTESIAN_POINT('',(-0.044499999875,-0.00395041209657952,0.0160570912579534));
#15241=CARTESIAN_POINT('',(-0.0445,0.,0.));
#15242=CARTESIAN_POINT('',(-0.0444999998749998,0.00395041214632822,0.0160570913147367));
#15243=CARTESIAN_POINT('',(-0.0445,0.00957362687104559,0.0216803060021358));
#15244=CARTESIAN_POINT('',(-0.0445,0.00769922196196155,0.019805901107181));
#15245=CARTESIAN_POINT('',(-0.0445,0.00582481705287752,0.0179314962122262));
#15246=CARTESIAN_POINT('',(-0.0445,0.00395041214379348,0.0160570913172714));
#15247=CARTESIAN_POINT('',(-0.0445000000002923,0.00957362684875627,0.0216803060057704));
#15248=CARTESIAN_POINT('',(-0.0445000000054388,1.31301128770511E-11,2.57694144345576E-11));
#15249=CARTESIAN_POINT('',(-0.0445000000002202,0.0139888823212884,0.0191311569644422));
#15250=CARTESIAN_POINT('',(-0.0445,0.0119306428861488,0.0114497028665492));
#15251=CARTESIAN_POINT('',(-0.0445,0.0126167227082072,0.0140101875948586));
#15252=CARTESIAN_POINT('',(-0.0445,0.0133028025302656,0.016570672323168));
#15253=CARTESIAN_POINT('',(-0.0445,0.013988882352324,0.0191311570514775));
#15254=CARTESIAN_POINT('',(-0.0445,0.0119306428918697,0.0114497028601498));
#15255=CARTESIAN_POINT('',(-0.0445,0.,0.));
#15256=CARTESIAN_POINT('',(-0.0444999999996452,0.0159746110500761,0.00427173727880919));
#15257=CARTESIAN_POINT('',(-0.0445,0.0235948629797496,0.00222989690610838));
#15258=CARTESIAN_POINT('',(-0.0445,0.0210547789802328,0.00291051037320731));
#15259=CARTESIAN_POINT('',(-0.0445,0.018514694980716,0.00359112384030625));
#15260=CARTESIAN_POINT('',(-0.0445,0.0159746109811992,0.00427173730740518));
#15261=CARTESIAN_POINT('',(-0.0445000000001154,0.0235948629947594,0.0022298969152439));
#15262=CARTESIAN_POINT('',(-0.0445000000068876,4.40842231272297E-11,8.49853498151601E-13));
#15263=CARTESIAN_POINT('',(-0.0445000000001778,0.0235625090884613,-0.00254914897306764));
#15264=CARTESIAN_POINT('',(-0.0445,0.0158810549909967,-0.00460738840309584));
#15265=CARTESIAN_POINT('',(-0.0445,0.0184415397191314,-0.00392130858560222));
#15266=CARTESIAN_POINT('',(-0.0445,0.0210020244472661,-0.0032352287681086));
#15267=CARTESIAN_POINT('',(-0.0445,0.0235625091754008,-0.00254914895061497));
#15268=CARTESIAN_POINT('',(-0.044499999875,0.0158810549891071,-0.00460738839604404));
#15269=CARTESIAN_POINT('',(-0.0445,0.,0.));
#15270=CARTESIAN_POINT('',(-0.0444999998749998,0.0119306429043919,-0.0114497029343883));
#15271=CARTESIAN_POINT('',(-0.0445,0.013988882352324,-0.0191311570514775));
#15272=CARTESIAN_POINT('',(-0.0445,0.0133028025363262,-0.0165706723457866));
#15273=CARTESIAN_POINT('',(-0.0445,0.0126167227203284,-0.0140101876400956));
#15274=CARTESIAN_POINT('',(-0.0445,0.0119306429043306,-0.0114497029344047));
#15275=CARTESIAN_POINT('',(-0.0445000000004407,0.01398888233812,-0.0191311570560501));
#15276=CARTESIAN_POINT('',(-0.0445000000054393,1.31303038846426E-11,-2.57695957250192E-11));
#15277=CARTESIAN_POINT('',(-0.044500000000146,0.00957362679562087,-0.021680305939673));
#15278=CARTESIAN_POINT('',(-0.0445,0.00395041209800159,-0.0160570912714795));
#15279=CARTESIAN_POINT('',(-0.0445,0.00582481702234959,-0.0179314961816983));
#15280=CARTESIAN_POINT('',(-0.0445,0.00769922194669759,-0.019805901091917));
#15281=CARTESIAN_POINT('',(-0.0445,0.00957362687104559,-0.0216803060021358));
#15282=CARTESIAN_POINT('',(-0.044499999875,0.00395041209972926,-0.0160570912569995));
#15283=CARTESIAN_POINT('',(-0.0445,0.,0.));
#15284=CARTESIAN_POINT('',(-0.0444999998749998,-0.00395041214962159,-0.0160570913139264));
#15285=CARTESIAN_POINT('',(-0.0445,-0.0095736268710456,-0.0216803060021358));
#15286=CARTESIAN_POINT('',(-0.0445,-0.00769922196237542,-0.0198059011075949));
#15287=CARTESIAN_POINT('',(-0.0445,-0.00582481705370523,-0.0179314962130539));
#15288=CARTESIAN_POINT('',(-0.0445,-0.00395041214503505,-0.016057091318513));
#15289=CARTESIAN_POINT('',(-0.0445000000002922,-0.00957362684875627,-0.0216803060057704));
#15290=CARTESIAN_POINT('',(-0.0445000000054376,-1.31302623148723E-11,-2.57695601066413E-11));
#15291=CARTESIAN_POINT('',(-0.0445000000002202,-0.0139888823212884,-0.0191311569644422));
#15292=CARTESIAN_POINT('',(-0.0445,-0.0119306428861488,-0.0114497028665492));
#15293=CARTESIAN_POINT('',(-0.0445,-0.0126167227082072,-0.0140101875948586));
#15294=CARTESIAN_POINT('',(-0.0445,-0.0133028025302656,-0.016570672323168));
#15295=CARTESIAN_POINT('',(-0.0445,-0.013988882352324,-0.0191311570514775));
#15296=CARTESIAN_POINT('',(-0.044499999875,-0.0119306428942181,-0.0114497028577028));
#15297=CARTESIAN_POINT('',(-0.0445,0.,0.));
#15298=CARTESIAN_POINT('',(-0.0444999998749998,-0.0158810550546861,-0.00460738838227197));
#15299=CARTESIAN_POINT('',(-0.0445,-0.0235625091754008,-0.00254914895061497));
#15300=CARTESIAN_POINT('',(-0.0445,-0.0210020244688091,-0.00323522876233617));
#15301=CARTESIAN_POINT('',(-0.0445,-0.0184415397622174,-0.00392130857405737));
#15302=CARTESIAN_POINT('',(-0.0445,-0.0158810550556257,-0.00460738838577856));
#15303=CARTESIAN_POINT('',(-0.0445000000003707,-0.0235625091821229,-0.00254914894712841));
#15304=CARTESIAN_POINT('',(-0.0445000000057756,-1.48440606719702E-11,1.19635928943991E-17));
#15305=CARTESIAN_POINT('',(-0.0445000000001852,-0.023562509088512,0.00254914897305407));
#15306=CARTESIAN_POINT('',(-0.0445,-0.0158810549893007,0.00460738840355029));
#15307=CARTESIAN_POINT('',(-0.0445,-0.0184415397180007,0.00392130858590519));
#15308=CARTESIAN_POINT('',(-0.0445,-0.0210020244467008,0.00323522876826008));
#15309=CARTESIAN_POINT('',(-0.0445,-0.0235625091754008,0.00254914895061497));
#15310=CARTESIAN_POINT('',(-0.0445000000003622,-0.01,-0.0173205080756646));
#15311=CARTESIAN_POINT('',(-0.044500000000308,-0.01,-0.0197705080752687));
#15312=CARTESIAN_POINT('',(-0.044500000000337,-0.0200000000003441,2.58823356637625E-19));
#15313=CARTESIAN_POINT('',(-0.044500000000337,-0.02,-0.00244999999980786));
#15314=CARTESIAN_POINT('',(-0.0445000000003614,-0.0200000000006125,0.00244999999974705));
#15315=CARTESIAN_POINT('',(-0.044500000000337,-0.0199999999996559,-5.49576725493911E-20));
#15316=CARTESIAN_POINT('',(-0.0445000000003622,-0.01,0.0173205080756646));
#15317=CARTESIAN_POINT('',(-0.0445000000004165,-0.01,0.0148705080755215));
#15318=CARTESIAN_POINT('',(-0.0445000000003622,0.01,0.0173205080756646));
#15319=CARTESIAN_POINT('',(-0.0445000000004165,0.01,0.0148705080755215));
#15320=CARTESIAN_POINT('',(-0.044500000000337,0.0199999999996559,9.70768175342268E-20));
#15321=CARTESIAN_POINT('',(-0.044500000000337,0.02,-0.00244999999980786));
#15322=CARTESIAN_POINT('',(-0.0445000000003614,0.0199999999993875,0.00244999999974705));
#15323=CARTESIAN_POINT('',(-0.044500000000337,0.0200000000003441,-3.39924582891466E-19));
#15324=CARTESIAN_POINT('',(-0.0445000000003622,0.01,-0.0173205080756646));
#15325=CARTESIAN_POINT('',(-0.044500000000308,0.01,-0.0197705080752687));
#15326=CARTESIAN_POINT('',(-0.0331339745963505,2.10159751068267E-14,-6.83211248137564E-19));
#15327=CARTESIAN_POINT('',(-0.0331339745963505,1.9700566598701E-15,-0.0175358983853182));
#15328=CARTESIAN_POINT('',(-0.0342520085854507,-2.75308153152585E-18,-0.0165358983850228));
#15329=CARTESIAN_POINT('',(-0.0342520085854131,0.0039504121119975,-0.0160570912542433));
#15330=CARTESIAN_POINT('',(-0.0342520085854251,0.00265925059751097,-0.0163747465508529));
#15331=CARTESIAN_POINT('',(-0.0342520085854379,0.0013296627181151,-0.0165358983850421));
#15332=CARTESIAN_POINT('',(-0.0342520085854507,2.21354587678372E-17,-0.0165358983850228));
#15333=CARTESIAN_POINT('',(-0.0342520089022404,0.00395041215716228,-0.0160570913151623));
#15334=CARTESIAN_POINT('',(-0.034433013025824,0.00415647342831627,-0.0162631525862801));
#15335=CARTESIAN_POINT('',(-0.0343819209654274,0.00408372706329651,-0.0161904062212731));
#15336=CARTESIAN_POINT('',(-0.0343218321493816,0.00401493175248625,-0.0161216109104749));
#15337=CARTESIAN_POINT('',(-0.0342520087109173,0.00395041221532456,-0.0160570913733245));
#15338=CARTESIAN_POINT('',(-0.0344330128635322,0.00415647320725126,-0.0162631523535427));
#15339=CARTESIAN_POINT('',(-0.0344330127020119,0.0120060661714172,-0.0117311874792547));
#15340=CARTESIAN_POINT('',(-0.0344330127020133,0.00986802652236389,-0.0139193244899128));
#15341=CARTESIAN_POINT('',(-0.034433012702027,0.00712047520748447,-0.0155056239641693));
#15342=CARTESIAN_POINT('',(-0.0344330127020451,0.00415647313777669,-0.0162631520817075));
#15343=CARTESIAN_POINT('',(-0.0344330130235902,0.0120060665703178,-0.0117311878690224));
#15344=CARTESIAN_POINT('',(-0.0342520086858872,0.0119306429240885,-0.0114497029892201));
#15345=CARTESIAN_POINT('',(-0.0343218322133286,0.0119542587426544,-0.0115378384239647));
#15346=CARTESIAN_POINT('',(-0.0343819208998164,0.0119794395195841,-0.0116318143628348));
#15347=CARTESIAN_POINT('',(-0.0344330130239393,0.0120060665702831,-0.0117311878688929));
#15348=CARTESIAN_POINT('',(-0.0342520087102053,0.01193064288788,-0.0114497028645091));
#15349=CARTESIAN_POINT('',(-0.0342520085854456,0.0158810549917541,-0.00460738838842381));
#15350=CARTESIAN_POINT('',(-0.0342520085854222,0.0151400885910336,-0.00716140102293671));
#15351=CARTESIAN_POINT('',(-0.0342520085854116,0.0137719995116387,-0.00953100081866742));
#15352=CARTESIAN_POINT('',(-0.0342520085854105,0.0119306428896003,-0.0114497028629186));
#15353=CARTESIAN_POINT('',(-0.0342520089017979,0.015881055068089,-0.00460738837380816));
#15354=CARTESIAN_POINT('',(-0.0344330129938737,0.0161625399379626,-0.00453196473023928));
#15355=CARTESIAN_POINT('',(-0.034381920935403,0.016063166568659,-0.00455859174429499));
#15356=CARTESIAN_POINT('',(-0.0343218321405072,0.0159691904637724,-0.00458377256570873));
#15357=CARTESIAN_POINT('',(-0.0342520087100322,0.0158810551471781,-0.00460738835261631));
#15358=CARTESIAN_POINT('',(-0.0344330128473697,0.0161625396544538,-0.00453196480620524));
#15359=CARTESIAN_POINT('',(-0.0344330127014593,0.,-9.36178073300934E-16));
#15360=CARTESIAN_POINT('',(-0.0344330129926893,0.0161625399363783,0.00453196473066377));
#15361=CARTESIAN_POINT('',(-0.0342520086857044,0.0158810551164701,0.00460738836084449));
#15362=CARTESIAN_POINT('',(-0.034321832199017,0.0159691905333651,0.00458377254706142));
#15363=CARTESIAN_POINT('',(-0.034381920878985,0.0160631664582187,0.00455859177388738));
#15364=CARTESIAN_POINT('',(-0.0344330129962152,0.0161625399425169,0.00453196472901897));
#15365=CARTESIAN_POINT('',(-0.0342520087102228,0.0158810549894791,0.0046073883955136));
#15366=CARTESIAN_POINT('',(-0.0342520085854105,0.0119306428896003,0.0114497028629186));
#15367=CARTESIAN_POINT('',(-0.0342520085854116,0.0137719995099208,0.00953100082045744));
#15368=CARTESIAN_POINT('',(-0.0342520085854222,0.0151400885885014,0.00716140102736863));
#15369=CARTESIAN_POINT('',(-0.0342520085854456,0.0158810549896802,0.00460738839557196));
#15370=CARTESIAN_POINT('',(-0.034252008901483,0.0119306429110209,0.0114497029404512));
#15371=CARTESIAN_POINT('',(-0.034433013023346,0.0120060665704802,0.0117311878682453));
#15372=CARTESIAN_POINT('',(-0.0343819209636497,0.0119794395533804,0.0116318144875807));
#15373=CARTESIAN_POINT('',(-0.034321832146695,0.0119542587212213,0.0115378383439753));
#15374=CARTESIAN_POINT('',(-0.0342520087094024,0.0119306429320419,0.0114497030189024));
#15375=CARTESIAN_POINT('',(-0.0344330128624694,0.0120060664878914,0.0117311875540647));
#15376=CARTESIAN_POINT('',(-0.0344330127020451,0.00415647328920086,0.0162631520430071));
#15377=CARTESIAN_POINT('',(-0.034433012702027,0.00712047535552922,0.0155056238969325));
#15378=CARTESIAN_POINT('',(-0.0344330127020133,0.00986802665874799,0.0139193243940575));
#15379=CARTESIAN_POINT('',(-0.0344330127020119,0.012006066288595,0.0117311873593312));
#15380=CARTESIAN_POINT('',(-0.0344330130250702,0.00415647342795653,0.0162631525859204));
#15381=CARTESIAN_POINT('',(-0.0342520086868176,0.00395041219305555,0.0160570913510556));
#15382=CARTESIAN_POINT('',(-0.0343218322145698,0.00401493180963198,0.0161216109676207));
#15383=CARTESIAN_POINT('',(-0.0343819209012451,0.00408372697198972,0.0161904061299663));
#15384=CARTESIAN_POINT('',(-0.0344330130254722,0.00415647342781538,0.0162631525857792));
#15385=CARTESIAN_POINT('',(-0.0342520087102066,0.00395041210349994,0.0160570912562923));
#15386=CARTESIAN_POINT('',(-0.0342520085854507,-3.62334336342478E-17,0.0165358983850228));
#15387=CARTESIAN_POINT('',(-0.0342520085854379,0.00132966271520138,0.0165358983850421));
#15388=CARTESIAN_POINT('',(-0.0342520085854251,0.00265925059168442,0.0163747465515626));
#15389=CARTESIAN_POINT('',(-0.0342520085854131,0.00395041210350958,0.0160570912563315));
#15390=CARTESIAN_POINT('',(-0.0342520087102254,-1.48481175253027E-12,0.0165358983850114));
#15391=CARTESIAN_POINT('',(-0.0331339745963505,2.52979239737867E-14,0.0175358983853182));
#15392=CARTESIAN_POINT('',(-0.0331339745963505,-2.10154316653151E-14,8.38648712071716E-19));
#15393=CARTESIAN_POINT('',(-0.0342520086872413,-0.00395041219344707,-0.0160570913514471));
#15394=CARTESIAN_POINT('',(-0.0343218322149425,-0.00401493181003064,-0.0161216109680193));
#15395=CARTESIAN_POINT('',(-0.0343819209015701,-0.00408372697239052,-0.0161904061303671));
#15396=CARTESIAN_POINT('',(-0.0344330130257521,-0.00415647342821389,-0.0162631525861777));
#15397=CARTESIAN_POINT('',(-0.0342520087102066,-0.00395041210679331,-0.0160570912554821));
#15398=CARTESIAN_POINT('',(-0.0344330130253497,-0.0041564734283552,-0.016263152586319));
#15399=CARTESIAN_POINT('',(-0.0342520085854507,-1.29547937350208E-17,-0.0165358983850228));
#15400=CARTESIAN_POINT('',(-0.0342520085854379,-0.00132966271633194,-0.0165358983850421));
#15401=CARTESIAN_POINT('',(-0.0342520085854251,-0.00265925059394516,-0.0163747465512872));
#15402=CARTESIAN_POINT('',(-0.0342520085854131,-0.00395041210680295,-0.0160570912555213));
#15403=CARTESIAN_POINT('',(-0.0342520085854131,-0.00395041211199747,0.0160570912542433));
#15404=CARTESIAN_POINT('',(-0.0342520085854251,-0.00265925059799155,0.0163747465507347));
#15405=CARTESIAN_POINT('',(-0.0342520085854379,-0.00132966271910495,0.0165358983849227));
#15406=CARTESIAN_POINT('',(-0.0342520085854507,-1.48481417980218E-12,0.0165358983850228));
#15407=CARTESIAN_POINT('',(-0.0342520089022404,-0.00395041215716228,0.0160570913151623));
#15408=CARTESIAN_POINT('',(-0.0344330130255441,-0.00415647342791775,0.0162631525858816));
#15409=CARTESIAN_POINT('',(-0.0343819209651601,-0.00408372706297781,0.0161904062209545));
#15410=CARTESIAN_POINT('',(-0.0343218321493167,-0.00401493175242626,0.0161216109104149));
#15411=CARTESIAN_POINT('',(-0.0342520087109173,-0.00395041221532456,0.0160570913733245));
#15412=CARTESIAN_POINT('',(-0.0344330128633927,-0.00415647320705185,0.0162631523533433));
#15413=CARTESIAN_POINT('',(-0.0344330127020119,-0.0120060661717061,0.011731187478959));
#15414=CARTESIAN_POINT('',(-0.0344330127020133,-0.00986802652257684,0.0139193244898027));
#15415=CARTESIAN_POINT('',(-0.034433012702027,-0.00712047520753155,0.0155056239641843));
#15416=CARTESIAN_POINT('',(-0.0344330127020451,-0.00415647313763734,0.0162631520817431));
#15417=CARTESIAN_POINT('',(-0.0344330130231881,-0.012006066570108,0.0117311878682395));
#15418=CARTESIAN_POINT('',(-0.0342520087094023,-0.0119306429320419,0.0114497030189024));
#15419=CARTESIAN_POINT('',(-0.0343218322266828,-0.0119542587482748,0.0115378384449406));
#15420=CARTESIAN_POINT('',(-0.0343819209052242,-0.0119794395224397,0.0116318143734919));
#15421=CARTESIAN_POINT('',(-0.03443301302348,-0.0120060665700438,0.0117311878679997));
#15422=CARTESIAN_POINT('',(-0.034252008839487,-0.0119306428898001,0.0114497028624593));
#15423=CARTESIAN_POINT('',(-0.0342520085854456,-0.0158810549917541,0.00460738838842376));
#15424=CARTESIAN_POINT('',(-0.0342520085854222,-0.0151400885910772,0.0071614010227863));
#15425=CARTESIAN_POINT('',(-0.0342520085854116,-0.013771999511801,0.00953100081838915));
#15426=CARTESIAN_POINT('',(-0.0342520085854105,-0.0119306428899256,0.0114497028625797));
#15427=CARTESIAN_POINT('',(-0.0342520089017979,-0.015881055068089,0.00460738837380815));
#15428=CARTESIAN_POINT('',(-0.0344330130210024,-0.016162539995109,0.00453196471727475));
#15429=CARTESIAN_POINT('',(-0.0343819209617668,-0.0160631666155137,0.00455859173408813));
#15430=CARTESIAN_POINT('',(-0.0343218321465883,-0.0159691904714484,0.00458377256365195));
#15431=CARTESIAN_POINT('',(-0.0342520087100322,-0.0158810551471781,0.00460738835261631));
#15432=CARTESIAN_POINT('',(-0.034433012862003,-0.0161625396803212,0.00453196480545577));
#15433=CARTESIAN_POINT('',(-0.034433012702032,-0.0161625394592827,-0.00453196456511526));
#15434=CARTESIAN_POINT('',(-0.0344330127020152,-0.0169885018748211,-0.00158629940353296));
#15435=CARTESIAN_POINT('',(-0.0344330127020152,-0.0169885018585916,0.00158629957734368));
#15436=CARTESIAN_POINT('',(-0.034433012702032,-0.0161625394129158,0.00453196473047549));
#15437=CARTESIAN_POINT('',(-0.0344330130224785,-0.0161625399943182,-0.00453196471513884));
#15438=CARTESIAN_POINT('',(-0.0342520086861361,-0.015881055117015,-0.00460738836069848));
#15439=CARTESIAN_POINT('',(-0.0343218322129477,-0.0159691905510249,-0.00458377254232949));
#15440=CARTESIAN_POINT('',(-0.0343819208988127,-0.016063166488791,-0.00455859176569555));
#15441=CARTESIAN_POINT('',(-0.0344330130226463,-0.0161625399939248,-0.00453196471524426));
#15442=CARTESIAN_POINT('',(-0.0342520087102228,-0.0158810549904241,-0.00460738839225635));
#15443=CARTESIAN_POINT('',(-0.0342520085854105,-0.0119306428896003,-0.0114497028629186));
#15444=CARTESIAN_POINT('',(-0.0342520085854116,-0.0137719995107036,-0.00953100081964178));
#15445=CARTESIAN_POINT('',(-0.0342520085854223,-0.0151400885896553,-0.00716140102534911));
#15446=CARTESIAN_POINT('',(-0.0342520085854456,-0.0158810549906252,-0.00460738839231471));
#15447=CARTESIAN_POINT('',(-0.034252008901483,-0.0119306429110209,-0.0114497029404512));
#15448=CARTESIAN_POINT('',(-0.0344330130226575,-0.0120060665709592,-0.0117311878677442));
#15449=CARTESIAN_POINT('',(-0.0343819209629934,-0.0119794395538897,-0.0116318144871932));
#15450=CARTESIAN_POINT('',(-0.0343218321466391,-0.0119542587212024,-0.0115378383439048));
#15451=CARTESIAN_POINT('',(-0.0342520087094023,-0.0119306429320419,-0.0114497030189024));
#15452=CARTESIAN_POINT('',(-0.0344330128623293,-0.0120060664878185,-0.0117311875537928));
#15453=CARTESIAN_POINT('',(-0.0344330127020451,-0.00415647328947946,-0.0162631520429359));
#15454=CARTESIAN_POINT('',(-0.034433012702027,-0.00712047535574833,-0.0155056238968224));
#15455=CARTESIAN_POINT('',(-0.0344330127020133,-0.00986802665890055,-0.0139193243939388));
#15456=CARTESIAN_POINT('',(-0.0344330127020119,-0.0120060662886953,-0.0117311873592286));
#15457=CARTESIAN_POINT('',(-0.0442000000003118,0.01,-0.017320508075658));
#15458=CARTESIAN_POINT('',(-0.0442000000003118,0.01,-0.017320508075658));
#15459=CARTESIAN_POINT('',(-0.044199999875144,0.00813804538124414,-0.0183955080746721));
#15460=CARTESIAN_POINT('',(-0.0442000000002041,0.01,-0.015170508075624));
#15461=CARTESIAN_POINT('',(-0.0442000000001921,0.01,-0.015170508075624));
#15462=CARTESIAN_POINT('',(-0.044200000000204,0.00924950842193217,-0.015170508075624));
#15463=CARTESIAN_POINT('',(-0.0442000000002087,0.00776993675738555,-0.0160329804609734));
#15464=CARTESIAN_POINT('',(-0.0442000000001946,0.00776279959244236,-0.0177455633018591));
#15465=CARTESIAN_POINT('',(-0.0442000000001921,0.00813804538092926,-0.0183955080741079));
#15466=CARTESIAN_POINT('',(-0.0442000000001119,0.0200000000003509,9.42587836741818E-20));
#15467=CARTESIAN_POINT('',(-0.0442000000001119,0.0200000000003509,9.42587836741817E-20));
#15468=CARTESIAN_POINT('',(-0.044199999875096,0.0199999999995591,-0.00214999999980227));
#15469=CARTESIAN_POINT('',(-0.044199999875096,0.02,0.00214999999980227));
#15470=CARTESIAN_POINT('',(-0.0442000000001921,0.02,0.00214999999960454));
#15471=CARTESIAN_POINT('',(-0.0443570796329555,0.0200000000000128,0.00214999999964654));
#15472=CARTESIAN_POINT('',(-0.0445000000003256,0.0200000000000035,0.00229292036704452));
#15473=CARTESIAN_POINT('',(-0.0445000000003369,0.02,0.00244999999980785));
#15474=CARTESIAN_POINT('',(-0.0445000000003369,0.02,-0.00244999999980785));
#15475=CARTESIAN_POINT('',(-0.0445000000003255,0.0200000000000035,-0.00229292036704452));
#15476=CARTESIAN_POINT('',(-0.0443570796329555,0.0200000000000127,-0.00214999999964655));
#15477=CARTESIAN_POINT('',(-0.0442000000001921,0.02,-0.00214999999960454));
#15478=CARTESIAN_POINT('',(-0.0442000000001119,0.0199999999996491,-3.34075843811147E-19));
#15479=CARTESIAN_POINT('',(-0.0442000000001921,0.02,0.00214999999960455));
#15480=CARTESIAN_POINT('',(-0.0442000000002049,0.0194371313163136,0.00214999999969641));
#15481=CARTESIAN_POINT('',(-0.0442000000002303,0.0183158751829514,0.00168476499344337));
#15482=CARTESIAN_POINT('',(-0.0442000000002463,0.0176170624086775,2.44360809131443E-13));
#15483=CARTESIAN_POINT('',(-0.0442000000002303,0.0183158751826059,-0.00168476499309796));
#15484=CARTESIAN_POINT('',(-0.0442000000002049,0.0194371313158727,-0.00214999999958097));
#15485=CARTESIAN_POINT('',(-0.0442000000001921,0.0199999999995591,-0.00214999999960455));
#15486=CARTESIAN_POINT('',(-0.0442000000003118,0.01,0.017320508075658));
#15487=CARTESIAN_POINT('',(-0.0442000000001921,0.01,0.019470508075692));
#15488=CARTESIAN_POINT('',(-0.0442000000001842,0.00924950842153377,0.019470508075692));
#15489=CARTESIAN_POINT('',(-0.0442000000001857,0.00851329117083413,0.0190454528477522));
#15490=CARTESIAN_POINT('',(-0.0442000000001921,0.00813804538168881,0.0183955080754235));
#15491=CARTESIAN_POINT('',(-0.0442000000001565,0.01,0.019470508075692));
#15492=CARTESIAN_POINT('',(-0.044199999875,0.00813804538167257,0.0183955080754328));
#15493=CARTESIAN_POINT('',(-0.0442,0.01,0.017320508076));
#15494=CARTESIAN_POINT('',(-0.044199999875096,0.0118619546182749,0.016245508076153));
#15495=CARTESIAN_POINT('',(-0.0442000000001684,0.01,0.017320508075658));
#15496=CARTESIAN_POINT('',(-0.0442000000003118,-0.01,0.017320508075658));
#15497=CARTESIAN_POINT('',(-0.0442000000001921,-0.00999999999999999,0.019470508075692));
#15498=CARTESIAN_POINT('',(-0.0442000000001802,-0.0107504915780945,0.019470508075692));
#15499=CARTESIAN_POINT('',(-0.0442000000001755,-0.0122300632426902,0.0186080356902759));
#15500=CARTESIAN_POINT('',(-0.0442000000001896,-0.0122372004075394,0.0168954528493138));
#15501=CARTESIAN_POINT('',(-0.0442000000001921,-0.0118619546189909,0.0162455080770697));
#15502=CARTESIAN_POINT('',(-0.0442000000001803,-0.01,0.019470508075692));
#15503=CARTESIAN_POINT('',(-0.044199999875,-0.0118619546176726,0.0162455080754329));
#15504=CARTESIAN_POINT('',(-0.0442,-0.01,0.017320508076));
#15505=CARTESIAN_POINT('',(-0.044199999875096,-0.00813804538124414,0.0183955080746721));
#15506=CARTESIAN_POINT('',(-0.044200000000216,-0.01,0.017320508075658));
#15507=CARTESIAN_POINT('',(-0.0442000000001119,-0.0199999999996491,3.6189501084092E-19));
#15508=CARTESIAN_POINT('',(-0.0442000000001119,-0.0199999999996491,3.6189501084092E-19));
#15509=CARTESIAN_POINT('',(-0.044199999875096,-0.0199999999998069,-0.00214999999980227));
#15510=CARTESIAN_POINT('',(-0.044199999875096,-0.0199999999995591,0.00214999999980227));
#15511=CARTESIAN_POINT('',(-0.0442000000001921,-0.02,0.00214999999960455));
#15512=CARTESIAN_POINT('',(-0.0443570796329555,-0.0199999999999872,0.00214999999964654));
#15513=CARTESIAN_POINT('',(-0.0445000000003255,-0.0199999999999965,0.00229292036704452));
#15514=CARTESIAN_POINT('',(-0.0445000000003369,-0.02,0.00244999999980786));
#15515=CARTESIAN_POINT('',(-0.0445000000003369,-0.02,-0.00244999999980786));
#15516=CARTESIAN_POINT('',(-0.0445000000003255,-0.0199999999999965,-0.00229292036704452));
#15517=CARTESIAN_POINT('',(-0.0443570796329555,-0.0199999999999872,-0.00214999999964655));
#15518=CARTESIAN_POINT('',(-0.0442000000001921,-0.02,-0.00214999999960455));
#15519=CARTESIAN_POINT('',(-0.0442000000001119,-0.0200000000003509,-1.67275847704353E-19));
#15520=CARTESIAN_POINT('',(-0.0442000000001922,-0.0200000000003509,-1.6727584759041E-19));
#15521=CARTESIAN_POINT('',(-0.0442000000003118,-0.01,-0.017320508075658));
#15522=CARTESIAN_POINT('',(-0.0442000000001921,-0.00813804538092926,-0.0183955080741079));
#15523=CARTESIAN_POINT('',(-0.0442000000001946,-0.00776279959244236,-0.017745563301859));
#15524=CARTESIAN_POINT('',(-0.0442000000002087,-0.00776993675738556,-0.0160329804609734));
#15525=CARTESIAN_POINT('',(-0.044200000000204,-0.00924950842193217,-0.015170508075624));
#15526=CARTESIAN_POINT('',(-0.0442000000001921,-0.01,-0.015170508075624));
#15527=CARTESIAN_POINT('',(-0.044199999875096,-0.00813804538146463,-0.018395508075054));
#15528=CARTESIAN_POINT('',(-0.0442000000002758,-0.01,-0.015170508075624));
#15529=CARTESIAN_POINT('',(-0.0442000000003118,-0.01,-0.017320508075658));
#15530=CARTESIAN_POINT('',(-0.0393760042937274,-0.012974499756,0.0153454297215));
#15531=CARTESIAN_POINT('',(-0.0384862022102034,-0.0140183571386411,0.0192411585091307));
#15532=CARTESIAN_POINT('',(-0.0370999087763453,-0.013352347141783,0.0167555753626619));
#15533=CARTESIAN_POINT('',(-0.035733240200822,-0.0126836892229704,0.0142601100369248));
#15534=CARTESIAN_POINT('',(-0.0344330130228521,-0.0120060665701493,0.0117311878683936));
#15535=CARTESIAN_POINT('',(-0.0384862022685832,-0.0140183571306401,0.0192411584797665));
#15536=CARTESIAN_POINT('',(-0.0444805635282456,-0.014018356622,0.019241156581));
#15537=CARTESIAN_POINT('',(-0.0424824431083581,-0.014018356622,0.019241156581));
#15538=CARTESIAN_POINT('',(-0.0404843226884707,-0.014018356622,0.019241156581));
#15539=CARTESIAN_POINT('',(-0.0384862022685832,-0.014018356622,0.019241156581));
#15540=CARTESIAN_POINT('',(-0.0444805635319336,-0.0140183566169593,0.019241156562634));
#15541=CARTESIAN_POINT('',(-0.0445000000129707,-0.0139888823224751,0.0191311570460743));
#15542=CARTESIAN_POINT('',(-0.0445000000166381,-0.0139989932774539,0.0191688916437659));
#15543=CARTESIAN_POINT('',(-0.0444935802519982,-0.0140088206617122,0.0192055678927093));
#15544=CARTESIAN_POINT('',(-0.044480563533571,-0.0140183566158597,0.0192411565580842));
#15545=CARTESIAN_POINT('',(-0.034252008839487,-0.01193064289,0.011449702862));
#15546=CARTESIAN_POINT('',(-0.0376680058929914,-0.01193064289,0.011449702862));
#15547=CARTESIAN_POINT('',(-0.0410840029464957,-0.01193064289,0.011449702862));
#15548=CARTESIAN_POINT('',(-0.0445,-0.01193064289,0.011449702862));
#15549=CARTESIAN_POINT('',(-0.0442000000055845,-1.31051679305457E-11,2.57086317240235E-11));
#15550=CARTESIAN_POINT('',(-0.0444805635188123,-0.0140183566003539,0.0192411565622842));
#15551=CARTESIAN_POINT('',(-0.0444283437647183,-0.0140566124263418,0.0193839292026706));
#15552=CARTESIAN_POINT('',(-0.0443084984770918,-0.0139913606486926,0.0195000961256288));
#15553=CARTESIAN_POINT('',(-0.0442000000005702,-0.0139023583532664,0.0195633440958977));
#15554=CARTESIAN_POINT('',(-0.0441999998126405,-0.0139023583539755,0.0195633440953938));
#15555=CARTESIAN_POINT('',(-0.0442000000001921,-0.0139023583537827,0.0195633440951225));
#15556=CARTESIAN_POINT('',(-0.0442000000001617,-0.0126734170487115,0.0204366703701264));
#15557=CARTESIAN_POINT('',(-0.0442000000001615,-0.0113619671847084,0.0211938363022351));
#15558=CARTESIAN_POINT('',(-0.0442000000001921,-0.00999117379229732,0.0218214675548383));
#15559=CARTESIAN_POINT('',(-0.0441999998752201,-0.00999117379233075,0.0218214675549114));
#15560=CARTESIAN_POINT('',(-0.0442000000004402,-0.00999117379338535,0.0218214675543966));
#15561=CARTESIAN_POINT('',(-0.0443082283281583,-0.00989214828484741,0.0218668073585679));
#15562=CARTESIAN_POINT('',(-0.0444284338973912,-0.00975848851517938,0.0218651676816527));
#15563=CARTESIAN_POINT('',(-0.044480563529604,-0.00965415207773743,0.0217608312354494));
#15564=CARTESIAN_POINT('',(-0.0444805634409269,-0.00965415208178998,0.02176083123879));
#15565=CARTESIAN_POINT('',(-0.0444805635173688,-0.00965415208444921,0.0217608312191856));
#15566=CARTESIAN_POINT('',(-0.044493580238476,-0.00962809936884818,0.0217347785035891));
#15567=CARTESIAN_POINT('',(-0.0445000000034239,-0.00960125048409792,0.0217079296411072));
#15568=CARTESIAN_POINT('',(-0.0445000000002923,-0.00957362683652262,0.0216803059935367));
#15569=CARTESIAN_POINT('',(-0.0393760042937274,-0.00680228209300001,0.0189089612505));
#15570=CARTESIAN_POINT('',(-0.0384862032523497,-0.009654152087,0.021760831244));
#15571=CARTESIAN_POINT('',(-0.040484323344315,-0.009654152087,0.021760831244));
#15572=CARTESIAN_POINT('',(-0.0424824434362803,-0.009654152087,0.021760831244));
#15573=CARTESIAN_POINT('',(-0.0444805635282456,-0.009654152087,0.021760831244));
#15574=CARTESIAN_POINT('',(-0.0384862032523497,-0.00965415458831338,0.0217608337456173));
#15575=CARTESIAN_POINT('',(-0.0344330130247402,-0.00415647342820006,0.016263152586164));
#15576=CARTESIAN_POINT('',(-0.0357332404762259,-0.00600777333354867,0.018114452491188));
#15577=CARTESIAN_POINT('',(-0.0370999095145224,-0.00783458133811811,0.0199412604954371));
#15578=CARTESIAN_POINT('',(-0.0384862032521895,-0.00965415486626073,0.0217608340232608));
#15579=CARTESIAN_POINT('',(-0.044499999875,-0.00395041209900001,0.016057091257));
#15580=CARTESIAN_POINT('',(-0.0410840028840801,-0.00395041209900001,0.016057091257));
#15581=CARTESIAN_POINT('',(-0.0376680058931603,-0.00395041209900001,0.016057091257));
#15582=CARTESIAN_POINT('',(-0.0342520089022404,-0.00395041209900001,0.016057091257));
#15583=CARTESIAN_POINT('',(-0.0295,0.,0.));
#15584=CARTESIAN_POINT('',(-0.04449999975,0.00395041209500243,0.0160570912583414));
#15585=CARTESIAN_POINT('',(-0.0410840027783333,0.00395041209500243,0.0160570912583414));
#15586=CARTESIAN_POINT('',(-0.0376680058066667,0.00395041209500243,0.0160570912583414));
#15587=CARTESIAN_POINT('',(-0.034252008835,0.00395041209500243,0.0160570912583414));
#15588=CARTESIAN_POINT('',(-0.0393760042937274,0.00680228209300001,0.0189089612505));
#15589=CARTESIAN_POINT('',(-0.0384862022100965,0.00965415349846632,0.0217608326554663));
#15590=CARTESIAN_POINT('',(-0.0370999087769037,0.0078345803494711,0.0199412595067901));
#15591=CARTESIAN_POINT('',(-0.0357332402020445,0.00600777294316644,0.0181144521008057));
#15592=CARTESIAN_POINT('',(-0.0344330130246683,0.00415647342809768,0.0162631525860615));
#15593=CARTESIAN_POINT('',(-0.0384862022685706,0.00965415347674228,0.02176083263408));
#15594=CARTESIAN_POINT('',(-0.0444805635282456,0.009654152087,0.021760831244));
#15595=CARTESIAN_POINT('',(-0.0424824431083539,0.009654152087,0.021760831244));
#15596=CARTESIAN_POINT('',(-0.0404843226884622,0.009654152087,0.021760831244));
#15597=CARTESIAN_POINT('',(-0.0384862022685706,0.009654152087,0.021760831244));
#15598=CARTESIAN_POINT('',(-0.0444805635304399,0.00965415207631084,0.0217608312336668));
#15599=CARTESIAN_POINT('',(-0.0445000000193966,0.00957362685480404,0.0216803059848004));
#15600=CARTESIAN_POINT('',(-0.0445000000226021,0.0096012504979128,0.0217079296279044));
#15601=CARTESIAN_POINT('',(-0.0444935802508817,0.00962809936227532,0.0217347785192799));
#15602=CARTESIAN_POINT('',(-0.0444805635321006,0.0096541520732335,0.0217608312302335));
#15603=CARTESIAN_POINT('',(-0.0442000000055845,1.31053917940051E-11,2.57091155293273E-11));
#15604=CARTESIAN_POINT('',(-0.0444805635171393,0.00965415208412121,0.021760831219211));
#15605=CARTESIAN_POINT('',(-0.0444283878394043,0.00975858068479965,0.0218652598335098));
#15606=CARTESIAN_POINT('',(-0.0443084084393283,0.00989198348882134,0.0218668828120512));
#15607=CARTESIAN_POINT('',(-0.0442000000004402,0.00999117379338535,0.0218214675543966));
#15608=CARTESIAN_POINT('',(-0.044199999844711,0.00999117381829546,0.0218214675430476));
#15609=CARTESIAN_POINT('',(-0.0442000000001922,0.00999117381825278,0.0218214675429544));
#15610=CARTESIAN_POINT('',(-0.0442000000001615,0.0113619671891927,0.0211938362982097));
#15611=CARTESIAN_POINT('',(-0.0442000000001618,0.0126734170333715,0.0204366703779577));
#15612=CARTESIAN_POINT('',(-0.0442000000001922,0.0139023583213122,0.0195633441181971));
#15613=CARTESIAN_POINT('',(-0.0441999997741247,0.013902358321505,0.0195633441184683));
#15614=CARTESIAN_POINT('',(-0.0444805635187775,0.014018356600366,0.0192411565623608));
#15615=CARTESIAN_POINT('',(-0.0444283437696937,0.0140566124226209,0.0193839291889622));
#15616=CARTESIAN_POINT('',(-0.0443084984666164,0.0139913606401035,0.0195000961317325));
#15617=CARTESIAN_POINT('',(-0.0442000000005702,0.0139023583532664,0.0195633440958977));
#15618=CARTESIAN_POINT('',(-0.0444805634416584,0.0140183566195451,0.0192411565718381));
#15619=CARTESIAN_POINT('',(-0.0444805635186538,0.0140183566004662,0.0192411565622887));
#15620=CARTESIAN_POINT('',(-0.0444935802393538,0.0140088206446543,0.0192055678907021));
#15621=CARTESIAN_POINT('',(-0.0445000000040598,0.0139989932902217,0.0191688916430041));
#15622=CARTESIAN_POINT('',(-0.0445000000004408,0.0139888823334323,0.0191311570385554));
#15623=CARTESIAN_POINT('',(-0.0393760042937274,0.012974499756,0.0153454297215));
#15624=CARTESIAN_POINT('',(-0.0384862032524104,0.014018356622,0.019241156581));
#15625=CARTESIAN_POINT('',(-0.0404843233443555,0.014018356622,0.019241156581));
#15626=CARTESIAN_POINT('',(-0.0424824434363005,0.014018356622,0.019241156581));
#15627=CARTESIAN_POINT('',(-0.0444805635282456,0.014018356622,0.019241156581));
#15628=CARTESIAN_POINT('',(-0.0384862032524104,0.014018357537509,0.0192411599981722));
#15629=CARTESIAN_POINT('',(-0.0344330130229279,0.0120060665701866,0.0117311878685389));
#15630=CARTESIAN_POINT('',(-0.0357332404750095,0.0126836893658611,0.0142601105702061));
#15631=CARTESIAN_POINT('',(-0.0370999095139687,0.0133523475036553,0.0167555767131877));
#15632=CARTESIAN_POINT('',(-0.0384862032523048,0.0140183576392926,0.0192411603775878));
#15633=CARTESIAN_POINT('',(-0.0445,0.01193064289,0.011449702862));
#15634=CARTESIAN_POINT('',(-0.041084002967161,0.01193064289,0.011449702862));
#15635=CARTESIAN_POINT('',(-0.037668005934322,0.01193064289,0.011449702862));
#15636=CARTESIAN_POINT('',(-0.034252008901483,0.01193064289,0.011449702862));
#15637=CARTESIAN_POINT('',(-0.0295,0.,0.));
#15638=CARTESIAN_POINT('',(-0.044199999749838,0.0158810549872041,0.00460738840260347));
#15639=CARTESIAN_POINT('',(-0.0408840027782253,0.0158810549872041,0.00460738840260347));
#15640=CARTESIAN_POINT('',(-0.0375680058066127,0.0158810549872041,0.00460738840260347));
#15641=CARTESIAN_POINT('',(-0.034252008835,0.0158810549872041,0.00460738840260347));
#15642=CARTESIAN_POINT('',(-0.0441999999375076,0.0158810551716672,0.00460738834575336));
#15643=CARTESIAN_POINT('',(-0.0441999998749613,0.0158810549895393,0.00460738839455436));
#15644=CARTESIAN_POINT('',(-0.0443716844373847,0.0158810549662353,0.00460738847488032));
#15645=CARTESIAN_POINT('',(-0.044500000000068,0.0159304182122806,0.00443700078956962));
#15646=CARTESIAN_POINT('',(-0.0444999999992906,0.0159746109794523,0.00427173728759232));
#15647=CARTESIAN_POINT('',(-0.0442,0.024530335195,0.001979237895));
#15648=CARTESIAN_POINT('',(-0.0442000000000539,0.0236725084664752,0.00251967472754294));
#15649=CARTESIAN_POINT('',(-0.0442000000000539,0.0210753573886682,0.00321557926146354));
#15650=CARTESIAN_POINT('',(-0.0442000000000539,0.0184782063108613,0.00391148379538414));
#15651=CARTESIAN_POINT('',(-0.0442000000000539,0.0158810552330543,0.00460738832930474));
#15652=CARTESIAN_POINT('',(-0.0441999999985952,0.0236725087085416,0.00251967466285297));
#15653=CARTESIAN_POINT('',(-0.0442,0.0235948629946094,0.00222989691563664));
#15654=CARTESIAN_POINT('',(-0.0442000000067454,4.40013553093732E-11,8.52580180210794E-13));
#15655=CARTESIAN_POINT('',(-0.0442000000002482,0.0235948629947446,0.00222989691525306));
#15656=CARTESIAN_POINT('',(-0.044199999875096,0.0238935321461809,0.00225812346418508));
#15657=CARTESIAN_POINT('',(-0.0442000000067717,4.40013553093804E-11,8.52580180210556E-13));
#15658=CARTESIAN_POINT('',(-0.0441999997689131,0.0238935321508499,-0.00225812341441558));
#15659=CARTESIAN_POINT('',(-0.0444805635187719,0.0236725086811496,-0.00251967465380841));
#15660=CARTESIAN_POINT('',(-0.0444283437697893,0.0238152813140498,-0.00248141885441365));
#15661=CARTESIAN_POINT('',(-0.0443084995967842,0.0238832590521061,-0.00236682456350268));
#15662=CARTESIAN_POINT('',(-0.0442000000002077,0.0238935321467111,-0.00225812345827953));
#15663=CARTESIAN_POINT('',(-0.044480563441677,0.023672508698868,-0.00251967466544691));
#15664=CARTESIAN_POINT('',(-0.0444805635187868,0.0236725086811511,-0.00251967465379354));
#15665=CARTESIAN_POINT('',(-0.0444935802398986,0.0236369200083081,-0.0025292106099421));
#15666=CARTESIAN_POINT('',(-0.0445000000044559,0.023600243767542,-0.00253903799543801));
#15667=CARTESIAN_POINT('',(-0.0445000000003558,0.023562509161789,-0.00254914895257684));
#15668=CARTESIAN_POINT('',(-0.0393760042937274,0.0197767818485,-0.003563531529));
#15669=CARTESIAN_POINT('',(-0.044499999875,0.015881054989,-0.004607388395));
#15670=CARTESIAN_POINT('',(-0.0410840028839326,0.015881054989,-0.004607388395));
#15671=CARTESIAN_POINT('',(-0.0376680058928653,0.015881054989,-0.004607388395));
#15672=CARTESIAN_POINT('',(-0.0342520089017979,0.015881054989,-0.004607388395));
#15673=CARTESIAN_POINT('',(-0.0384862032524471,0.023672508708,-0.002519674663));
#15674=CARTESIAN_POINT('',(-0.0404843233443799,0.023672508708,-0.002519674663));
#15675=CARTESIAN_POINT('',(-0.0424824434363127,0.023672508708,-0.002519674663));
#15676=CARTESIAN_POINT('',(-0.0444805635282456,0.023672508708,-0.002519674663));
#15677=CARTESIAN_POINT('',(-0.038486203252447,0.0236725121255199,-0.00251967374727935));
#15678=CARTESIAN_POINT('',(-0.0344330129932801,0.0161625399382474,-0.00453196473016298));
#15679=CARTESIAN_POINT('',(-0.0357332404541263,0.0186914626596971,-0.00385434192918779));
#15680=CARTESIAN_POINT('',(-0.0370999095034317,0.0211869288216903,-0.00318568378630103));
#15681=CARTESIAN_POINT('',(-0.0384862032523079,0.0236725125049948,-0.0025196736455983));
#15682=CARTESIAN_POINT('',(-0.0295,0.,0.));
#15683=CARTESIAN_POINT('',(-0.04449999975,0.0119306428861598,-0.0114497028660997));
#15684=CARTESIAN_POINT('',(-0.0410840027783333,0.0119306428861598,-0.0114497028660997));
#15685=CARTESIAN_POINT('',(-0.0376680058066667,0.0119306428861598,-0.0114497028660997));
#15686=CARTESIAN_POINT('',(-0.034252008835,0.0119306428861598,-0.0114497028660997));
#15687=CARTESIAN_POINT('',(-0.0393760042937274,0.012974499756,-0.0153454297215));
#15688=CARTESIAN_POINT('',(-0.0384862022102251,0.0140183571386519,-0.0192411585091713));
#15689=CARTESIAN_POINT('',(-0.037099908776487,0.0133523471418517,-0.0167555753629181));
#15690=CARTESIAN_POINT('',(-0.035733240201101,0.0126836892231061,-0.0142601100374313));
#15691=CARTESIAN_POINT('',(-0.0344330130232636,0.0120060665703642,-0.0117311878691955));
#15692=CARTESIAN_POINT('',(-0.0384862022686053,0.0140183571306509,-0.0192411584798069));
#15693=CARTESIAN_POINT('',(-0.0444805635282456,0.014018356622,-0.019241156581));
#15694=CARTESIAN_POINT('',(-0.0424824431083655,0.014018356622,-0.019241156581));
#15695=CARTESIAN_POINT('',(-0.0404843226884854,0.014018356622,-0.019241156581));
#15696=CARTESIAN_POINT('',(-0.0384862022686053,0.014018356622,-0.019241156581));
#15697=CARTESIAN_POINT('',(-0.0444805635319414,0.0140183566169537,-0.0192411565626129));
#15698=CARTESIAN_POINT('',(-0.0445000000129707,0.0139888823224751,-0.0191311570460743));
#15699=CARTESIAN_POINT('',(-0.044500000016638,0.0139989932774517,-0.0191688916437578));
#15700=CARTESIAN_POINT('',(-0.0444935802520009,0.0140088206617081,-0.0192055678926938));
#15701=CARTESIAN_POINT('',(-0.0444805635335792,0.0140183566158538,-0.0192411565580619));
#15702=CARTESIAN_POINT('',(-0.0442000000055849,1.31055792648314E-11,-2.57092921253891E-11));
#15703=CARTESIAN_POINT('',(-0.0444805635188167,0.014018356600344,-0.019241156562263));
#15704=CARTESIAN_POINT('',(-0.0444283437647304,0.014056612426345,-0.0193839292026541));
#15705=CARTESIAN_POINT('',(-0.0443084984770938,0.0139913606486981,-0.0195000961256248));
#15706=CARTESIAN_POINT('',(-0.0442000000005702,0.0139023583532664,-0.0195633440958977));
#15707=CARTESIAN_POINT('',(-0.0441999998126405,0.0139023583539033,-0.019563344095445));
#15708=CARTESIAN_POINT('',(-0.0442000000001921,0.0139023583537106,-0.0195633440951738));
#15709=CARTESIAN_POINT('',(-0.0442000000001617,0.0126734170595584,-0.0204366703624114));
#15710=CARTESIAN_POINT('',(-0.0442000000001615,0.0113619672079449,-0.0211938362888249));
#15711=CARTESIAN_POINT('',(-0.0442000000001921,0.00999117382876566,-0.021821467538141));
#15712=CARTESIAN_POINT('',(-0.044199999774127,0.00999117382878557,-0.0218214675381844));
#15713=CARTESIAN_POINT('',(-0.0444805635186256,0.00965415208114367,-0.0217608312162303));
#15714=CARTESIAN_POINT('',(-0.0444283437697871,0.00975866889166734,-0.0218653480433214));
#15715=CARTESIAN_POINT('',(-0.044308500011943,0.00989189970270077,-0.0218669211743478));
#15716=CARTESIAN_POINT('',(-0.0442000000004402,0.00999117379338393,-0.0218214675543935));
#15717=CARTESIAN_POINT('',(-0.0444805634416919,0.00965415208025887,-0.0217608312372589));
#15718=CARTESIAN_POINT('',(-0.0444805635188954,0.00965415208138903,-0.0217608312161197));
#15719=CARTESIAN_POINT('',(-0.0444935802389732,0.00962809936671424,-0.0217347785014494));
#15720=CARTESIAN_POINT('',(-0.0445000000034239,0.00960125048298382,-0.0217079296399931));
#15721=CARTESIAN_POINT('',(-0.0445000000002923,0.00957362683652262,-0.0216803059935368));
#15722=CARTESIAN_POINT('',(-0.0393760042937274,0.00680228209300001,-0.0189089612505));
#15723=CARTESIAN_POINT('',(-0.0384862032527067,0.009654152087,-0.021760831244));
#15724=CARTESIAN_POINT('',(-0.040484323344553,0.009654152087,-0.021760831244));
#15725=CARTESIAN_POINT('',(-0.0424824434363993,0.009654152087,-0.021760831244));
#15726=CARTESIAN_POINT('',(-0.0444805635282456,0.009654152087,-0.021760831244));
#15727=CARTESIAN_POINT('',(-0.0384862032527067,0.00965415458873634,-0.0217608337460403));
#15728=CARTESIAN_POINT('',(-0.0344330130250192,0.00415647342859888,-0.0162631525865627));
#15729=CARTESIAN_POINT('',(-0.0357332404765253,0.00600777333395774,-0.018114452491597));
#15730=CARTESIAN_POINT('',(-0.0370999095149851,0.00783458133873632,-0.0199412604960553));
#15731=CARTESIAN_POINT('',(-0.0384862032526683,0.00965415486689057,-0.0217608340238905));
#15732=CARTESIAN_POINT('',(-0.044499999875,0.00395041209900001,-0.016057091257));
#15733=CARTESIAN_POINT('',(-0.0410840028840801,0.00395041209900001,-0.016057091257));
#15734=CARTESIAN_POINT('',(-0.0376680058931603,0.00395041209900001,-0.016057091257));
#15735=CARTESIAN_POINT('',(-0.0342520089022404,0.00395041209900001,-0.016057091257));
#15736=CARTESIAN_POINT('',(-0.0295,0.,0.));
#15737=CARTESIAN_POINT('',(-0.04449999975,-0.00395041210158917,-0.0160570912567209));
#15738=CARTESIAN_POINT('',(-0.0410840027783333,-0.00395041210158917,-0.0160570912567209));
#15739=CARTESIAN_POINT('',(-0.0376680058066667,-0.00395041210158917,-0.0160570912567209));
#15740=CARTESIAN_POINT('',(-0.034252008835,-0.00395041210158917,-0.0160570912567209));
#15741=CARTESIAN_POINT('',(-0.0393760042937274,-0.00680228209300001,-0.0189089612505));
#15742=CARTESIAN_POINT('',(-0.0384862022103422,-0.00965415349879022,-0.0217608326557902));
#15743=CARTESIAN_POINT('',(-0.037099908777168,-0.00783458034982418,-0.0199412595071432));
#15744=CARTESIAN_POINT('',(-0.0357332402023234,-0.00600777294354627,-0.0181144521011855));
#15745=CARTESIAN_POINT('',(-0.0344330130249473,-0.0041564734284965,-0.0162631525864603));
#15746=CARTESIAN_POINT('',(-0.0384862022688168,-0.00965415347706603,-0.0217608326344038));
#15747=CARTESIAN_POINT('',(-0.0444805635282456,-0.009654152087,-0.021760831244));
#15748=CARTESIAN_POINT('',(-0.042482443108436,-0.009654152087,-0.021760831244));
#15749=CARTESIAN_POINT('',(-0.0404843226886264,-0.009654152087,-0.021760831244));
#15750=CARTESIAN_POINT('',(-0.0384862022688168,-0.009654152087,-0.021760831244));
#15751=CARTESIAN_POINT('',(-0.044480563531975,-0.00965415207323825,-0.0217608312305942));
#15752=CARTESIAN_POINT('',(-0.0445000000193967,-0.00957362685480405,-0.0216803059848005));
#15753=CARTESIAN_POINT('',(-0.044500000022602,-0.00960125049679463,-0.0217079296267862));
#15754=CARTESIAN_POINT('',(-0.0444935802513844,-0.00962809936013126,-0.0217347785171359));
#15755=CARTESIAN_POINT('',(-0.0444805635336362,-0.00965415207016007,-0.0217608312271601));
#15756=CARTESIAN_POINT('',(-0.0442000000055833,-1.31055491163998E-11,-2.57092734960733E-11));
#15757=CARTESIAN_POINT('',(-0.0444805635186711,-0.00965415208105065,-0.0217608312161348));
#15758=CARTESIAN_POINT('',(-0.0444283437648285,-0.00975866890166532,-0.0218653480534098));
#15759=CARTESIAN_POINT('',(-0.0443085000224662,-0.00989189969309658,-0.0218669211787452));
#15760=CARTESIAN_POINT('',(-0.0442000000004402,-0.00999117379338393,-0.0218214675543935));
#15761=CARTESIAN_POINT('',(-0.0441999998126405,-0.00999117379246263,-0.0218214675548153));
#15762=CARTESIAN_POINT('',(-0.0442000000001921,-0.00999117379244271,-0.0218214675547718));
#15763=CARTESIAN_POINT('',(-0.0442000000001615,-0.0113619671727517,-0.0211938363076986));
#15764=CARTESIAN_POINT('',(-0.0442000000001617,-0.0126734170257031,-0.0204366703834131));
#15765=CARTESIAN_POINT('',(-0.0442000000001921,-0.013902358321375,-0.0195633441181525));
#15766=CARTESIAN_POINT('',(-0.0441999997741401,-0.0139023583215678,-0.0195633441184237));
#15767=CARTESIAN_POINT('',(-0.0444805635187713,-0.0140183566003803,-0.0192411565623913));
#15768=CARTESIAN_POINT('',(-0.0444283437696747,-0.0140566124226176,-0.0193839291889904));
#15769=CARTESIAN_POINT('',(-0.0443084984666218,-0.0139913606400945,-0.0195000961317389));
#15770=CARTESIAN_POINT('',(-0.0442000000005701,-0.0139023583532664,-0.0195633440958977));
#15771=CARTESIAN_POINT('',(-0.0444805634416528,-0.0140183566195491,-0.0192411565718533));
#15772=CARTESIAN_POINT('',(-0.0444805635186475,-0.0140183566004804,-0.0192411565623192));
#15773=CARTESIAN_POINT('',(-0.0444935802393554,-0.0140088206446659,-0.0192055678907229));
#15774=CARTESIAN_POINT('',(-0.0445000000040597,-0.0139989932902247,-0.0191688916430152));
#15775=CARTESIAN_POINT('',(-0.0445000000004407,-0.0139888823334323,-0.0191311570385554));
#15776=CARTESIAN_POINT('',(-0.0393760042937274,-0.012974499756,-0.0153454297215));
#15777=CARTESIAN_POINT('',(-0.0384862032529767,-0.014018356622,-0.019241156581));
#15778=CARTESIAN_POINT('',(-0.040484323344733,-0.014018356622,-0.019241156581));
#15779=CARTESIAN_POINT('',(-0.0424824434364893,-0.014018356622,-0.019241156581));
#15780=CARTESIAN_POINT('',(-0.0444805635282456,-0.014018356622,-0.019241156581));
#15781=CARTESIAN_POINT('',(-0.0384862032529767,-0.0140183575377542,-0.0192411599990874));
#15782=CARTESIAN_POINT('',(-0.0344330130222391,-0.0120060665706653,-0.011731187868038));
#15783=CARTESIAN_POINT('',(-0.0357332404745547,-0.0126836893664783,-0.0142601105702223));
#15784=CARTESIAN_POINT('',(-0.0370999095143791,-0.0133523475038579,-0.0167555767139436));
#15785=CARTESIAN_POINT('',(-0.0384862032529973,-0.0140183576396257,-0.019241160378831));
#15786=CARTESIAN_POINT('',(-0.044499999875,-0.01193064289,-0.011449702862));
#15787=CARTESIAN_POINT('',(-0.0410840028838277,-0.01193064289,-0.011449702862));
#15788=CARTESIAN_POINT('',(-0.0376680058926553,-0.01193064289,-0.011449702862));
#15789=CARTESIAN_POINT('',(-0.034252008901483,-0.01193064289,-0.011449702862));
#15790=CARTESIAN_POINT('',(-0.0295,0.,0.));
#15791=CARTESIAN_POINT('',(-0.04449999975,-0.0158810549890941,-0.00460738839608896));
#15792=CARTESIAN_POINT('',(-0.0410840027783333,-0.0158810549890941,-0.00460738839608896));
#15793=CARTESIAN_POINT('',(-0.0376680058066667,-0.0158810549890941,-0.00460738839608896));
#15794=CARTESIAN_POINT('',(-0.034252008835,-0.0158810549890941,-0.00460738839608896));
#15795=CARTESIAN_POINT('',(-0.0393760042937274,-0.0197767818485,-0.003563531529));
#15796=CARTESIAN_POINT('',(-0.0384862022101706,-0.0236725106364736,-0.00251967414626707));
#15797=CARTESIAN_POINT('',(-0.0370999087760845,-0.0211869274895885,-0.00318568414323665));
#15798=CARTESIAN_POINT('',(-0.0357332402003217,-0.0186914621634017,-0.00385434206216974));
#15799=CARTESIAN_POINT('',(-0.0344330130221634,-0.0161625399944248,-0.00453196471511027));
#15800=CARTESIAN_POINT('',(-0.0384862022686588,-0.0236725106070218,-0.00251967415415977));
#15801=CARTESIAN_POINT('',(-0.0444805635282456,-0.023672508708,-0.002519674663));
#15802=CARTESIAN_POINT('',(-0.0424824431083833,-0.023672508708,-0.002519674663));
#15803=CARTESIAN_POINT('',(-0.0404843226885211,-0.023672508708,-0.002519674663));
#15804=CARTESIAN_POINT('',(-0.0384862022686588,-0.023672508708,-0.002519674663));
#15805=CARTESIAN_POINT('',(-0.0444805635320151,-0.0236725086897196,-0.00251967466791268));
#15806=CARTESIAN_POINT('',(-0.0445000000154798,-0.023562509163137,-0.0025491489365736));
#15807=CARTESIAN_POINT('',(-0.0445000000196407,-0.0236002437613621,-0.00253903798145185));
#15808=CARTESIAN_POINT('',(-0.0444935802521013,-0.0236369200196111,-0.00252921062331408));
#15809=CARTESIAN_POINT('',(-0.0444805635336595,-0.0236725086852255,-0.0025196746691024));
#15810=CARTESIAN_POINT('',(-0.0442000000052978,-1.47752458924516E-11,1.30076225163517E-17));
#15811=CARTESIAN_POINT('',(-0.0444805635188413,-0.0236725086811181,-0.00251967465379378));
#15812=CARTESIAN_POINT('',(-0.0444283437649074,-0.0238152813279393,-0.00248141885068248));
#15813=CARTESIAN_POINT('',(-0.0443085007036546,-0.0238832591538571,-0.00236682348911541));
#15814=CARTESIAN_POINT('',(-0.0441999999998855,-0.0238935321469101,-0.00225812345825258));
#15815=CARTESIAN_POINT('',(-0.0441999965249051,-0.0238935321468263,-0.00225812345938652));
#15816=CARTESIAN_POINT('',(-0.0442000000001921,-0.0238935321468806,-0.00225812345939164));
#15817=CARTESIAN_POINT('',(-0.0442000000001596,-0.0240353842328595,-0.000757165945200664));
#15818=CARTESIAN_POINT('',(-0.0442000000001596,-0.024035384234115,0.000757165905346178));
#15819=CARTESIAN_POINT('',(-0.0442000000001921,-0.0238935321506249,0.00225812341977237));
#15820=CARTESIAN_POINT('',(-0.0441999964978638,-0.0238935321505707,0.00225812341976725));
#15821=CARTESIAN_POINT('',(-0.0444805635187896,-0.0236725086812809,0.00251967465375806));
#15822=CARTESIAN_POINT('',(-0.0444283437698302,-0.0238152813142717,0.00248141885426767));
#15823=CARTESIAN_POINT('',(-0.0443085006931829,-0.0238832591548499,0.00236682347861122));
#15824=CARTESIAN_POINT('',(-0.0441999999998855,-0.0238935321469101,0.00225812345825258));
#15825=CARTESIAN_POINT('',(-0.044480563441692,-0.0236725086989376,0.00251967466542826));
#15826=CARTESIAN_POINT('',(-0.0444805635188046,-0.0236725086812824,0.00251967465374319));
#15827=CARTESIAN_POINT('',(-0.0444935802399076,-0.0236369200084268,0.00252921060989514));
#15828=CARTESIAN_POINT('',(-0.0445000000044733,-0.0236002437676551,0.00253903799540771));
#15829=CARTESIAN_POINT('',(-0.0445000000003707,-0.0235625091618915,0.00254914895254941));
#15830=CARTESIAN_POINT('',(-0.0393760042937274,-0.0197767818485,0.003563531529));
#15831=CARTESIAN_POINT('',(-0.0384862032520929,-0.023672508708,0.002519674663));
#15832=CARTESIAN_POINT('',(-0.0404843233441438,-0.023672508708,0.002519674663));
#15833=CARTESIAN_POINT('',(-0.0424824434361947,-0.023672508708,0.002519674663));
#15834=CARTESIAN_POINT('',(-0.0444805635282456,-0.023672508708,0.002519674663));
#15835=CARTESIAN_POINT('',(-0.0384862032520929,-0.0236725121249481,0.00251967374743256));
#15836=CARTESIAN_POINT('',(-0.0344330130206301,-0.0161625399952047,0.00453196471691751));
#15837=CARTESIAN_POINT('',(-0.0357332404728482,-0.0186914626973602,0.00385434192111219));
#15838=CARTESIAN_POINT('',(-0.0370999095134191,-0.0211869288395885,0.00318568378150523));
#15839=CARTESIAN_POINT('',(-0.0384862032519836,-0.0236725125044133,0.00251967364575413));
#15840=CARTESIAN_POINT('',(-0.044499999875,-0.015881054989,0.004607388395));
#15841=CARTESIAN_POINT('',(-0.0410840028839326,-0.015881054989,0.004607388395));
#15842=CARTESIAN_POINT('',(-0.0376680058928653,-0.015881054989,0.004607388395));
#15843=CARTESIAN_POINT('',(-0.0342520089017979,-0.015881054989,0.004607388395));
#15844=CARTESIAN_POINT('',(-0.0295,0.,0.));
#15845=CARTESIAN_POINT('',(-0.0247416697501165,0.,-9.27109177476128E-16));
#15846=CARTESIAN_POINT('',(-0.0384862032527451,0.00965415486652353,-0.021760834024199));
#15847=CARTESIAN_POINT('',(-0.038494882212823,0.00966554660283219,-0.0217722254619481));
#15848=CARTESIAN_POINT('',(-0.0385033092139225,0.00967786860797711,-0.0217827245711364));
#15849=CARTESIAN_POINT('',(-0.0385114728776262,0.00969116769071119,-0.0217922854079731));
#15850=CARTESIAN_POINT('',(-0.0385114732742117,0.00969116834084262,-0.0217922858702222));
#15851=CARTESIAN_POINT('',(-0.0385114736704593,0.0140270890746655,-0.019288941705194));
#15852=CARTESIAN_POINT('',(-0.0385114736704593,0.012674860590309,-0.020272294223402));
#15853=CARTESIAN_POINT('',(-0.0385114736704593,0.0112188914949441,-0.0211128983725261));
#15854=CARTESIAN_POINT('',(-0.0385114736704593,0.00969116899111081,-0.0217922863325698));
#15855=CARTESIAN_POINT('',(-0.0385114728778453,0.0140270889245788,-0.0192889401165226));
#15856=CARTESIAN_POINT('',(-0.0385114728777164,0.0140270889245852,-0.0192889401165866));
#15857=CARTESIAN_POINT('',(-0.0385033092139972,0.0140254585383594,-0.0192726423546479));
#15858=CARTESIAN_POINT('',(-0.0384948822128803,0.0140225270456425,-0.0192567216305467));
#15859=CARTESIAN_POINT('',(-0.0384862032527859,0.0140183576393019,-0.0192411603786139));
#15860=CARTESIAN_POINT('',(-0.0361231220777228,0.00770660176395194,-0.0181444388314769));
#15861=CARTESIAN_POINT('',(-0.0364648722135284,0.00787297362658244,-0.0187168829308698));
#15862=CARTESIAN_POINT('',(-0.0370051857100642,0.00845252547520145,-0.019493059608721));
#15863=CARTESIAN_POINT('',(-0.0375391602638124,0.00968559833622874,-0.0199436995216774));
#15864=CARTESIAN_POINT('',(-0.0377837871637064,0.0107243093220201,-0.0198906462410908));
#15865=CARTESIAN_POINT('',(-0.0378106634033261,0.0116810478206927,-0.0193992046145791));
#15866=CARTESIAN_POINT('',(-0.0375458092115704,0.0125508820226309,-0.0183019088978515));
#15867=CARTESIAN_POINT('',(-0.0370936280807999,0.0126082281033858,-0.0172854180292052));
#15868=CARTESIAN_POINT('',(-0.0367610930019189,0.0124258527783243,-0.0167032268933286));
#15869=CARTESIAN_POINT('',(-0.0367610930181501,0.0124258527913459,-0.0167032269172659));
#15870=CARTESIAN_POINT('',(-0.0361231220786324,0.00770660176472532,-0.0181444388312368));
#15871=CARTESIAN_POINT('',(-0.0367610930019189,0.0124258527783243,-0.0167032268933286));
#15872=CARTESIAN_POINT('',(-0.0364268270990884,0.0122425282637756,-0.016118005443108));
#15873=CARTESIAN_POINT('',(-0.0358828098136817,0.0116542707196792,-0.0153834168354138));
#15874=CARTESIAN_POINT('',(-0.0352742106702343,0.0104542679403436,-0.0149560441847424));
#15875=CARTESIAN_POINT('',(-0.034970034410582,0.00942843977547389,-0.0150102461084905));
#15876=CARTESIAN_POINT('',(-0.0349337878900483,0.00847535144861393,-0.0154977244593865));
#15877=CARTESIAN_POINT('',(-0.0351821444489868,0.00782363555287664,-0.0163099017911));
#15878=CARTESIAN_POINT('',(-0.0356144093597047,0.00756137032066298,-0.0172491749161208));
#15879=CARTESIAN_POINT('',(-0.0359478246821774,0.00762126293631469,-0.0178508092217905));
#15880=CARTESIAN_POINT('',(-0.0361231220777228,0.00770660176395194,-0.0181444388314769));
#15881=CARTESIAN_POINT('',(-0.0247416697501165,0.,-9.27109177476128E-16));
#15882=CARTESIAN_POINT('',(-0.038486203260216,0.0236725124984624,-0.002519673636394));
#15883=CARTESIAN_POINT('',(-0.0384948821067245,0.0236880734374344,-0.00251550387707458));
#15884=CARTESIAN_POINT('',(-0.0385033089939486,0.0237033267480975,-0.00251008235773586));
#15885=CARTESIAN_POINT('',(-0.0385114725590369,0.023718256032576,-0.00250334555419547));
#15886=CARTESIAN_POINT('',(-0.0385114731149663,0.0237182570487454,-0.00250334509564679));
#15887=CARTESIAN_POINT('',(-0.0385114736704593,0.,-9.39994586434264E-16));
#15888=CARTESIAN_POINT('',(-0.0385114718743307,0.0237182547802193,0.00250334611931137));
#15889=CARTESIAN_POINT('',(-0.0385114711901184,0.0237182535297626,0.00250334668357001));
#15890=CARTESIAN_POINT('',(-0.0385038414966823,0.0237043005914817,0.0025096427595367));
#15891=CARTESIAN_POINT('',(-0.0384954181831038,0.0236890346032608,0.00251524655040276));
#15892=CARTESIAN_POINT('',(-0.0384862012493829,0.0236725089103646,0.00251967460880542));
#15893=CARTESIAN_POINT('',(-0.0384862012657654,0.0236725088091823,0.00251967463590271));
#15894=CARTESIAN_POINT('',(-0.0384862012074146,0.0236725088385615,0.00251967462801615));
#15895=CARTESIAN_POINT('',(-0.0370999081087009,0.0211869262660569,0.00318568447108093));
#15896=CARTESIAN_POINT('',(-0.0357332398658379,0.0186914615155662,0.00385434223575671));
#15897=CARTESIAN_POINT('',(-0.0344330129923926,0.0161625399365206,0.00453196473062564));
#15898=CARTESIAN_POINT('',(-0.0361231220777228,0.0195668458469756,-0.0023981065151534));
#15899=CARTESIAN_POINT('',(-0.0364648722136017,0.0201457829107077,-0.00254024630548127));
#15900=CARTESIAN_POINT('',(-0.0370051857100481,0.0211077475601334,-0.00242642797910508));
#15901=CARTESIAN_POINT('',(-0.0375391602638148,0.0221145495981621,-0.0015838755607176));
#15902=CARTESIAN_POINT('',(-0.0377837871637081,0.0225879596037126,-0.000657798821766451));
#15903=CARTESIAN_POINT('',(-0.0378106634033168,0.0226407279192869,0.000416481880123052));
#15904=CARTESIAN_POINT('',(-0.0375458092116211,0.022125359054538,0.00171842820318643));
#15905=CARTESIAN_POINT('',(-0.0370936280805749,0.0212737251842116,0.00227633678167192));
#15906=CARTESIAN_POINT('',(-0.0367610930019189,0.0206783452020235,0.00240949073966257));
#15907=CARTESIAN_POINT('',(-0.0367610930181502,0.0206783452308322,0.00240949072780955));
#15908=CARTESIAN_POINT('',(-0.0361231220786325,0.0195668458477632,-0.00239810651169203));
#15909=CARTESIAN_POINT('',(-0.0367610930019189,0.0206783452020235,0.00240949073966257));
#15910=CARTESIAN_POINT('',(-0.03642682709907,0.0200798663083023,0.00254333772243173));
#15911=CARTESIAN_POINT('',(-0.035882809813686,0.019149565135917,0.00240118609225308));
#15912=CARTESIAN_POINT('',(-0.0352742106702333,0.0181794481747533,0.00157563951687282));
#15913=CARTESIAN_POINT('',(-0.0349700344105827,0.0177134743348323,0.000660145306282492));
#15914=CARTESIAN_POINT('',(-0.0349337878900463,0.0176590988069142,-0.000408992572770604));
#15915=CARTESIAN_POINT('',(-0.0351821444489944,0.0180366070604978,-0.00137948376032849));
#15916=CARTESIAN_POINT('',(-0.0356144093596766,0.0187189088315577,-0.00207624867662167));
#15917=CARTESIAN_POINT('',(-0.035947824682238,0.0192698857319822,-0.00232519730293998));
#15918=CARTESIAN_POINT('',(-0.0361231220777228,0.0195668458469756,-0.0023981065151534));
#15919=CARTESIAN_POINT('',(-0.039226004293684,0.0197767818485,0.003563531529));
#15920=CARTESIAN_POINT('',(-0.0442,0.023672508708,0.002519674663));
#15921=CARTESIAN_POINT('',(-0.0422954004219218,0.023672508708,0.002519674663));
#15922=CARTESIAN_POINT('',(-0.0403908008438436,0.023672508708,0.002519674663));
#15923=CARTESIAN_POINT('',(-0.0384862012657654,0.023672508708,0.002519674663));
#15924=CARTESIAN_POINT('',(-0.0247416697501165,0.,-9.27109177476128E-16));
#15925=CARTESIAN_POINT('',(-0.0384862032593478,0.0140183576289848,0.0192411603767344));
#15926=CARTESIAN_POINT('',(-0.0384948822191775,0.0140225270354065,0.0192567216280387));
#15927=CARTESIAN_POINT('',(-0.038503309213364,0.0140254585381575,0.0192726423534367));
#15928=CARTESIAN_POINT('',(-0.0385114728769827,0.0140270889244387,0.01928894011512));
#15929=CARTESIAN_POINT('',(-0.0385114732738496,0.0140270890035019,0.0192889409072152));
#15930=CARTESIAN_POINT('',(-0.0385114736704593,0.00969116897825783,0.0217922863382837));
#15931=CARTESIAN_POINT('',(-0.0385114736704593,0.011218891489756,0.0211128983759107));
#15932=CARTESIAN_POINT('',(-0.0385114736704593,0.0126748605921952,0.0202722942228765));
#15933=CARTESIAN_POINT('',(-0.0385114736704593,0.014027089082578,0.0192889416994381));
#15934=CARTESIAN_POINT('',(-0.0385114720962522,0.00969116641671853,0.0217922844930147));
#15935=CARTESIAN_POINT('',(-0.0385114717024072,0.00969116577635566,0.0217922840319173));
#15936=CARTESIAN_POINT('',(-0.0385033084027854,0.00967786742257547,0.0217827235606114));
#15937=CARTESIAN_POINT('',(-0.038494881794112,0.00966554605324076,0.0217722249123752));
#15938=CARTESIAN_POINT('',(-0.0384862032527165,0.00965415486648457,0.0217608340241601));
#15939=CARTESIAN_POINT('',(-0.0361231220777228,0.0118602440896865,0.015746332315506));
#15940=CARTESIAN_POINT('',(-0.0364648722136085,0.0122728092489834,0.0161766366562693));
#15941=CARTESIAN_POINT('',(-0.0370051857103236,0.0126552220632647,0.0170666316051076));
#15942=CARTESIAN_POINT('',(-0.0375391602633533,0.0124289512728845,0.0183598239629085));
#15943=CARTESIAN_POINT('',(-0.0377837871654629,0.0118636502964869,0.0192328474262822));
#15944=CARTESIAN_POINT('',(-0.0378106633967592,0.0109596800744716,0.0198156864636229));
#15945=CARTESIAN_POINT('',(-0.0375458092464411,0.00957447705560089,0.0200203371759163));
#15946=CARTESIAN_POINT('',(-0.0370936279261474,0.00866549692365674,0.0195617546232574));
#15947=CARTESIAN_POINT('',(-0.036761093001919,0.00825249241403732,0.0191127176213848));
#15948=CARTESIAN_POINT('',(-0.0367610930181502,0.00825249243626566,0.0191127176418733));
#15949=CARTESIAN_POINT('',(-0.0361231220786325,0.0118602440845922,0.0157463323192722));
#15950=CARTESIAN_POINT('',(-0.036761093001919,0.00825249241403732,0.0191127176213848));
#15951=CARTESIAN_POINT('',(-0.036426827099111,0.00783733807984076,0.0186613431873148));
#15952=CARTESIAN_POINT('',(-0.035882809813574,0.00749529443304704,0.0177846029157222));
#15953=CARTESIAN_POINT('',(-0.0352742106704064,0.00772518021396054,0.0165316837164498));
#15954=CARTESIAN_POINT('',(-0.0349700344099314,0.00828503457162375,0.0156703914105354));
#15955=CARTESIAN_POINT('',(-0.0349337878924788,0.00918374736601869,0.0150887318900222));
#15956=CARTESIAN_POINT('',(-0.0351821444399159,0.0102129715007087,0.0149304180205763));
#15957=CARTESIAN_POINT('',(-0.035614409393558,0.0111575385677808,0.015172926274143));
#15958=CARTESIAN_POINT('',(-0.0359478246092337,0.0116486226930708,0.0155256118420533));
#15959=CARTESIAN_POINT('',(-0.0361231220777228,0.0118602440896865,0.015746332315506));
#15960=CARTESIAN_POINT('',(-0.0247416697501165,0.,-9.27109177476128E-16));
#15961=CARTESIAN_POINT('',(-0.0384862032593708,-0.0096541548701199,0.0217608340143427));
#15962=CARTESIAN_POINT('',(-0.0384948821046016,-0.00966554645544961,0.0217722253014528));
#15963=CARTESIAN_POINT('',(-0.0385033089913836,-0.00967786828270555,0.0217827242938166));
#15964=CARTESIAN_POINT('',(-0.0385114725553467,-0.0096911671656983,0.0217922850305355));
#15965=CARTESIAN_POINT('',(-0.0385114731130998,-0.00969116807390871,0.0217922856835205));
#15966=CARTESIAN_POINT('',(-0.0385114736704593,-0.0140270890860421,0.0192889416969189));
#15967=CARTESIAN_POINT('',(-0.0385114736704593,-0.0126748605958359,0.0202722942206002));
#15968=CARTESIAN_POINT('',(-0.0385114736704593,-0.0112188914935475,0.021112898373896));
#15969=CARTESIAN_POINT('',(-0.0385114736704593,-0.00969116898217136,0.0217922863365434));
#15970=CARTESIAN_POINT('',(-0.0385114728767313,-0.0140270889243563,0.0192889401142976));
#15971=CARTESIAN_POINT('',(-0.0385114728763616,-0.0140270889247215,0.0192889401144462));
#15972=CARTESIAN_POINT('',(-0.0385033092129711,-0.014025458538453,0.019272642353242));
#15973=CARTESIAN_POINT('',(-0.0384948822124526,-0.0140225270454405,0.0192567216297753));
#15974=CARTESIAN_POINT('',(-0.0384862032527417,-0.0140183576392802,0.019241160378533));
#15975=CARTESIAN_POINT('',(-0.0361231220777228,-0.00770660175650897,0.0181444388346364));
#15976=CARTESIAN_POINT('',(-0.0364648722136209,-0.00787297366731662,0.0187168829137092));
#15977=CARTESIAN_POINT('',(-0.0370051857103217,-0.00845252549508946,0.0194930596000144));
#15978=CARTESIAN_POINT('',(-0.0375391602633525,-0.00968559832410782,0.019943699526334));
#15979=CARTESIAN_POINT('',(-0.0377837871654679,-0.0107243093096923,0.0198906462517043));
#15980=CARTESIAN_POINT('',(-0.03781066339674,-0.0116810478333493,0.0193992045938186));
#15981=CARTESIAN_POINT('',(-0.0375458092465435,-0.0125508820586186,0.018301908946452));
#15982=CARTESIAN_POINT('',(-0.0370936279256935,-0.0126082279839681,0.0172854177833506));
#15983=CARTESIAN_POINT('',(-0.036761093001919,-0.0124258527881758,0.016703226885998));
#15984=CARTESIAN_POINT('',(-0.0367610930181502,-0.0124258527946297,0.0167032269148224));
#15985=CARTESIAN_POINT('',(-0.0361231220786325,-0.00770660176224433,0.01814443883229));
#15986=CARTESIAN_POINT('',(-0.036761093001919,-0.0124258527881758,0.016703226885998));
#15987=CARTESIAN_POINT('',(-0.0364268270991507,-0.0122425282287825,0.0161180054691239));
#15988=CARTESIAN_POINT('',(-0.0358828098135649,-0.0116542707355394,0.0153834168229345));
#15989=CARTESIAN_POINT('',(-0.0352742106704084,-0.0104542679526858,0.014956044176835));
#15990=CARTESIAN_POINT('',(-0.0349700344099297,-0.00942843976427119,0.015010246114524));
#15991=CARTESIAN_POINT('',(-0.0349337878924834,-0.00847535144396104,0.0154977244663839));
#15992=CARTESIAN_POINT('',(-0.0351821444398992,-0.00782363554441411,0.0163099017780492));
#15993=CARTESIAN_POINT('',(-0.0356144093936205,-0.00756137031897134,0.0172491749807311));
#15994=CARTESIAN_POINT('',(-0.035947824609099,-0.00762126291761072,0.0178508090922294));
#15995=CARTESIAN_POINT('',(-0.0361231220777228,-0.00770660175650897,0.0181444388346364));
#15996=CARTESIAN_POINT('',(-0.0247416697501165,0.,-9.27109177476128E-16));
#15997=CARTESIAN_POINT('',(-0.0384862032581869,-0.0236725124992893,0.00251967363853479));
#15998=CARTESIAN_POINT('',(-0.0384948822179627,-0.0236880736413488,0.0025155038247818));
#15999=CARTESIAN_POINT('',(-0.0385033092129298,-0.0237033271444534,0.00251008221703059));
#16000=CARTESIAN_POINT('',(-0.038511472876488,-0.0237182566131209,0.00250334529222524));
#16001=CARTESIAN_POINT('',(-0.0385114732736763,-0.02371825733873,0.00250334496717108));
#16002=CARTESIAN_POINT('',(-0.0385114736704593,-0.0237182580651627,-0.00250334463653795));
#16003=CARTESIAN_POINT('',(-0.0385114736704593,-0.0238937520861163,-0.000840604150423141));
#16004=CARTESIAN_POINT('',(-0.0385114736704593,-0.0238937520859224,0.00084060415593165));
#16005=CARTESIAN_POINT('',(-0.0385114736704593,-0.0237182580645854,0.00250334464200599));
#16006=CARTESIAN_POINT('',(-0.0385114728771051,-0.0237182566137558,-0.0025033452919386));
#16007=CARTESIAN_POINT('',(-0.0385114728771736,-0.0237182566135553,-0.00250334529157726));
#16008=CARTESIAN_POINT('',(-0.0385033092137543,-0.0237033271451377,-0.00251008221630948));
#16009=CARTESIAN_POINT('',(-0.0384948822126514,-0.0236880736481024,-0.00251550383130167));
#16010=CARTESIAN_POINT('',(-0.038486203252893,-0.0236725125060437,-0.00251967364531955));
#16011=CARTESIAN_POINT('',(-0.0361231220777228,-0.01956684584839,0.00239810650361112));
#16012=CARTESIAN_POINT('',(-0.0364648722135854,-0.0201457829121783,0.00254024629359048));
#16013=CARTESIAN_POINT('',(-0.0370051857097729,-0.0211077475580505,0.00242642799183558));
#16014=CARTESIAN_POINT('',(-0.0375391602642789,-0.0221145495984874,0.00158387556971517));
#16015=CARTESIAN_POINT('',(-0.0377837871619422,-0.0225879596001145,0.000657798828281427));
#16016=CARTESIAN_POINT('',(-0.0378106634099163,-0.0226407279317958,-0.000416481859769928));
#16017=CARTESIAN_POINT('',(-0.0375458091765785,-0.0221253589897648,-0.00171842825316367));
#16018=CARTESIAN_POINT('',(-0.0370936282359893,-0.0212737254634035,-0.00227633671071596));
#16019=CARTESIAN_POINT('',(-0.0367610930019189,-0.0206783452030119,-0.00240949073118205));
#16020=CARTESIAN_POINT('',(-0.0367610930181502,-0.0206783452311617,-0.00240949072498272));
#16021=CARTESIAN_POINT('',(-0.0361231220786325,-0.0195668458482347,0.00239810650784461));
#16022=CARTESIAN_POINT('',(-0.0367610930019189,-0.0206783452030119,-0.00240949073118205));
#16023=CARTESIAN_POINT('',(-0.0364268270992314,-0.0200798663096345,-0.00254333771413222));
#16024=CARTESIAN_POINT('',(-0.0358828098134473,-0.0191495651337216,-0.00240118610461706));
#16025=CARTESIAN_POINT('',(-0.0352742106705773,-0.0181794481741787,-0.00157563953253189));
#16026=CARTESIAN_POINT('',(-0.0349700344092999,-0.0177134743335201,-0.000660145294956659));
#16027=CARTESIAN_POINT('',(-0.0349337878948338,-0.0176590988142993,0.000408992586881077));
#16028=CARTESIAN_POINT('',(-0.035182144431127,-0.0180366070313037,0.00137948373618994));
#16029=CARTESIAN_POINT('',(-0.0356144094263585,-0.0187189089456695,0.0020762486950472));
#16030=CARTESIAN_POINT('',(-0.0359478245385584,-0.0192698854899551,0.00232519723181412));
#16031=CARTESIAN_POINT('',(-0.0361231220777228,-0.01956684584839,0.00239810650361112));
#16032=CARTESIAN_POINT('',(-0.0247416697501165,0.,-9.27109177476128E-16));
#16033=CARTESIAN_POINT('',(-0.038486203252956,-0.0140183576393836,-0.0192411603789189));
#16034=CARTESIAN_POINT('',(-0.0384948822124652,-0.0140225270454284,-0.019256721629813));
#16035=CARTESIAN_POINT('',(-0.0385033092130316,-0.0140254585380152,-0.0192726423528298));
#16036=CARTESIAN_POINT('',(-0.0385114728762402,-0.0140270889242906,-0.0192889401136396));
#16037=CARTESIAN_POINT('',(-0.0385114732734456,-0.0140270890073774,-0.0192889409035327));
#16038=CARTESIAN_POINT('',(-0.0385114736704593,-0.0096911689871971,-0.0217922863343103));
#16039=CARTESIAN_POINT('',(-0.0385114736704593,-0.0112188914984166,-0.0211128983713105));
#16040=CARTESIAN_POINT('',(-0.0385114736704593,-0.0126748606005111,-0.020272294217679));
#16041=CARTESIAN_POINT('',(-0.0385114736704593,-0.0140270890904905,-0.0192889416936859));
#16042=CARTESIAN_POINT('',(-0.0385114728774152,-0.00969116769002384,-0.0217922854074788));
#16043=CARTESIAN_POINT('',(-0.0385114728772461,-0.00969116769009225,-0.021792285407528));
#16044=CARTESIAN_POINT('',(-0.038503309213807,-0.00967786860783287,-0.0217827245709812));
#16045=CARTESIAN_POINT('',(-0.038494882212988,-0.00966554660309386,-0.0217722254621444));
#16046=CARTESIAN_POINT('',(-0.0384862032532088,-0.00965415486713206,-0.0217608340248075));
#16047=CARTESIAN_POINT('',(-0.0361231220777228,-0.0118602440803994,-0.015746332322503));
#16048=CARTESIAN_POINT('',(-0.036464872213627,-0.0122728092814391,-0.0161766366319176));
#16049=CARTESIAN_POINT('',(-0.0370051857100415,-0.0126552220776526,-0.01706663159448));
#16050=CARTESIAN_POINT('',(-0.0375391602638173,-0.0124289512594974,-0.0183598239733153));
#16051=CARTESIAN_POINT('',(-0.0377837871637024,-0.0118636502776772,-0.0192328474337847));
#16052=CARTESIAN_POINT('',(-0.0378106634033369,-0.0109596800952083,-0.019815686465));
#16053=CARTESIAN_POINT('',(-0.0375458092115145,-0.00957447702796622,-0.0200203371222328));
#16054=CARTESIAN_POINT('',(-0.037093628081047,-0.0086654970730925,-0.0195617548508813));
#16055=CARTESIAN_POINT('',(-0.0367610930019189,-0.00825249242187748,-0.0191127176180015));
#16056=CARTESIAN_POINT('',(-0.0367610930181501,-0.00825249243887905,-0.0191127176407455));
#16057=CARTESIAN_POINT('',(-0.0361231220786324,-0.0118602440814965,-0.0157463323216046));
#16058=CARTESIAN_POINT('',(-0.0367610930019189,-0.00825249242187748,-0.0191127176180015));
#16059=CARTESIAN_POINT('',(-0.0364268270990136,-0.00783733803641719,-0.018661343205973));
#16060=CARTESIAN_POINT('',(-0.0358828098136985,-0.00749529441315766,-0.017784602925027));
#16061=CARTESIAN_POINT('',(-0.0352742106702312,-0.00772518023068291,-0.016531683708193));
#16062=CARTESIAN_POINT('',(-0.0349700344105825,-0.00828503455619132,-0.0156703914194872));
#16063=CARTESIAN_POINT('',(-0.0349337878900495,-0.00918374735540738,-0.0150887318920016));
#16064=CARTESIAN_POINT('',(-0.0351821444489816,-0.0102129715049413,-0.0149304180362941));
#16065=CARTESIAN_POINT('',(-0.0356144093597242,-0.0111575385083902,-0.0151729262453948));
#16066=CARTESIAN_POINT('',(-0.0359478246821352,-0.0116486227929187,-0.0155256119249019));
#16067=CARTESIAN_POINT('',(-0.0361231220777228,-0.0118602440803994,-0.015746332322503));
#16068=CARTESIAN_POINT('',(-0.0345,0.01,-0.017320508076));
#16069=CARTESIAN_POINT('',(-0.0370209006250624,0.0120502416069907,-0.0166731987585513));
#16070=CARTESIAN_POINT('',(-0.0369382714896785,0.0120102199855764,-0.016546437114325));
#16071=CARTESIAN_POINT('',(-0.0368384384344523,0.0119515655400817,-0.0164007187842568));
#16072=CARTESIAN_POINT('',(-0.0367214014593838,0.0118619547328937,-0.0162455082750017));
#16073=CARTESIAN_POINT('',(-0.0367214015196458,0.0118619576137187,-0.0162455065980668));
#16074=CARTESIAN_POINT('',(-0.037020900637956,0.0120502416154678,-0.0166731987850141));
#16075=CARTESIAN_POINT('',(-0.0367214013837088,0.0118619546747634,-0.0162455081743171));
#16076=CARTESIAN_POINT('',(-0.0367099515900364,0.0118531879996303,-0.0162303238457225));
#16077=CARTESIAN_POINT('',(-0.036670659517387,0.0118230656559306,-0.0161785319977277));
#16078=CARTESIAN_POINT('',(-0.036581771380862,0.0117478247863627,-0.0160659297891458));
#16079=CARTESIAN_POINT('',(-0.0364479212855715,0.0116231137497877,-0.0159049183945184));
#16080=CARTESIAN_POINT('',(-0.0363510261528849,0.0115197512730407,-0.0157983752279772));
#16081=CARTESIAN_POINT('',(-0.0362580223097223,0.011416510277242,-0.0156993012950561));
#16082=CARTESIAN_POINT('',(-0.0361233029084067,0.0112500261099531,-0.0155680128195404));
#16083=CARTESIAN_POINT('',(-0.0360272431295662,0.0111204292982917,-0.0154825522935279));
#16084=CARTESIAN_POINT('',(-0.0359036001279196,0.0109384060206373,-0.0153831278620205));
#16085=CARTESIAN_POINT('',(-0.0357761189415156,0.0107336230397511,-0.0152928731905691));
#16086=CARTESIAN_POINT('',(-0.0355839197980515,0.0103729533951222,-0.0151906973984985));
#16087=CARTESIAN_POINT('',(-0.0354386203310907,0.0100314764218445,-0.0151589427817623));
#16088=CARTESIAN_POINT('',(-0.0352978141924959,0.00958374411058124,-0.015196844402381));
#16089=CARTESIAN_POINT('',(-0.0352031355092724,0.00907592308678395,-0.0153447793638773));
#16090=CARTESIAN_POINT('',(-0.0352317165648889,0.00855567326232278,-0.0156889692127796));
#16091=CARTESIAN_POINT('',(-0.0353617578831115,0.00822759558954855,-0.0160791452283518));
#16092=CARTESIAN_POINT('',(-0.0355339605712917,0.00801012797788875,-0.0164765050992009));
#16093=CARTESIAN_POINT('',(-0.0356900432181194,0.007905672438546,-0.0167851632512574));
#16094=CARTESIAN_POINT('',(-0.0358977301719722,0.00785023330030782,-0.0171562408689187));
#16095=CARTESIAN_POINT('',(-0.0360269463636352,0.0078480581130412,-0.0173712503755659));
#16096=CARTESIAN_POINT('',(-0.0361556833141385,0.00786282854433334,-0.0175781112950878));
#16097=CARTESIAN_POINT('',(-0.0362517163778589,0.00788664178093596,-0.0177265531559471));
#16098=CARTESIAN_POINT('',(-0.036337936705,0.00791668749714797,-0.0178562799663004));
#16099=CARTESIAN_POINT('',(-0.0363829297000817,0.00793596622153825,-0.0179223922516189));
#16100=CARTESIAN_POINT('',(-0.0363829296981285,0.00793596622218309,-0.0179223922530286));
#16101=CARTESIAN_POINT('',(-0.0363829297000817,0.00793596622153825,-0.0179223922516189));
#16102=CARTESIAN_POINT('',(-0.0364957535948001,0.00798408903520211,-0.018087419206871));
#16103=CARTESIAN_POINT('',(-0.0366085774895185,0.0080520952982146,-0.0182466381820913));
#16104=CARTESIAN_POINT('',(-0.0367214013842369,0.00813804543863112,-0.018395508174088));
#16105=CARTESIAN_POINT('',(-0.0367214014146636,0.00813803958835936,-0.0183955115197437));
#16106=CARTESIAN_POINT('',(-0.0367214014593838,0.00813804549645274,-0.0183955082742379));
#16107=CARTESIAN_POINT('',(-0.0368094504194448,0.00820546129493275,-0.0185122758337192));
#16108=CARTESIAN_POINT('',(-0.0369082047152564,0.00829303764241074,-0.0186381460995257));
#16109=CARTESIAN_POINT('',(-0.0370729160017973,0.00846997363213822,-0.0188345415471286));
#16110=CARTESIAN_POINT('',(-0.0372054092113008,0.00862943751340597,-0.0189847044560509));
#16111=CARTESIAN_POINT('',(-0.0374076931229372,0.00892027604482932,-0.0191924775219796));
#16112=CARTESIAN_POINT('',(-0.0375741836148829,0.00921705183109107,-0.0193348076621258));
#16113=CARTESIAN_POINT('',(-0.0377619138370971,0.00963575500054258,-0.0194525344836347));
#16114=CARTESIAN_POINT('',(-0.037887321460399,0.0100037924316706,-0.019482814463935));
#16115=CARTESIAN_POINT('',(-0.0379943792822189,0.0104428423755329,-0.0194389153257726));
#16116=CARTESIAN_POINT('',(-0.0380653382950535,0.0109633665553823,-0.0192778414401676));
#16117=CARTESIAN_POINT('',(-0.0380390815294276,0.0114596043683887,-0.0189394219781793));
#16118=CARTESIAN_POINT('',(-0.0379290145681861,0.0117932120462459,-0.0185312244554124));
#16119=CARTESIAN_POINT('',(-0.0377914075938047,0.0119983498352797,-0.0181451935333134));
#16120=CARTESIAN_POINT('',(-0.0376479878673514,0.0121064916090377,-0.0178074586875425));
#16121=CARTESIAN_POINT('',(-0.0374402992000161,0.0121604331951634,-0.0173824655935396));
#16122=CARTESIAN_POINT('',(-0.0372619157421967,0.0121430293601063,-0.0170606765916029));
#16123=CARTESIAN_POINT('',(-0.0371044376010776,0.0120907029448459,-0.0168013531294359));
#16124=CARTESIAN_POINT('',(-0.0370209006250624,0.0120502416069907,-0.0166731987585513));
#16125=CARTESIAN_POINT('',(-0.0345,0.02,0.));
#16126=CARTESIAN_POINT('',(-0.0370209006250623,0.0204645344905706,0.0020992159743748));
#16127=CARTESIAN_POINT('',(-0.0369382705057487,0.0203347433302252,0.00212793739765262));
#16128=CARTESIAN_POINT('',(-0.0368384374592961,0.0201792202695511,0.00214999998707071));
#16129=CARTESIAN_POINT('',(-0.0367214014857045,0.0200000001551052,0.00214999999999999));
#16130=CARTESIAN_POINT('',(-0.0367214015239592,0.020000000186686,0.00215000333369359));
#16131=CARTESIAN_POINT('',(-0.037020900637956,0.020464534518328,0.00209921596804585));
#16132=CARTESIAN_POINT('',(-0.0367214013837088,0.02,0.00215));
#16133=CARTESIAN_POINT('',(-0.0367099554160874,0.0199824725070566,0.00215));
#16134=CARTESIAN_POINT('',(-0.0366706659873135,0.019922562352937,0.00214980948896017));
#16135=CARTESIAN_POINT('',(-0.0365817765395305,0.0197874235171236,0.00214095075204637));
#16136=CARTESIAN_POINT('',(-0.0364479182980935,0.0195856157382105,0.0021134520269105));
#16137=CARTESIAN_POINT('',(-0.036351027246845,0.0194416715666082,0.00207720991389666));
#16138=CARTESIAN_POINT('',(-0.0362580217381144,0.0193042480471294,0.00203733687752704));
#16139=CARTESIAN_POINT('',(-0.0361233041008781,0.0191073093362409,0.0019588033066822));
#16140=CARTESIAN_POINT('',(-0.0360272389301111,0.0189684923098096,0.00188929327715607));
#16141=CARTESIAN_POINT('',(-0.0359036157332686,0.018791404597601,0.00178139164708577));
#16142=CARTESIAN_POINT('',(-0.0357760361093145,0.0186107110588261,0.00164905760404357));
#16143=CARTESIAN_POINT('',(-0.0355845872611166,0.0183429504643919,0.00138866627066025));
#16144=CARTESIAN_POINT('',(-0.0354400098074399,0.0181456531209698,0.00111147707696002));
#16145=CARTESIAN_POINT('',(-0.03529745132709,0.0179522358157694,0.000700457148034725));
#16146=CARTESIAN_POINT('',(-0.0352033477140133,0.0178272165772559,0.00018810871030881));
#16147=CARTESIAN_POINT('',(-0.0352316825933261,0.0178648366965161,-0.000435137210319832));
#16148=CARTESIAN_POINT('',(-0.0353617642821612,0.0180387546663257,-0.000914250187794874));
#16149=CARTESIAN_POINT('',(-0.0355339588539763,0.018274133653175,-0.00130128242879006));
#16150=CARTESIAN_POINT('',(-0.0356900436883312,0.0184892146354852,-0.0015460673103522));
#16151=CARTESIAN_POINT('',(-0.0358977301136426,0.0187828569969928,-0.00177961911331699));
#16152=CARTESIAN_POINT('',(-0.0360269463745861,0.018967973191657,-0.00188900746452468));
#16153=CARTESIAN_POINT('',(-0.0361556833111519,0.0191545051998489,-0.00197964638969947));
#16154=CARTESIAN_POINT('',(-0.0362517163788544,0.0192949662460383,-0.00203324444307963));
#16155=CARTESIAN_POINT('',(-0.0363379367050664,0.0194223358162089,-0.00207208749676157));
#16156=CARTESIAN_POINT('',(-0.0363829297000817,0.0194892300968965,-0.00208844777432515));
#16157=CARTESIAN_POINT('',(-0.0363829296981285,0.0194892300988016,-0.00208844777506104));
#16158=CARTESIAN_POINT('',(-0.0363829297000817,0.0194892300968965,-0.00208844777432515));
#16159=CARTESIAN_POINT('',(-0.0364957535948001,0.0196562090392939,-0.00212928567282428));
#16160=CARTESIAN_POINT('',(-0.0366085774895185,0.0198280998481142,-0.00215000000905572));
#16161=CARTESIAN_POINT('',(-0.0367214013842369,0.0200000001132622,-0.00215));
#16162=CARTESIAN_POINT('',(-0.0367214014146637,0.0200000000856372,-0.00215000673932028));
#16163=CARTESIAN_POINT('',(-0.0367214014593838,0.0200000002289055,-0.00214999999999999));
#16164=CARTESIAN_POINT('',(-0.0368094504193861,0.0201348318009116,-0.00214999998564479));
#16165=CARTESIAN_POINT('',(-0.0369082047152033,0.0202876268224398,-0.0021370917768919));
#16166=CARTESIAN_POINT('',(-0.0370729160019053,0.0205461782643721,-0.00208205843868064));
#16167=CARTESIAN_POINT('',(-0.0372054092112306,0.020755955098582,-0.00201904012105865));
#16168=CARTESIAN_POINT('',(-0.0374076931230288,0.0210813111179108,-0.00187105309729519));
#16169=CARTESIAN_POINT('',(-0.0375741836148664,0.0213529605279511,-0.00168520279732712));
#16170=CARTESIAN_POINT('',(-0.0377619138370714,0.0216642665308313,-0.00138145862673429));
#16171=CARTESIAN_POINT('',(-0.0378873214604069,0.0218745084786354,-0.00107786885189048));
#16172=CARTESIAN_POINT('',(-0.0379943792822128,0.0220560156817041,-0.000675690877956248));
#16173=CARTESIAN_POINT('',(-0.0380653382950567,0.0221767836948601,-0.000144366772012301));
#16174=CARTESIAN_POINT('',(-0.0380390815294298,0.0221318227501571,0.000454597511353307));
#16175=CARTESIAN_POINT('',(-0.0379290145681815,0.0219451171645996,0.000947608996721526));
#16176=CARTESIAN_POINT('',(-0.0377914075938135,0.0217133734739575,0.00131827899434535));
#16177=CARTESIAN_POINT('',(-0.0376479878673206,0.0214749574045774,0.00158079994060532));
#16178=CARTESIAN_POINT('',(-0.0374402992000349,0.021133873381878,0.00184001127146523));
#16179=CARTESIAN_POINT('',(-0.0372619157421523,0.0208464940139058,0.00198583360922132));
#16180=CARTESIAN_POINT('',(-0.0371044376010594,0.020595750100268,0.00207017933538683));
#16181=CARTESIAN_POINT('',(-0.0370209006250624,0.0204645344905706,0.0020992159743748));
#16182=CARTESIAN_POINT('',(-0.0345,0.01,0.017320508076));
#16183=CARTESIAN_POINT('',(-0.0367214013837088,0.00813804543876341,0.0183955081743171));
#16184=CARTESIAN_POINT('',(-0.036709951590334,0.0081292787622546,0.0183803238470431));
#16185=CARTESIAN_POINT('',(-0.0366706595167616,0.00809948687850548,0.0183283412064286));
#16186=CARTESIAN_POINT('',(-0.0365817713831444,0.00803959093910059,0.0182068796030137));
#16187=CARTESIAN_POINT('',(-0.036447921275181,0.00796250650255608,0.0180183709572674));
#16188=CARTESIAN_POINT('',(-0.0363510262349874,0.00792191862466955,0.0178755850102194));
#16189=CARTESIAN_POINT('',(-0.0362580220091763,0.00788773869361132,0.0177366380281489));
#16190=CARTESIAN_POINT('',(-0.0361233040284883,0.00785728120029016,0.0175268168356142));
#16191=CARTESIAN_POINT('',(-0.0360272389494077,0.00784807019341441,0.0173718428777057));
#16192=CARTESIAN_POINT('',(-0.035903615728472,0.00785297187537506,0.017164529571628));
#16193=CARTESIAN_POINT('',(-0.0357760361120757,0.00787722975389325,0.0169418773656573));
#16194=CARTESIAN_POINT('',(-0.0355845872602483,0.00796885496384819,0.0165797942171482));
#16195=CARTESIAN_POINT('',(-0.0354400098076728,0.00811025917636308,0.0162703351102285));
#16196=CARTESIAN_POINT('',(-0.0352974513270266,0.00836950422341811,0.0158973208455679));
#16197=CARTESIAN_POINT('',(-0.0352033477140518,0.00875070136687583,0.0155328767903185));
#16198=CARTESIAN_POINT('',(-0.0352316825933103,0.0093092582264464,0.0152538338089243));
#16199=CARTESIAN_POINT('',(-0.0353617642821792,0.00981114122123326,0.015164894700211));
#16200=CARTESIAN_POINT('',(-0.0355339588539459,0.0102640104672661,0.0151752227618142));
#16201=CARTESIAN_POINT('',(-0.0356900436884346,0.0105835408845637,0.0152390959156379));
#16202=CARTESIAN_POINT('',(-0.0358977301136305,0.0109326238595562,0.015376621758773));
#16203=CARTESIAN_POINT('',(-0.0360269463745872,0.0111199150479226,0.0154822429103865));
#16204=CARTESIAN_POINT('',(-0.0361556833111771,0.0112916766638192,0.015598464905532));
#16205=CARTESIAN_POINT('',(-0.0362517163787524,0.0114083244625806,0.0156933087129476));
#16206=CARTESIAN_POINT('',(-0.0363379367050222,0.0115056483189857,0.0157841924695875));
#16207=CARTESIAN_POINT('',(-0.0363829297000817,0.0115532638753583,0.0158339444772937));
#16208=CARTESIAN_POINT('',(-0.0363829296981285,0.0115532638766184,0.0158339444786343));
#16209=CARTESIAN_POINT('',(-0.0367214015132256,0.0081380426038155,0.0183955099315374));
#16210=CARTESIAN_POINT('',(-0.0363829297000817,0.0115532638753583,0.0158339444772937));
#16211=CARTESIAN_POINT('',(-0.0364957535948001,0.0116721200040918,0.0159581335340468));
#16212=CARTESIAN_POINT('',(-0.0366085774895185,0.0117760045498996,0.0160966381730355));
#16213=CARTESIAN_POINT('',(-0.0367214013842369,0.0118619546746311,0.016245508174088));
#16214=CARTESIAN_POINT('',(-0.036721401387368,0.0118619604980822,0.0162455047799774));
#16215=CARTESIAN_POINT('',(-0.0367214014593838,0.0118619547324527,0.016245508274238));
#16216=CARTESIAN_POINT('',(-0.0368094504192976,0.0119293705059561,0.0163622758478791));
#16217=CARTESIAN_POINT('',(-0.036908204704608,0.0119945891381311,0.0165010543259075));
#16218=CARTESIAN_POINT('',(-0.0370729160195937,0.0120762047020714,0.0167524831030568));
#16219=CARTESIAN_POINT('',(-0.0372054091160399,0.0121265172076173,0.0169656643651337));
#16220=CARTESIAN_POINT('',(-0.0374076938913033,0.012161038121922,0.0173214241803676));
#16221=CARTESIAN_POINT('',(-0.0375741808104541,0.0121358975638703,0.0176496057587877));
#16222=CARTESIAN_POINT('',(-0.037761924286446,0.012028553013407,0.0180710725252609));
#16223=CARTESIAN_POINT('',(-0.0378872824673064,0.0118705612476647,0.0184049580447914));
#16224=CARTESIAN_POINT('',(-0.0379945248052401,0.0116137510202535,0.0187631780484681));
#16225=CARTESIAN_POINT('',(-0.0380645656555082,0.0112103498256101,0.0191337210208826));
#16226=CARTESIAN_POINT('',(-0.0380387434788214,0.0105616359467533,0.0194571705170615));
#16227=CARTESIAN_POINT('',(-0.0378458600825369,0.00984779301411321,0.0194914490882087));
#16228=CARTESIAN_POINT('',(-0.0376442920894866,0.00936086686795073,0.0193855797151924));
#16229=CARTESIAN_POINT('',(-0.0373865925798895,0.00887009516448303,0.0191803803526782));
#16230=CARTESIAN_POINT('',(-0.0371879791841231,0.00859580643238259,0.0189706556630093));
#16231=CARTESIAN_POINT('',(-0.0370209006250624,0.00841429288357993,0.0187724147329261));
#16232=CARTESIAN_POINT('',(-0.037020900637956,0.0084142929028602,0.0187724147537266));
#16233=CARTESIAN_POINT('',(-0.0370209006250624,0.00841429288357992,0.0187724147329261));
#16234=CARTESIAN_POINT('',(-0.0369382714896786,0.00832452489015545,0.0186743741699733));
#16235=CARTESIAN_POINT('',(-0.0368384384344524,0.00822765633725887,0.0185507187651021));
#16236=CARTESIAN_POINT('',(-0.0367214014593838,0.00813804549689372,0.0183955082750017));
#16237=CARTESIAN_POINT('',(-0.0345,-0.01,0.017320508076));
#16238=CARTESIAN_POINT('',(-0.0367214013837088,-0.0118619546747634,0.0162455081743171));
#16239=CARTESIAN_POINT('',(-0.0367099515900164,-0.011853187999615,0.0162303238456961));
#16240=CARTESIAN_POINT('',(-0.0366706595162203,-0.0118230656539648,0.0161785319969529));
#16241=CARTESIAN_POINT('',(-0.0365817713827235,-0.0117478247895692,0.0160659297903309));
#16242=CARTESIAN_POINT('',(-0.0364479212753901,-0.0116231137323535,0.01590491838796));
#16243=CARTESIAN_POINT('',(-0.0363510262352104,-0.0115197514139159,0.0157983752810768));
#16244=CARTESIAN_POINT('',(-0.0362580220090889,-0.0114165097628226,0.015699301101133));
#16245=CARTESIAN_POINT('',(-0.0361233040286148,-0.0112500280267554,0.0155680135421333));
#16246=CARTESIAN_POINT('',(-0.0360272389493788,-0.0111204221455142,0.0154825495970883));
#16247=CARTESIAN_POINT('',(-0.0359036157284611,-0.0109384327149448,0.0153831379251861));
#16248=CARTESIAN_POINT('',(-0.0357760361120856,-0.0107334813091317,0.0152928197612594));
#16249=CARTESIAN_POINT('',(-0.0355845872602139,-0.0103740954991592,0.0151911279464576));
#16250=CARTESIAN_POINT('',(-0.0354400098076825,-0.0100353939449807,0.0151588580332771));
#16251=CARTESIAN_POINT('',(-0.0352974513270221,-0.00958273159223996,0.015196863697529));
#16252=CARTESIAN_POINT('',(-0.0352033477140545,-0.00907651521044848,0.0153447680800186));
#16253=CARTESIAN_POINT('',(-0.0352316825933093,-0.00855557847003619,0.0156889710191991));
#16254=CARTESIAN_POINT('',(-0.0353617642821804,-0.00822761344513396,0.0160791448880825));
#16255=CARTESIAN_POINT('',(-0.0355339588539356,-0.00801012318586718,0.016476505190529));
#16256=CARTESIAN_POINT('',(-0.0356900436884747,-0.00790567375104684,0.0167851632262147));
#16257=CARTESIAN_POINT('',(-0.0358977301136069,-0.00785023313742566,0.0171562408720358));
#16258=CARTESIAN_POINT('',(-0.0360269463746216,-0.00784805814372892,0.0173712503749636));
#16259=CARTESIAN_POINT('',(-0.0361556833111774,-0.0078628285360704,0.0175781112952451));
#16260=CARTESIAN_POINT('',(-0.0362517163787167,-0.00788664178329998,0.0177265531559201));
#16261=CARTESIAN_POINT('',(-0.0363379367050056,-0.00791668749715034,0.0178562799663085));
#16262=CARTESIAN_POINT('',(-0.0363829297000817,-0.00793596622153825,0.0179223922516189));
#16263=CARTESIAN_POINT('',(-0.0363829296981285,-0.00793596622218309,0.0179223922530286));
#16264=CARTESIAN_POINT('',(-0.0367214015132256,-0.0118619576141813,0.0162455065977611));
#16265=CARTESIAN_POINT('',(-0.0363829297000817,-0.00793596622153825,0.0179223922516189));
#16266=CARTESIAN_POINT('',(-0.0364957535948001,-0.00798408903520211,0.018087419206871));
#16267=CARTESIAN_POINT('',(-0.0366085774895185,-0.0080520952982146,0.0182466381820913));
#16268=CARTESIAN_POINT('',(-0.0367214013842369,-0.00813804543863112,0.018395508174088));
#16269=CARTESIAN_POINT('',(-0.036721401387368,-0.00813803958757096,0.0183955115202174));
#16270=CARTESIAN_POINT('',(-0.0367214014593838,-0.00813804549645275,0.0183955082742379));
#16271=CARTESIAN_POINT('',(-0.0368094504194815,-0.00820546129496087,0.0185122758337679));
#16272=CARTESIAN_POINT('',(-0.0369082049132582,-0.00829303830385063,0.0186381461090242));
#16273=CARTESIAN_POINT('',(-0.037072915671782,-0.00846997252972903,0.0188345415312814));
#16274=CARTESIAN_POINT('',(-0.0372054109935089,-0.00862944346656265,0.0189847045417791));
#16275=CARTESIAN_POINT('',(-0.0374076787331404,-0.00892022797846519,0.019192476829662));
#16276=CARTESIAN_POINT('',(-0.0375742361574633,-0.00921722733948676,0.0193348101900589));
#16277=CARTESIAN_POINT('',(-0.0377617180565947,-0.00963510103336886,0.0194525250642369));
#16278=CARTESIAN_POINT('',(-0.0378881050762795,-0.0100063292794282,0.0194828665958168));
#16279=CARTESIAN_POINT('',(-0.0379944159747534,-0.0104434483789157,0.0194386388515495));
#16280=CARTESIAN_POINT('',(-0.0380653168371592,-0.0109630121629511,0.0192780031230472));
#16281=CARTESIAN_POINT('',(-0.0380390849645502,-0.0114596611018754,0.0189393960949147));
#16282=CARTESIAN_POINT('',(-0.0379290139211953,-0.0117932013607519,0.0185312293304056));
#16283=CARTESIAN_POINT('',(-0.0377914077671703,-0.0119983526985195,0.0181451922270323));
#16284=CARTESIAN_POINT('',(-0.0376479878208797,-0.0121064908415727,0.0178074590376732));
#16285=CARTESIAN_POINT('',(-0.0374402992125289,-0.0121604334017888,0.0173824654992756));
#16286=CARTESIAN_POINT('',(-0.0372619157386173,-0.0121430293010699,0.0170606766185285));
#16287=CARTESIAN_POINT('',(-0.0371044376010756,-0.012090702944845,0.0168013531294328));
#16288=CARTESIAN_POINT('',(-0.0370209006250624,-0.0120502416069907,0.0166731987585513));
#16289=CARTESIAN_POINT('',(-0.037020900637956,-0.0120502416154678,0.0166731987850141));
#16290=CARTESIAN_POINT('',(-0.0370209006250624,-0.0120502416069907,0.0166731987585513));
#16291=CARTESIAN_POINT('',(-0.0369382714896785,-0.0120102199855764,0.016546437114325));
#16292=CARTESIAN_POINT('',(-0.0368384384344523,-0.0119515655400817,0.0164007187842568));
#16293=CARTESIAN_POINT('',(-0.0367214014593838,-0.0118619547328937,0.0162455082750017));
#16294=CARTESIAN_POINT('',(-0.0345,-0.02,0.));
#16295=CARTESIAN_POINT('',(-0.0367214013837088,-0.0200000001135268,-0.00215));
#16296=CARTESIAN_POINT('',(-0.0367099515894606,-0.0199824667607752,-0.00215000000092581));
#16297=CARTESIAN_POINT('',(-0.0366706595152771,-0.0199225525306318,-0.00214980920870223));
#16298=CARTESIAN_POINT('',(-0.0365817713819794,-0.0197874157272833,-0.00214094981195455));
#16299=CARTESIAN_POINT('',(-0.036447921275795,-0.0195856202356591,-0.00211345256966799));
#16300=CARTESIAN_POINT('',(-0.0363510262352866,-0.0194416700387721,-0.00207720972953836));
#16301=CARTESIAN_POINT('',(-0.0362580220091507,-0.0193042484564968,-0.00203733692692017));
#16302=CARTESIAN_POINT('',(-0.0361233040282915,-0.0191073092266076,-0.00195880329346809));
#16303=CARTESIAN_POINT('',(-0.0360272389495356,-0.0189684923391471,-0.0018892932806967));
#16304=CARTESIAN_POINT('',(-0.0359036157281572,-0.0187914045898843,-0.00178139164613739));
#16305=CARTESIAN_POINT('',(-0.0357760361122662,-0.0186107110632828,-0.0016490576045929));
#16306=CARTESIAN_POINT('',(-0.0355845872601076,-0.0183429504628644,-0.00138866627045801));
#16307=CARTESIAN_POINT('',(-0.0354400098077096,-0.0181456531213779,-0.00111147707701261));
#16308=CARTESIAN_POINT('',(-0.0352974513270199,-0.0179522358156644,-0.000700457148026627));
#16309=CARTESIAN_POINT('',(-0.0352033477140541,-0.0178272165773168,-0.000188108710314427));
#16310=CARTESIAN_POINT('',(-0.0352316825933212,-0.0178648366965096,0.000435137210326799));
#16311=CARTESIAN_POINT('',(-0.0353617642821596,-0.0180387546663218,0.000914250187784095));
#16312=CARTESIAN_POINT('',(-0.03553395885398,-0.0182741336531804,0.00130128242879666));
#16313=CARTESIAN_POINT('',(-0.035690043688318,-0.0184892146354674,0.00154606731033654));
#16314=CARTESIAN_POINT('',(-0.0358977301136526,-0.0187828569970073,0.00177961911332545));
#16315=CARTESIAN_POINT('',(-0.0360269463745707,-0.0189679731916343,0.00188900746451258));
#16316=CARTESIAN_POINT('',(-0.03615568331116,-0.0191545051998607,0.00197964638970481));
#16317=CARTESIAN_POINT('',(-0.0362517163788373,-0.0192949662460136,0.00203324444307036));
#16318=CARTESIAN_POINT('',(-0.0363379367050595,-0.0194223358161986,0.00207208749675905));
#16319=CARTESIAN_POINT('',(-0.0363829297000817,-0.0194892300968965,0.00208844777432515));
#16320=CARTESIAN_POINT('',(-0.0363829296981285,-0.0194892300988016,0.00208844777506104));
#16321=CARTESIAN_POINT('',(-0.0367214015132256,-0.0200000002179966,-0.00215000333373415));
#16322=CARTESIAN_POINT('',(-0.0363829297000817,-0.0194892300968965,0.00208844777432515));
#16323=CARTESIAN_POINT('',(-0.0364957535948001,-0.0196562090026207,0.00212928566385514));
#16324=CARTESIAN_POINT('',(-0.0366085774895185,-0.019828099772606,0.00215));
#16325=CARTESIAN_POINT('',(-0.0367214013842369,-0.02,0.00215));
#16326=CARTESIAN_POINT('',(-0.0367214014187913,-0.0200000000544145,0.00215000673958342));
#16327=CARTESIAN_POINT('',(-0.0367214014855027,-0.0200000001547961,0.00214999999999999));
#16328=CARTESIAN_POINT('',(-0.0368094489890548,-0.0201348294968441,0.00214999999029253));
#16329=CARTESIAN_POINT('',(-0.0369082050670065,-0.0202876273874728,0.00213709176971192));
#16330=CARTESIAN_POINT('',(-0.0370729159603206,-0.020546178196832,0.00208205843123112));
#16331=CARTESIAN_POINT('',(-0.0372054092685199,-0.0207559551904642,0.00201904010762059));
#16332=CARTESIAN_POINT('',(-0.0374076931255592,-0.0210813111222118,0.00187105308343718));
#16333=CARTESIAN_POINT('',(-0.0375741836336396,-0.0213529605587038,0.00168520277677421));
#16334=CARTESIAN_POINT('',(-0.0377619138459259,-0.0216642665456907,0.00138145860675146));
#16335=CARTESIAN_POINT('',(-0.0378873214687462,-0.0218745084926748,0.0010778688280807));
#16336=CARTESIAN_POINT('',(-0.0379943792862313,-0.0220560156885546,0.00067569085601466));
#16337=CARTESIAN_POINT('',(-0.0380653382957039,-0.0221767836959647,0.000144366751129057));
#16338=CARTESIAN_POINT('',(-0.0380390815274064,-0.0221318227466957,-0.000454597526155525));
#16339=CARTESIAN_POINT('',(-0.0379290145646173,-0.0219451171585747,-0.00094760900861487));
#16340=CARTESIAN_POINT('',(-0.0377914075906246,-0.0217133734686235,-0.00131827900098319));
#16341=CARTESIAN_POINT('',(-0.0376479878638091,-0.0214749573987788,-0.0015807999458275));
#16342=CARTESIAN_POINT('',(-0.037440299198058,-0.0211338733786737,-0.00184001127321334));
#16343=CARTESIAN_POINT('',(-0.0372619157406907,-0.0208464940115701,-0.00198583361015462));
#16344=CARTESIAN_POINT('',(-0.0371044376005431,-0.020595750099457,-0.00207017933556629));
#16345=CARTESIAN_POINT('',(-0.0370209006250623,-0.0204645344905706,-0.0020992159743748));
#16346=CARTESIAN_POINT('',(-0.037020900637956,-0.020464534518328,-0.00209921596804585));
#16347=CARTESIAN_POINT('',(-0.0370209006250623,-0.0204645344905706,-0.0020992159743748));
#16348=CARTESIAN_POINT('',(-0.0369382714896785,-0.0203347448757318,-0.00212793705564823));
#16349=CARTESIAN_POINT('',(-0.0368384384344523,-0.0201792218773405,-0.00214999998084516));
#16350=CARTESIAN_POINT('',(-0.0367214014593838,-0.0200000002297874,-0.00214999999999999));
#16351=CARTESIAN_POINT('',(-0.0345,-0.01,-0.017320508076));
#16352=CARTESIAN_POINT('',(-0.0370209006250624,-0.00841429288357993,-0.0187724147329261));
#16353=CARTESIAN_POINT('',(-0.0369382714896786,-0.00832452489015546,-0.0186743741699733));
#16354=CARTESIAN_POINT('',(-0.0368384384344524,-0.00822765633725888,-0.0185507187651021));
#16355=CARTESIAN_POINT('',(-0.0367214014593838,-0.00813804549689372,-0.0183955082750017));
#16356=CARTESIAN_POINT('',(-0.0367214015196458,-0.00813804260431159,-0.0183955099312896));
#16357=CARTESIAN_POINT('',(-0.037020900637956,-0.0084142929028602,-0.0187724147537266));
#16358=CARTESIAN_POINT('',(-0.0367214013837088,-0.00813804543876341,-0.0183955081743171));
#16359=CARTESIAN_POINT('',(-0.0367099515902943,-0.00812927876222418,-0.0183803238469904));
#16360=CARTESIAN_POINT('',(-0.0366706595167001,-0.00809948687848419,-0.0183283412063308));
#16361=CARTESIAN_POINT('',(-0.0365817713830814,-0.00803959093902229,-0.01820687960295));
#16362=CARTESIAN_POINT('',(-0.0364479212752632,-0.00796250650282354,-0.0180183709572473));
#16363=CARTESIAN_POINT('',(-0.0363510262345629,-0.00792191862265392,-0.0178755850107191));
#16364=CARTESIAN_POINT('',(-0.0362580220107654,-0.00788773870098001,-0.0177366380263864));
#16365=CARTESIAN_POINT('',(-0.0361233040225563,-0.00785728117283103,-0.0175268168421644));
#16366=CARTESIAN_POINT('',(-0.0360272389715468,-0.00784807029588221,-0.0173718428532673));
#16367=CARTESIAN_POINT('',(-0.0359036156458474,-0.00785297149296298,-0.017164529662831));
#16368=CARTESIAN_POINT('',(-0.0357760365507627,-0.00787723178427133,-0.0169418768814245));
#16369=CARTESIAN_POINT('',(-0.0355845837251886,-0.00796883860250597,-0.0165797981192282));
#16370=CARTESIAN_POINT('',(-0.0354400227144834,-0.00811031891300495,-0.0162703208634176));
#16371=CARTESIAN_POINT('',(-0.035297403234844,-0.00836928163819279,-0.0158973739307318));
#16372=CARTESIAN_POINT('',(-0.0352036030273427,-0.00875188303428271,-0.0155325949701537));
#16373=CARTESIAN_POINT('',(-0.0352300877690043,-0.00930187689549947,-0.0152555942094222));
#16374=CARTESIAN_POINT('',(-0.0353624250665134,-0.00981312376305411,-0.0151648195632774));
#16375=CARTESIAN_POINT('',(-0.0355323875544582,-0.0102612841707686,-0.0151742083556311));
#16376=CARTESIAN_POINT('',(-0.0356952788199552,-0.0105915687258194,-0.0152431274376651));
#16377=CARTESIAN_POINT('',(-0.0359199076858085,-0.0109730735621656,-0.015389020528737));
#16378=CARTESIAN_POINT('',(-0.0361452214386918,-0.011283331940451,-0.0155847980942524));
#16379=CARTESIAN_POINT('',(-0.036292938920463,-0.011458027693942,-0.0157344351657852));
#16380=CARTESIAN_POINT('',(-0.0363829297000817,-0.0115532638753583,-0.0158339444772937));
#16381=CARTESIAN_POINT('',(-0.0363829296981285,-0.0115532638766184,-0.0158339444786343));
#16382=CARTESIAN_POINT('',(-0.0363829297000817,-0.0115532638753583,-0.0158339444772937));
#16383=CARTESIAN_POINT('',(-0.0364957535948001,-0.0116721200040918,-0.0159581335340468));
#16384=CARTESIAN_POINT('',(-0.0366085774895185,-0.0117760045498996,-0.0160966381730355));
#16385=CARTESIAN_POINT('',(-0.0367214013842369,-0.0118619546746311,-0.016245508174088));
#16386=CARTESIAN_POINT('',(-0.0367214014146637,-0.0118619604972779,-0.0162455047804234));
#16387=CARTESIAN_POINT('',(-0.0367214014593838,-0.0118619547324527,-0.016245508274238));
#16388=CARTESIAN_POINT('',(-0.0368094504192829,-0.0119293705059448,-0.0163622758478597));
#16389=CARTESIAN_POINT('',(-0.0369082047152049,-0.0119945891801026,-0.0165010543225801));
#16390=CARTESIAN_POINT('',(-0.0370729160019372,-0.0120762046321228,-0.0167524831086091));
#16391=CARTESIAN_POINT('',(-0.0372054092111889,-0.012126517585255,-0.0169656643348472));
#16392=CARTESIAN_POINT('',(-0.0374076931232449,-0.0121610350729264,-0.0173214244251849));
#16393=CARTESIAN_POINT('',(-0.0375741836148091,-0.0121359086968873,-0.0176496048646528));
#16394=CARTESIAN_POINT('',(-0.0377619138370843,-0.0120285115303349,-0.0180710758569835));
#16395=CARTESIAN_POINT('',(-0.0378873214603961,-0.0118707160469429,-0.0184049456120169));
#16396=CARTESIAN_POINT('',(-0.0379943792822431,-0.0116131733062125,-0.0187632244478438));
#16397=CARTESIAN_POINT('',(-0.0380653382950396,-0.0112134171394556,-0.0191334746681379));
#16398=CARTESIAN_POINT('',(-0.0380390815294286,-0.0106722183817588,-0.0193940194895447));
#16399=CARTESIAN_POINT('',(-0.0379290145681879,-0.0101519051183761,-0.0194788334521171));
#16400=CARTESIAN_POINT('',(-0.0377914075938042,-0.00971502363865889,-0.0194634725276762));
#16401=CARTESIAN_POINT('',(-0.0376479878673517,-0.00936846579559278,-0.0193882586280947));
#16402=CARTESIAN_POINT('',(-0.0374402992000195,-0.00897344018668948,-0.0192224768650296));
#16403=CARTESIAN_POINT('',(-0.0372619157421827,-0.0087034646538467,-0.0190465102007785));
#16404=CARTESIAN_POINT('',(-0.0371044376010715,-0.0085050471554441,-0.0188715324648092));
#16405=CARTESIAN_POINT('',(-0.0370209006250624,-0.00841429288357993,-0.0187724147329261));
#16406=CARTESIAN_POINT('',(-0.087860759494,-0.013728578874,0.019318802295));
#16407=CARTESIAN_POINT('',(-0.0385114728765227,-0.0140270889248519,0.0192889401143525));
#16408=CARTESIAN_POINT('',(-0.038573289075003,-0.0140394345481,0.0194123501448213));
#16409=CARTESIAN_POINT('',(-0.0386752804813098,-0.0139811072101053,0.0195073825579457));
#16410=CARTESIAN_POINT('',(-0.0387712812922,-0.0139023583533399,0.0195633440960825));
#16411=CARTESIAN_POINT('',(-0.0387712814781634,-0.0139023583534943,0.0195633440959764));
#16412=CARTESIAN_POINT('',(-0.0441999997501262,-0.01390235835348,0.019563344096154));
#16413=CARTESIAN_POINT('',(-0.0423904270131806,-0.01390235835348,0.019563344096154));
#16414=CARTESIAN_POINT('',(-0.0405808542762351,-0.01390235835348,0.019563344096154));
#16415=CARTESIAN_POINT('',(-0.0387712815392895,-0.01390235835348,0.019563344096154));
#16416=CARTESIAN_POINT('',(-0.087860759494,-0.009866284121,0.02154869921));
#16417=CARTESIAN_POINT('',(-0.04419999975,-0.00999117379127614,0.0218214675554262));
#16418=CARTESIAN_POINT('',(-0.0423904270660306,-0.00999117379127614,0.0218214675554262));
#16419=CARTESIAN_POINT('',(-0.0405808543820613,-0.00999117379127614,0.0218214675554262));
#16420=CARTESIAN_POINT('',(-0.038771281698092,-0.00999117379127614,0.0218214675554262));
#16421=CARTESIAN_POINT('',(-0.038771281698092,-0.0099911738207244,0.0218214675419355));
#16422=CARTESIAN_POINT('',(-0.0387712812921071,-0.00999117379334386,0.0218214675543855));
#16423=CARTESIAN_POINT('',(-0.0386753744229194,-0.00990342107731365,0.0218616459994942));
#16424=CARTESIAN_POINT('',(-0.0385732282122488,-0.00979177178844656,0.0218646104089203));
#16425=CARTESIAN_POINT('',(-0.0385114731132445,-0.00969116807386408,0.0217922856834247));
#16426=CARTESIAN_POINT('',(-0.087860759494,0.,0.));
#16427=CARTESIAN_POINT('',(-0.038771281292,-0.00999117382072726,0.0218214675419417));
#16428=CARTESIAN_POINT('',(-0.038771281292,-0.0113619672026171,0.0211938362919151));
#16429=CARTESIAN_POINT('',(-0.038771281292,-0.0126734170568365,0.0204366703644534));
#16430=CARTESIAN_POINT('',(-0.038771281292,-0.0139023583534153,0.0195633440958652));
#16431=CARTESIAN_POINT('',(-0.087860759494,0.009866284121,0.02154869921));
#16432=CARTESIAN_POINT('',(-0.0385114717026308,0.00969116577615237,0.0217922840320089));
#16433=CARTESIAN_POINT('',(-0.0385732483128315,0.00979180548548719,0.0218646360742229));
#16434=CARTESIAN_POINT('',(-0.0386753409989158,0.00990339049508929,0.0218616600018668));
#16435=CARTESIAN_POINT('',(-0.0387712812921071,0.00999117379334386,0.0218214675543855));
#16436=CARTESIAN_POINT('',(-0.0387712813225499,0.00999117382638656,0.0218214675391701));
#16437=CARTESIAN_POINT('',(-0.038771281542,0.0099911737873573,0.0218214675572204));
#16438=CARTESIAN_POINT('',(-0.040580854278,0.0099911737873573,0.0218214675572204));
#16439=CARTESIAN_POINT('',(-0.042390427014,0.0099911737873573,0.0218214675572204));
#16440=CARTESIAN_POINT('',(-0.04419999975,0.0099911737873573,0.0218214675572204));
#16441=CARTESIAN_POINT('',(-0.087860759494,0.013728578874,0.019318802295));
#16442=CARTESIAN_POINT('',(-0.03851147287724,0.0140270889244258,0.0192889401149925));
#16443=CARTESIAN_POINT('',(-0.038573288943412,0.0140394345209634,0.0194123498809255));
#16444=CARTESIAN_POINT('',(-0.0386752806869572,0.0139811070414031,0.0195073826778311));
#16445=CARTESIAN_POINT('',(-0.0387712812922,0.0139023583533399,0.0195633440960825));
#16446=CARTESIAN_POINT('',(-0.0387712813306431,0.0139023583200914,0.0195633441197136));
#16447=CARTESIAN_POINT('',(-0.0387712815392895,0.0139023583534361,0.0195633440961853));
#16448=CARTESIAN_POINT('',(-0.0405808542762351,0.0139023583534361,0.0195633440961853));
#16449=CARTESIAN_POINT('',(-0.0423904270131806,0.0139023583534361,0.0195633440961853));
#16450=CARTESIAN_POINT('',(-0.0441999997501262,0.0139023583534361,0.0195633440961853));
#16451=CARTESIAN_POINT('',(-0.087860759494,0.,0.));
#16452=CARTESIAN_POINT('',(-0.038771281292,0.0139023583499953,0.0195633440982956));
#16453=CARTESIAN_POINT('',(-0.038771281292,0.0126734170460618,0.0204366703717869));
#16454=CARTESIAN_POINT('',(-0.038771281292,0.0113619671835387,0.0211938363027715));
#16455=CARTESIAN_POINT('',(-0.038771281292,0.00999117379281267,0.0218214675547227));
#16456=CARTESIAN_POINT('',(-0.0442,0.0235948629949949,0.002229896915));
#16457=CARTESIAN_POINT('',(-0.0441999999970615,0.023893532146402,0.00225812346420597));
#16458=CARTESIAN_POINT('',(-0.0441999999970615,0.0238821025668367,0.0023790614791501));
#16459=CARTESIAN_POINT('',(-0.0441999999970615,0.0237898463900922,0.00248823412576593));
#16460=CARTESIAN_POINT('',(-0.0441999999970615,0.0236725087091264,0.00251967466286776));
#16461=CARTESIAN_POINT('',(-0.087860759494,0.023594862995,-0.002229896915));
#16462=CARTESIAN_POINT('',(-0.0387712815392895,0.0238935321468372,-0.00225812345819673));
#16463=CARTESIAN_POINT('',(-0.0405808542762351,0.0238935321468372,-0.00225812345819673));
#16464=CARTESIAN_POINT('',(-0.0423904270131806,0.0238935321468372,-0.00225812345819673));
#16465=CARTESIAN_POINT('',(-0.0441999997501262,0.0238935321468372,-0.00225812345819673));
#16466=CARTESIAN_POINT('',(-0.0387712813230477,0.0238935321497167,-0.00225812342724101));
#16467=CARTESIAN_POINT('',(-0.0385114731151673,0.0237182570486275,-0.00250334509570224));
#16468=CARTESIAN_POINT('',(-0.0385732893238704,0.0238313057094952,-0.00245233165510885));
#16469=CARTESIAN_POINT('',(-0.0386752804420734,0.0238844424877642,-0.00235430245929402));
#16470=CARTESIAN_POINT('',(-0.0387712812922245,0.0238935321467271,-0.00225812345823865));
#16471=CARTESIAN_POINT('',(-0.087860759494,0.,0.));
#16472=CARTESIAN_POINT('',(-0.038771281542,0.0238935321456456,0.00225812346983103));
#16473=CARTESIAN_POINT('',(-0.040580854278,0.0238935321456456,0.00225812346983103));
#16474=CARTESIAN_POINT('',(-0.042390427014,0.0238935321456456,0.00225812346983103));
#16475=CARTESIAN_POINT('',(-0.04419999975,0.0238935321456456,0.00225812346983103));
#16476=CARTESIAN_POINT('',(-0.0387712813158654,0.0238935321486615,0.0022581234372457));
#16477=CARTESIAN_POINT('',(-0.038771281292,0.,0.));
#16478=CARTESIAN_POINT('',(-0.087860759494,0.013728578874,-0.019318802295));
#16479=CARTESIAN_POINT('',(-0.0385114728779744,0.0140270889245724,-0.0192889401164586));
#16480=CARTESIAN_POINT('',(-0.0385732890765705,0.0140394345468466,-0.0194123501457808));
#16481=CARTESIAN_POINT('',(-0.0386752804819875,0.013981107209601,-0.0195073825583042));
#16482=CARTESIAN_POINT('',(-0.0387712812922,0.0139023583533399,-0.0195633440960825));
#16483=CARTESIAN_POINT('',(-0.0387712814781634,0.013902358347653,-0.0195633441001275));
#16484=CARTESIAN_POINT('',(-0.0441999997501262,0.0139023583533358,-0.0195633440962565));
#16485=CARTESIAN_POINT('',(-0.0423904270131806,0.0139023583533358,-0.0195633440962565));
#16486=CARTESIAN_POINT('',(-0.0405808542762351,0.0139023583533358,-0.0195633440962565));
#16487=CARTESIAN_POINT('',(-0.0387712815392895,0.0139023583533358,-0.0195633440962565));
#16488=CARTESIAN_POINT('',(-0.087860759494,0.009866284121,-0.02154869921));
#16489=CARTESIAN_POINT('',(-0.0385114728779643,0.00969116769057448,-0.0217922854078746));
#16490=CARTESIAN_POINT('',(-0.0385732889440606,0.00979187088396713,-0.0218646818897494));
#16491=CARTESIAN_POINT('',(-0.0386752807584405,0.00990333537634139,-0.0218616852385245));
#16492=CARTESIAN_POINT('',(-0.0387712812921071,0.00999117379334244,-0.0218214675543824));
#16493=CARTESIAN_POINT('',(-0.0387712813312419,0.00999117383538471,-0.0218214675352231));
#16494=CARTESIAN_POINT('',(-0.0387712815392895,0.00999117379350284,-0.0218214675543916));
#16495=CARTESIAN_POINT('',(-0.0405808542762351,0.00999117379350284,-0.0218214675543916));
#16496=CARTESIAN_POINT('',(-0.0423904270131806,0.00999117379350284,-0.0218214675543916));
#16497=CARTESIAN_POINT('',(-0.0441999997501262,0.00999117379350284,-0.0218214675543916));
#16498=CARTESIAN_POINT('',(-0.087860759494,0.,0.));
#16499=CARTESIAN_POINT('',(-0.038771281292,0.00999117380568283,-0.0218214675488299));
#16500=CARTESIAN_POINT('',(-0.038771281292,0.0113619671887648,-0.0211938362994007));
#16501=CARTESIAN_POINT('',(-0.038771281292,0.0126734170441997,-0.0204366703723515));
#16502=CARTESIAN_POINT('',(-0.038771281292,0.0139023583419703,-0.0195633441039984));
#16503=CARTESIAN_POINT('',(-0.087860759494,-0.009866284121,-0.02154869921));
#16504=CARTESIAN_POINT('',(-0.0385114728775843,-0.00969116768995542,-0.0217922854074296));
#16505=CARTESIAN_POINT('',(-0.0385732890761236,-0.00979187109936457,-0.0218646820449889));
#16506=CARTESIAN_POINT('',(-0.0386752805524257,-0.00990333518783425,-0.0218616853248344));
#16507=CARTESIAN_POINT('',(-0.0387712812921071,-0.00999117379334244,-0.0218214675543824));
#16508=CARTESIAN_POINT('',(-0.0387712814781634,-0.00999117379760892,-0.0218214675525191));
#16509=CARTESIAN_POINT('',(-0.0441999997501262,-0.00999117379345386,-0.021821467554414));
#16510=CARTESIAN_POINT('',(-0.0423904270131806,-0.00999117379345386,-0.021821467554414));
#16511=CARTESIAN_POINT('',(-0.0405808542762351,-0.00999117379345386,-0.021821467554414));
#16512=CARTESIAN_POINT('',(-0.0387712815392895,-0.00999117379345386,-0.021821467554414));
#16513=CARTESIAN_POINT('',(-0.087860759494,-0.013728578874,-0.019318802295));
#16514=CARTESIAN_POINT('',(-0.0385114728754421,-0.014027088925738,-0.019288940113728));
#16515=CARTESIAN_POINT('',(-0.03857328894209,-0.014039434522914,-0.0194123498813593));
#16516=CARTESIAN_POINT('',(-0.0386752806859938,-0.0139811070422414,-0.0195073826772354));
#16517=CARTESIAN_POINT('',(-0.0387712812922,-0.0139023583533399,-0.0195633440960825));
#16518=CARTESIAN_POINT('',(-0.0387712813300123,-0.0139023583246212,-0.0195633441164946));
#16519=CARTESIAN_POINT('',(-0.0387712815392895,-0.0139023583535364,-0.019563344096114));
#16520=CARTESIAN_POINT('',(-0.0405808542762351,-0.0139023583535364,-0.019563344096114));
#16521=CARTESIAN_POINT('',(-0.0423904270131806,-0.0139023583535364,-0.019563344096114));
#16522=CARTESIAN_POINT('',(-0.0441999997501262,-0.0139023583535364,-0.019563344096114));
#16523=CARTESIAN_POINT('',(-0.087860759494,0.,0.));
#16524=CARTESIAN_POINT('',(-0.038771281292,-0.0139023583580203,-0.0195633440925927));
#16525=CARTESIAN_POINT('',(-0.038771281292,-0.0126734170544451,-0.0204366703665882));
#16526=CARTESIAN_POINT('',(-0.038771281292,-0.0113619671922325,-0.0211938362981107));
#16527=CARTESIAN_POINT('',(-0.038771281292,-0.00999117380176398,-0.0218214675506242));
#16528=CARTESIAN_POINT('',(-0.087860759494,-0.023594862995,-0.002229896915));
#16529=CARTESIAN_POINT('',(-0.0385114728774445,-0.0237182566135284,-0.00250334529184601));
#16530=CARTESIAN_POINT('',(-0.0385732890757216,-0.0238313056460365,-0.0024523319000197));
#16531=CARTESIAN_POINT('',(-0.0386752803220459,-0.0238844424764206,-0.00235430257962145));
#16532=CARTESIAN_POINT('',(-0.0387712812922245,-0.0238935321467551,-0.00225812345824131));
#16533=CARTESIAN_POINT('',(-0.0387712814781634,-0.0238935321469843,-0.00225812345615336));
#16534=CARTESIAN_POINT('',(-0.0441999965249051,-0.0238935321468321,-0.00225812345825037));
#16535=CARTESIAN_POINT('',(-0.0423904248630333,-0.0238935321468321,-0.00225812345825037));
#16536=CARTESIAN_POINT('',(-0.0405808532011614,-0.0238935321468321,-0.00225812345825037));
#16537=CARTESIAN_POINT('',(-0.0387712815392895,-0.0238935321468321,-0.00225812345825037));
#16538=CARTESIAN_POINT('',(-0.087860759494,-0.023594862995,0.002229896915));
#16539=CARTESIAN_POINT('',(-0.0385114728763641,-0.0237182566134299,0.0025033452929254));
#16540=CARTESIAN_POINT('',(-0.0385732889426975,-0.023831305405075,0.00245233201003066));
#16541=CARTESIAN_POINT('',(-0.038675280526865,-0.0238844424958164,0.00235430237439214));
#16542=CARTESIAN_POINT('',(-0.0387712812922245,-0.0238935321467551,0.00225812345824131));
#16543=CARTESIAN_POINT('',(-0.0387712813303033,-0.02389353215034,0.00225812342064574));
#16544=CARTESIAN_POINT('',(-0.0387712815392895,-0.0238935321468256,0.00225812345831925));
#16545=CARTESIAN_POINT('',(-0.0405808531921476,-0.0238935321468256,0.00225812345831925));
#16546=CARTESIAN_POINT('',(-0.0423904248450057,-0.0238935321468256,0.00225812345831925));
#16547=CARTESIAN_POINT('',(-0.0441999964978638,-0.0238935321468256,0.00225812345831925));
#16548=CARTESIAN_POINT('',(-0.087860759494,0.,0.));
#16549=CARTESIAN_POINT('',(-0.038771281292,-0.0238935321466156,0.00225812345956669));
#16550=CARTESIAN_POINT('',(-0.038771281292,-0.0240353842336054,0.000757165933885015));
#16551=CARTESIAN_POINT('',(-0.038771281292,-0.02403538423378,-0.000757165928341963));
#16552=CARTESIAN_POINT('',(-0.038771281292,-0.0238935321471364,-0.00225812345405635));
#16553=CARTESIAN_POINT('',(-0.0363829297,0.007935966222,-0.017922392252));
#16554=CARTESIAN_POINT('',(-0.036137554584,0.007975350095,-0.01805745087));
#16555=CARTESIAN_POINT('',(-0.036123122079,0.007706601765,-0.018144438831));
#16556=CARTESIAN_POINT('',(-0.036296388628,0.00789888486,-0.017795229609));
#16557=CARTESIAN_POINT('',(-0.036059352191,0.00792917773300001,-0.017929626577));
#16558=CARTESIAN_POINT('',(-0.03603658062,0.007664471384,-0.017999478691));
#16559=CARTESIAN_POINT('',(-0.036211750879,0.007873865053,-0.017666078425));
#16560=CARTESIAN_POINT('',(-0.03598108599,0.007894696976,-0.017796520282));
#16561=CARTESIAN_POINT('',(-0.035951943258,0.00763618434,-0.017852211978));
#16562=CARTESIAN_POINT('',(-0.036046427611,0.007847575992,-0.017403812149));
#16563=CARTESIAN_POINT('',(-0.03582764111,0.00785209075899999,-0.01752422126));
#16564=CARTESIAN_POINT('',(-0.03578661999,0.007606880233,-0.017553069188));
#16565=CARTESIAN_POINT('',(-0.035965731891,0.007846286179,-0.017270695297));
#16566=CARTESIAN_POINT('',(-0.035752240428,0.00784321052600001,-0.017384956612));
#16567=CARTESIAN_POINT('',(-0.03570592427,0.00760583974,-0.017401191901));
#16568=CARTESIAN_POINT('',(-0.035867783855,0.007860916809,-0.017101471238));
#16569=CARTESIAN_POINT('',(-0.035659677357,0.00785025534,-0.017205405462));
#16570=CARTESIAN_POINT('',(-0.035607976234,0.007623195358,-0.017208053208));
#16571=CARTESIAN_POINT('',(-0.03584830488,0.007864675489,-0.017067415562));
#16572=CARTESIAN_POINT('',(-0.035641412325,0.007852547538,-0.017169542439));
#16573=CARTESIAN_POINT('',(-0.035588497259,0.007627622941,-0.017169181517));
#16574=CARTESIAN_POINT('',(-0.035810061793,0.007873792339,-0.016999715979));
#16575=CARTESIAN_POINT('',(-0.035605524332,0.00785891862899999,-0.017098165957));
#16576=CARTESIAN_POINT('',(-0.035550254172,0.007638313039,-0.017091901304));
#16577=CARTESIAN_POINT('',(-0.035791254693,0.00787915358,-0.016965999395));
#16578=CARTESIAN_POINT('',(-0.035587855191,0.00786298741,-0.01706256955));
#16579=CARTESIAN_POINT('',(-0.035531447072,0.007644579318,-0.017053409847));
#16580=CARTESIAN_POINT('',(-0.035735788251,0.007897644484,-0.016865244352));
#16581=CARTESIAN_POINT('',(-0.035535852231,0.007877830875,-0.016956380478));
#16582=CARTESIAN_POINT('',(-0.03547598063,0.007666140505,-0.016938375535));
#16583=CARTESIAN_POINT('',(-0.035700081089,0.007913175312,-0.016798599729));
#16584=CARTESIAN_POINT('',(-0.035502196601,0.007891267476,-0.016885756544));
#16585=CARTESIAN_POINT('',(-0.035440273468,0.007684190871,-0.016862271769));
#16586=CARTESIAN_POINT('',(-0.035596955729,0.007969579454,-0.016600233953));
#16587=CARTESIAN_POINT('',(-0.035405412743,0.007942282341,-0.016676313757));
#16588=CARTESIAN_POINT('',(-0.035337148108,0.007749601706,-0.016635705408));
#16589=CARTESIAN_POINT('',(-0.035533471872,0.008020130655,-0.016470062373));
#16590=CARTESIAN_POINT('',(-0.03534514464,0.007990615333,-0.016537412932));
#16591=CARTESIAN_POINT('',(-0.035273664252,0.00780806873,-0.016486967212));
#16592=CARTESIAN_POINT('',(-0.035462076716,0.008101852446,-0.016310148785));
#16593=CARTESIAN_POINT('',(-0.0352770564989999,0.008072198153,-0.016365801681));
#16594=CARTESIAN_POINT('',(-0.035202269094,0.007902417857,-0.016304149447));
#16595=CARTESIAN_POINT('',(-0.035448157312,0.008119195502,-0.016278204166));
#16596=CARTESIAN_POINT('',(-0.035263851039,0.008089510152,-0.016331706315));
#16597=CARTESIAN_POINT('',(-0.035188349691,0.007922433981,-0.016267624501));
#16598=CARTESIAN_POINT('',(-0.035421421576,0.008155528492,-0.01621518104));
#16599=CARTESIAN_POINT('',(-0.035238481118,0.008125981757,-0.0162644302));
#16600=CARTESIAN_POINT('',(-0.035161613954,0.007964353608,-0.016195554481));
#16601=CARTESIAN_POINT('',(-0.035408615027,0.008174492909,-0.016184132248));
#16602=CARTESIAN_POINT('',(-0.035226318844,0.008145113188,-0.016231268977));
#16603=CARTESIAN_POINT('',(-0.035148807406,0.007986227718,-0.01616004343));
#16604=CARTESIAN_POINT('',(-0.035371903227,0.008233790533,-0.016092375852));
#16605=CARTESIAN_POINT('',(-0.035191509303,0.008205098964,-0.016133439925));
#16606=CARTESIAN_POINT('',(-0.035112095605,0.008054604749,-0.016055083828));
#16607=CARTESIAN_POINT('',(-0.035349701075,0.00827652121,-0.01603305419));
#16608=CARTESIAN_POINT('',(-0.035170375015,0.00824874590400001,-0.016070010593));
#16609=CARTESIAN_POINT('',(-0.035089893455,0.008103854486,-0.015987204245));
#16610=CARTESIAN_POINT('',(-0.035310076825,0.008368595603,-0.015918211266));
#16611=CARTESIAN_POINT('',(-0.035132682741,0.008343387593,-0.015947352599));
#16612=CARTESIAN_POINT('',(-0.035050269204,0.008209928279,-0.015855746634));
#16613=CARTESIAN_POINT('',(-0.035292653375,0.008417937511,-0.015862688976));
#16614=CARTESIAN_POINT('',(-0.035116074086,0.00839440358600001,-0.015888019139));
#16615=CARTESIAN_POINT('',(-0.035032845755,0.008266750265,-0.015792167434));
#16616=CARTESIAN_POINT('',(-0.035270404132,0.008497251596,-0.015782437272));
#16617=CARTESIAN_POINT('',(-0.035094864144,0.008476841102,-0.015802332322));
#16618=CARTESIAN_POINT('',(-0.03501059651,0.00835805282,-0.015700230057));
#16619=CARTESIAN_POINT('',(-0.03526362249,0.008524662259,-0.015756120857));
#16620=CARTESIAN_POINT('',(-0.035088401673,0.008505365652,-0.015774270534));
#16621=CARTESIAN_POINT('',(-0.035003814869,0.008389601082,-0.015670074582));
#16622=CARTESIAN_POINT('',(-0.035251577427,0.008580564888,-0.015705227052));
#16623=CARTESIAN_POINT('',(-0.035076925826,0.008563640037,-0.01572005437));
#16624=CARTESIAN_POINT('',(-0.034991769806,0.008453930794,-0.015611741863));
#16625=CARTESIAN_POINT('',(-0.035246291308,0.008609118788,-0.015680578683));
#16626=CARTESIAN_POINT('',(-0.035071886429,0.00859346260300001,-0.015693811186));
#16627=CARTESIAN_POINT('',(-0.034986483687,0.008486783572,-0.015583483346));
#16628=CARTESIAN_POINT('',(-0.035223521483,0.008754870702,-0.01556128769));
#16629=CARTESIAN_POINT('',(-0.035050225188,0.008745616554,-0.015567192245));
#16630=CARTESIAN_POINT('',(-0.034963713862,0.008654451161,-0.015446682695));
#16631=CARTESIAN_POINT('',(-0.035216913712,0.008880915106,-0.0154783625));
#16632=CARTESIAN_POINT('',(-0.035043883179,0.008878570113,-0.015479125626));
#16633=CARTESIAN_POINT('',(-0.034957106091,0.00879936203,-0.015351462313));
#16634=CARTESIAN_POINT('',(-0.035223876434,0.009050786794,-0.015391012352));
#16635=CARTESIAN_POINT('',(-0.035050518048,0.009057568695,-0.015387635792));
#16636=CARTESIAN_POINT('',(-0.034964068813,0.008994538787,-0.015250984281));
#16637=CARTESIAN_POINT('',(-0.03522604562,0.00908540579,-0.015374366785));
#16638=CARTESIAN_POINT('',(-0.035052587043,0.009094097267,-0.015370243184));
#16639=CARTESIAN_POINT('',(-0.034966237999,0.009034309077,-0.015231826369));
#16640=CARTESIAN_POINT('',(-0.035231850552,0.009154857947,-0.015343216139));
#16641=CARTESIAN_POINT('',(-0.035058120997,0.009167395622,-0.015337818228));
#16642=CARTESIAN_POINT('',(-0.034972042931,0.009114084127,-0.015195952232));
#16643=CARTESIAN_POINT('',(-0.0352354894,0.009189818174,-0.015328642479));
#16644=CARTESIAN_POINT('',(-0.035061591095,0.009204314377,-0.015322709066));
#16645=CARTESIAN_POINT('',(-0.034975681779,0.009154234899,-0.01517915715));
#16646=CARTESIAN_POINT('',(-0.035248550352,0.009295383715,-0.015287847634));
#16647=CARTESIAN_POINT('',(-0.035074046816,0.00931586337800001,-0.015280597597));
#16648=CARTESIAN_POINT('',(-0.034988742731,0.009275456669,-0.01513210841));
#16649=CARTESIAN_POINT('',(-0.035260111701,0.009366671914,-0.015264544541));
#16650=CARTESIAN_POINT('',(-0.035085080525,0.009391243379,-0.015256839807));
#16651=CARTESIAN_POINT('',(-0.03500030408,0.009357294881,-0.01510518209));
#16652=CARTESIAN_POINT('',(-0.035281577861,0.009474939166,-0.015235272178));
#16653=CARTESIAN_POINT('',(-0.035105505104,0.009505505488,-0.015227540121));
#16654=CARTESIAN_POINT('',(-0.03502177024,0.009481550391,-0.01507127367));
#16655=CARTESIAN_POINT('',(-0.035289421938,0.009511251248,-0.015226463836));
#16656=CARTESIAN_POINT('',(-0.035112977015,0.009543870113,-0.01521881712));
#16657=CARTESIAN_POINT('',(-0.035029614317,0.009523219169,-0.015061053398));
#16658=CARTESIAN_POINT('',(-0.035306476701,0.009584322003,-0.01521074306));
#16659=CARTESIAN_POINT('',(-0.035129211644,0.00962103848500001,-0.015203474112));
#16660=CARTESIAN_POINT('',(-0.03504666908,0.009607057743,-0.015042775596));
#16661=CARTESIAN_POINT('',(-0.035315718145,0.009621192412,-0.015203814));
#16662=CARTESIAN_POINT('',(-0.035138009535,0.00965997509200001,-0.015196840927));
#16663=CARTESIAN_POINT('',(-0.035055910524,0.0096493557,-0.015034698584));
#16664=CARTESIAN_POINT('',(-0.035345244257,0.009731576519,-0.015186028085));
#16665=CARTESIAN_POINT('',(-0.035166136457,0.00977663711299999,-0.015180221674));
#16666=CARTESIAN_POINT('',(-0.035085436637,0.009775971844,-0.01501389589));
#16667=CARTESIAN_POINT('',(-0.035367258146,0.009804686247,-0.01517816092));
#16668=CARTESIAN_POINT('',(-0.035187092355,0.009853788047,-0.015173570618));
#16669=CARTESIAN_POINT('',(-0.035107450524,0.009859809659,-0.015004586152));
#16670=CARTESIAN_POINT('',(-0.035415540032,0.009950034894,-0.01516985648));
#16671=CARTESIAN_POINT('',(-0.035232955499,0.010006887199,-0.015168405072));
#16672=CARTESIAN_POINT('',(-0.035155732411,0.01002644331,-0.014994457537));
#16673=CARTESIAN_POINT('',(-0.035441809443,0.010022273518,-0.015169421497));
#16674=CARTESIAN_POINT('',(-0.035257918294,0.010082919856,-0.015169944486));
#16675=CARTESIAN_POINT('',(-0.035182001822,0.0101092388,-0.014993641282));
#16676=CARTESIAN_POINT('',(-0.035498359317,0.010165935271,-0.01517571553));
#16677=CARTESIAN_POINT('',(-0.035311533473,0.010233771266,-0.015180838497));
#16678=CARTESIAN_POINT('',(-0.035238551696,0.01027385273,-0.015000197616));
#16679=CARTESIAN_POINT('',(-0.035528803299,0.010237694895,-0.015182511514));
#16680=CARTESIAN_POINT('',(-0.035340397738,0.010309011127,-0.01519034352));
#16681=CARTESIAN_POINT('',(-0.035268995678,0.010356056437,-0.015007645243));
#16682=CARTESIAN_POINT('',(-0.035624302868,0.010448231116,-0.015212973614));
#16683=CARTESIAN_POINT('',(-0.035431143853,0.010530150409,-0.015229867744));
#16684=CARTESIAN_POINT('',(-0.035364495247,0.010597173211,-0.015041521636));
#16685=CARTESIAN_POINT('',(-0.035693625065,0.010582922476,-0.015246481917));
#16686=CARTESIAN_POINT('',(-0.035496770299,0.010670383783,-0.015270793079));
#16687=CARTESIAN_POINT('',(-0.035433817443,0.010751346613,-0.015079216188));
#16688=CARTESIAN_POINT('',(-0.035804878296,0.010777396222,-0.015314797255));
#16689=CARTESIAN_POINT('',(-0.035600812464,0.010870193851,-0.015350654782));
#16690=CARTESIAN_POINT('',(-0.035545070675,0.010973839943,-0.015156427299));
#16691=CARTESIAN_POINT('',(-0.035843360668,0.010841212942,-0.01534073771));
#16692=CARTESIAN_POINT('',(-0.035636958249,0.01093587108,-0.015380883423));
#16693=CARTESIAN_POINT('',(-0.035583553047,0.011046831996,-0.015185790742));
#16694=CARTESIAN_POINT('',(-0.035921655233,0.010964716188,-0.015397891995));
#16695=CARTESIAN_POINT('',(-0.035710302083,0.011062419569,-0.015446810101));
#16696=CARTESIAN_POINT('',(-0.035661847612,0.011188055569,-0.01525056404));
#16697=CARTESIAN_POINT('',(-0.035961464931,0.011024436082,-0.015429078645));
#16698=CARTESIAN_POINT('',(-0.035747535996,0.011123315491,-0.015482566139));
#16699=CARTESIAN_POINT('',(-0.035701657309,0.011256325476,-0.015285942678));
#16700=CARTESIAN_POINT('',(-0.036082708725,0.011197835672,-0.015530092476));
#16701=CARTESIAN_POINT('',(-0.035861344783,0.01130037601,-0.015598213312));
#16702=CARTESIAN_POINT('',(-0.035822901104,0.011454498054,-0.015400624625));
#16703=CARTESIAN_POINT('',(-0.036165937985,0.011305805198,-0.015607312287));
#16704=CARTESIAN_POINT('',(-0.035938765603,0.011408558316,-0.015685491612));
#16705=CARTESIAN_POINT('',(-0.035906130364,0.011577821075,-0.015488403863));
#16706=CARTESIAN_POINT('',(-0.036272749616,0.011431478006,-0.015715991043));
#16707=CARTESIAN_POINT('',(-0.036036325391,0.011531489845,-0.015805195535));
#16708=CARTESIAN_POINT('',(-0.036012941995,0.011721279377,-0.015612059748));
#16709=CARTESIAN_POINT('',(-0.036294271622,0.011456162931,-0.015738362019));
#16710=CARTESIAN_POINT('',(-0.036056160144,0.011555785974,-0.015830037016));
#16711=CARTESIAN_POINT('',(-0.036034464001,0.011749453109,-0.015637518901));
#16712=CARTESIAN_POINT('',(-0.036337241164,0.011504198589,-0.015783958945));
#16713=CARTESIAN_POINT('',(-0.036095695252,0.011602868295,-0.015880530299));
#16714=CARTESIAN_POINT('',(-0.036077433543,0.011804268644,-0.015689420125));
#16715=CARTESIAN_POINT('',(-0.036358730845,0.011527600241,-0.015807226781));
#16716=CARTESIAN_POINT('',(-0.03611543566,0.011625696687,-0.015906237255));
#16717=CARTESIAN_POINT('',(-0.036098923223,0.011830968578,-0.015715909844));
#16718=CARTESIAN_POINT('',(-0.036423211553,0.011595992591,-0.015878412814));
#16719=CARTESIAN_POINT('',(-0.036174782484,0.011692352266,-0.015984962597));
#16720=CARTESIAN_POINT('',(-0.036163403931,0.011908986452,-0.015796966748));
#16721=CARTESIAN_POINT('',(-0.036466213928,0.011639174576,-0.015927710753));
#16722=CARTESIAN_POINT('',(-0.036214084658,0.011733813027,-0.016039055431));
#16723=CARTESIAN_POINT('',(-0.036206406307,0.011958226934,-0.015853118487));
#16724=CARTESIAN_POINT('',(-0.036595254777,0.011761619038,-0.016081028728));
#16725=CARTESIAN_POINT('',(-0.03633245937,0.011851005228,-0.016207593429));
#16726=CARTESIAN_POINT('',(-0.036335447156,0.012097793945,-0.016027801545));
#16727=CARTESIAN_POINT('',(-0.036681322249,0.01183384166,-0.01619042867));
#16728=CARTESIAN_POINT('',(-0.036410235723,0.011917375548,-0.016326105441));
#16729=CARTESIAN_POINT('',(-0.036421514628,0.012180036844,-0.016152509941));
#16730=CARTESIAN_POINT('',(-0.03678899075,0.011911891549,-0.016336502043));
#16731=CARTESIAN_POINT('',(-0.036505370032,0.01198586263,-0.016480211706));
#16732=CARTESIAN_POINT('',(-0.036529183129,0.012268805633,-0.016319094869));
#16733=CARTESIAN_POINT('',(-0.036810556304,0.011926900857,-0.016366226459));
#16734=CARTESIAN_POINT('',(-0.036524605066,0.011999026208,-0.016511861903));
#16735=CARTESIAN_POINT('',(-0.036550748683,0.012285869776,-0.016352996559));
#16736=CARTESIAN_POINT('',(-0.036853337272,0.011955422756,-0.016426124399));
#16737=CARTESIAN_POINT('',(-0.036562661331,0.012023724111,-0.016575442629));
#16738=CARTESIAN_POINT('',(-0.036593529651,0.012318283097,-0.016421318697));
#16739=CARTESIAN_POINT('',(-0.036874593816,0.011968966814,-0.016456352488));
#16740=CARTESIAN_POINT('',(-0.036581516731,0.012035273907,-0.016607435016));
#16741=CARTESIAN_POINT('',(-0.036614786195,0.012333668079,-0.016455801366));
#16742=CARTESIAN_POINT('',(-0.036937968442,0.012007462527,-0.016547866518));
#16743=CARTESIAN_POINT('',(-0.03663781018,0.012067727143,-0.016704386433));
#16744=CARTESIAN_POINT('',(-0.03667816082,0.012377374469,-0.016560205216));
#16745=CARTESIAN_POINT('',(-0.03697969206,0.01203028214,-0.016609980557));
#16746=CARTESIAN_POINT('',(-0.036674489896,0.012086090141,-0.016769529197));
#16747=CARTESIAN_POINT('',(-0.036719884461,0.012403252403,-0.016631080369));
#16748=CARTESIAN_POINT('',(-0.037020900622,0.012050241607,-0.016673198758));
#16749=CARTESIAN_POINT('',(-0.036710197303,0.012101269023,-0.016834819376));
#16750=CARTESIAN_POINT('',(-0.036761093001,0.012425852784,-0.016703226885));
#16751=CARTESIAN_POINT('',(-0.0370209006219633,0.0123363218309527,-0.0165828765281445));
#16752=CARTESIAN_POINT('',(-0.0363829297000878,0.00764796150808044,-0.0180063760900247));
#16753=CARTESIAN_POINT('',(-0.0370209006725265,0.0120502416314727,-0.016673198835513));
#16754=CARTESIAN_POINT('',(-0.0367101973471479,0.0121012690417669,-0.0168348194567234));
#16755=CARTESIAN_POINT('',(-0.0367610930515268,0.0124258528117109,-0.0167032269734606));
#16756=CARTESIAN_POINT('',(-0.037103317012847,0.0120901601826742,-0.0167996340374687));
#16757=CARTESIAN_POINT('',(-0.0367834353017993,0.0121324018021573,-0.0169687333890695));
#16758=CARTESIAN_POINT('',(-0.0368435097848469,0.0124710533801557,-0.0168475194030382));
#16759=CARTESIAN_POINT('',(-0.0371836845969985,0.012118723833302,-0.0169304571286969));
#16760=CARTESIAN_POINT('',(-0.036852619292111,0.0121502141620385,-0.0171032960490522));
#16761=CARTESIAN_POINT('',(-0.0369238769759985,0.0125032416596733,-0.016996863092627));
#16762=CARTESIAN_POINT('',(-0.037301116085,0.012142960991,-0.017133757444));
#16763=CARTESIAN_POINT('',(-0.03695137278,0.012158036728,-0.017307056189));
#16764=CARTESIAN_POINT('',(-0.037041308464,0.012530204072,-0.017229010285));
#16765=CARTESIAN_POINT('',(-0.037339424126,0.012147832408,-0.017202180744));
#16766=CARTESIAN_POINT('',(-0.036983551057,0.01215730462,-0.01737562732));
#16767=CARTESIAN_POINT('',(-0.037079616505,0.012535518531,-0.017307152903));
#16768=CARTESIAN_POINT('',(-0.037413681214,0.012151009491,-0.017339044018));
#16769=CARTESIAN_POINT('',(-0.037045412802,0.012149475489,-0.017511610772));
#16770=CARTESIAN_POINT('',(-0.037153873593,0.012538634267,-0.017463477304));
#16771=CARTESIAN_POINT('',(-0.037449744946,0.012149340492,-0.017407681576));
#16772=CARTESIAN_POINT('',(-0.037075133644,0.012142279398,-0.017579166281));
#16773=CARTESIAN_POINT('',(-0.037189937325,0.012536463788,-0.017541884702));
#16774=CARTESIAN_POINT('',(-0.037519742735,0.012139323808,-0.017545357834));
#16775=CARTESIAN_POINT('',(-0.037132298021,0.012121588311,-0.017713430993));
#16776=CARTESIAN_POINT('',(-0.037259935114,0.012524478835,-0.017699177365));
#16777=CARTESIAN_POINT('',(-0.037553677068,0.012130977326,-0.017614396504));
#16778=CARTESIAN_POINT('',(-0.037159681014,0.012107993462,-0.017780075124));
#16779=CARTESIAN_POINT('',(-0.037293869447,0.012514665743,-0.017778062592));
#16780=CARTESIAN_POINT('',(-0.037602938649,0.0121131804,-0.017718254592));
#16781=CARTESIAN_POINT('',(-0.037198872381,0.012082909484,-0.01787893623));
#16782=CARTESIAN_POINT('',(-0.037343131027,0.012493905947,-0.017896748231));
#16783=CARTESIAN_POINT('',(-0.037619085386,0.012106366928,-0.017752924047));
#16784=CARTESIAN_POINT('',(-0.037211691522,0.012073695505,-0.01791189675));
#16785=CARTESIAN_POINT('',(-0.037359277765,0.012485977458,-0.017936369838));
#16786=CARTESIAN_POINT('',(-0.037650817756,0.012090910276,-0.017822364053));
#16787=CARTESIAN_POINT('',(-0.037236742776,0.012053626329,-0.017977570801));
#16788=CARTESIAN_POINT('',(-0.037391010135,0.012468026175,-0.018015733672));
#16789=CARTESIAN_POINT('',(-0.037666411882,0.012082254089,-0.017857158743));
#16790=CARTESIAN_POINT('',(-0.037248972401,0.012042747188,-0.018010293639));
#16791=CARTESIAN_POINT('',(-0.037406604261,0.012457988408,-0.018055503508));
#16792=CARTESIAN_POINT('',(-0.037742059103,0.012034811789,-0.018029350412));
#16793=CARTESIAN_POINT('',(-0.037308672836,0.011984184277,-0.018173339907));
#16794=CARTESIAN_POINT('',(-0.037482251481,0.012403043831,-0.018252328917));
#16795=CARTESIAN_POINT('',(-0.037795953594,0.0119833468,-0.018163051804));
#16796=CARTESIAN_POINT('',(-0.0373492095610001,0.01192624568,-0.018295048154));
#16797=CARTESIAN_POINT('',(-0.037536145973,0.012343640815,-0.018405198115));
#16798=CARTESIAN_POINT('',(-0.037866774638,0.011884976998,-0.018357148242));
#16799=CARTESIAN_POINT('',(-0.037401307565,0.01182386073,-0.018467879798));
#16800=CARTESIAN_POINT('',(-0.037606967016,0.012230324528,-0.018627184794));
#16801=CARTESIAN_POINT('',(-0.037888699602,0.011848634259,-0.018420763928));
#16802=CARTESIAN_POINT('',(-0.037417279271,0.011786751401,-0.018524231365));
#16803=CARTESIAN_POINT('',(-0.037628891981,0.012188489579,-0.018699952716));
#16804=CARTESIAN_POINT('',(-0.037918925522,0.011788411713,-0.018514434973));
#16805=CARTESIAN_POINT('',(-0.037439020962,0.011726989924,-0.018606332456));
#16806=CARTESIAN_POINT('',(-0.037659117901,0.012119208257,-0.018807118231));
#16807=CARTESIAN_POINT('',(-0.037928582819,0.011767311068,-0.018545460028));
#16808=CARTESIAN_POINT('',(-0.037445936687,0.011706228285,-0.018633469683));
#16809=CARTESIAN_POINT('',(-0.037668775198,0.01209494007,-0.018842615969));
#16810=CARTESIAN_POINT('',(-0.037946745879,0.011723686791,-0.018606120592));
#16811=CARTESIAN_POINT('',(-0.037458875717,0.011663774496,-0.018686340803));
#16812=CARTESIAN_POINT('',(-0.037686938258,0.012044779429,-0.018912028045));
#16813=CARTESIAN_POINT('',(-0.03795527555,0.011701127516,-0.01863582313));
#16814=CARTESIAN_POINT('',(-0.037464908394,0.011642051742,-0.018712112891));
#16815=CARTESIAN_POINT('',(-0.037695467929,0.012018845928,-0.018946019049));
#16816=CARTESIAN_POINT('',(-0.037995201404,0.011584625415,-0.018781219738));
#16817=CARTESIAN_POINT('',(-0.037493219634,0.01153014651,-0.018838837483));
#16818=CARTESIAN_POINT('',(-0.037735393783,0.011884946284,-0.019112424772));
#16819=CARTESIAN_POINT('',(-0.03801852767,0.011479690222,-0.018887669477));
#16820=CARTESIAN_POINT('',(-0.037508976952,0.011433957386,-0.018929023907));
#16821=CARTESIAN_POINT('',(-0.037758720049,0.011764426365,-0.019234309834));
#16822=CARTESIAN_POINT('',(-0.038040144091,0.011303793235,-0.019031755487));
#16823=CARTESIAN_POINT('',(-0.037523624808,0.011276525335,-0.019052132642));
#16824=CARTESIAN_POINT('',(-0.03778033647,0.011562515578,-0.019399384648));
#16825=CARTESIAN_POINT('',(-0.038045091154,0.011241659818,-0.019077372673));
#16826=CARTESIAN_POINT('',(-0.0375269479359999,0.011221473817,-0.019091228452));
#16827=CARTESIAN_POINT('',(-0.037785283533,0.011491209999,-0.019451665162));
#16828=CARTESIAN_POINT('',(-0.038050108278,0.011114326029,-0.019160771595));
#16829=CARTESIAN_POINT('',(-0.037530327064,0.011109308985,-0.019163421876));
#16830=CARTESIAN_POINT('',(-0.037790300657,0.011345109716,-0.019547286114));
#16831=CARTESIAN_POINT('',(-0.038050243047,0.011048838426,-0.019198846514));
#16832=CARTESIAN_POINT('',(-0.037530417095,0.011052089911,-0.019196655463));
#16833=CARTESIAN_POINT('',(-0.037790435426,0.011269985121,-0.019590962239));
#16834=CARTESIAN_POINT('',(-0.038045857381,0.010914292279,-0.019267887587));
#16835=CARTESIAN_POINT('',(-0.037527464034,0.01093462983,-0.019257973428));
#16836=CARTESIAN_POINT('',(-0.03778604976,0.011115665703,-0.019670206775));
#16837=CARTESIAN_POINT('',(-0.038041336883,0.010845233676,-0.019298853626));
#16838=CARTESIAN_POINT('',(-0.037524429559,0.010874566119,-0.019285974336));
#16839=CARTESIAN_POINT('',(-0.037781529262,0.011036470818,-0.019705775052));
#16840=CARTESIAN_POINT('',(-0.038027559938,0.010703495215,-0.019353576094));
#16841=CARTESIAN_POINT('',(-0.037515080889,0.010750844555,-0.019336843363));
#16842=CARTESIAN_POINT('',(-0.037767752317,0.010873951929,-0.019768689912));
#16843=CARTESIAN_POINT('',(-0.038018235775,0.010630560705,-0.019377346763));
#16844=CARTESIAN_POINT('',(-0.037508746133,0.010687144809,-0.019359690396));
#16845=CARTESIAN_POINT('',(-0.037758428154,0.010790336157,-0.019796053532));
#16846=CARTESIAN_POINT('',(-0.037983863425,0.010411968137,-0.019436057889));
#16847=CARTESIAN_POINT('',(-0.037485152239,0.010495505976,-0.019418486321));
#16848=CARTESIAN_POINT('',(-0.037724055805,0.010539762158,-0.019863756543));
#16849=CARTESIAN_POINT('',(-0.03795238138,0.010264782581,-0.019459321592));
#16850=CARTESIAN_POINT('',(-0.037463427014,0.010365206315,-0.0194459996));
#16851=CARTESIAN_POINT('',(-0.037692573758,0.010371083162,-0.019890768551));
#16852=CARTESIAN_POINT('',(-0.037902538675,0.010079089663,-0.019469374787));
#16853=CARTESIAN_POINT('',(-0.037427207905,0.010194849921,-0.0194650503));
#16854=CARTESIAN_POINT('',(-0.037642731053,0.010158316591,-0.019902820673));
#16855=CARTESIAN_POINT('',(-0.0378920119,0.010041777162,-0.019470420515));
#16856=CARTESIAN_POINT('',(-0.037419583631,0.010160752482,-0.019468052396));
#16857=CARTESIAN_POINT('',(-0.037632204279,0.010115566184,-0.019904130213));
#16858=CARTESIAN_POINT('',(-0.037870126119,0.009967782025,-0.019470585011));
#16859=CARTESIAN_POINT('',(-0.037403612981,0.010092740755,-0.019472397637));
#16860=CARTESIAN_POINT('',(-0.037610318498,0.01003079121,-0.019904547896));
#16861=CARTESIAN_POINT('',(-0.037858748966,0.009931022823,-0.019469712501));
#16862=CARTESIAN_POINT('',(-0.037395262434,0.010058774628,-0.019473761339));
#16863=CARTESIAN_POINT('',(-0.037598941345,0.009988678904,-0.019903666229));
#16864=CARTESIAN_POINT('',(-0.037823348421,0.009821438911,-0.019464328495));
#16865=CARTESIAN_POINT('',(-0.037369172913,0.009957259452,-0.01947541277));
#16866=CARTESIAN_POINT('',(-0.0375635408,0.009863142675,-0.019897861604));
#16867=CARTESIAN_POINT('',(-0.037798059306,0.009749306074,-0.019457057728));
#16868=CARTESIAN_POINT('',(-0.037350277137,0.009889495687,-0.019473344227));
#16869=CARTESIAN_POINT('',(-0.037538251684,0.009780517328,-0.019889787243));
#16870=CARTESIAN_POINT('',(-0.037744193093,0.009606821654,-0.019435479151));
#16871=CARTESIAN_POINT('',(-0.037309379895,0.00975396796899999,-0.019462636177));
#16872=CARTESIAN_POINT('',(-0.037484385472,0.009617322054,-0.019865602347));
#16873=CARTESIAN_POINT('',(-0.037715615604,0.009536470315,-0.019421170251));
#16874=CARTESIAN_POINT('',(-0.037287455068,0.00968630927800001,-0.019454099651));
#16875=CARTESIAN_POINT('',(-0.037455807983,0.00953675241,-0.019849490561));
#16876=CARTESIAN_POINT('',(-0.037670271841,0.009432272932,-0.019394506946));
#16877=CARTESIAN_POINT('',(-0.037251993154,0.009584454943,-0.019436123721));
#16878=CARTESIAN_POINT('',(-0.03741046422,0.009417432004,-0.019819385249));
#16879=CARTESIAN_POINT('',(-0.037654725402,0.009397729381,-0.019384735691));
#16880=CARTESIAN_POINT('',(-0.037239813053,0.00955062727099999,-0.01942931378));
#16881=CARTESIAN_POINT('',(-0.037394917781,0.009377876793,-0.019808341439));
#16882=CARTESIAN_POINT('',(-0.037623119912,0.009329767162,-0.019363680484));
#16883=CARTESIAN_POINT('',(-0.037214887215,0.00948368581700001,-0.019414133917));
#16884=CARTESIAN_POINT('',(-0.037363312291,0.00930005825,-0.019784524364));
#16885=CARTESIAN_POINT('',(-0.037607024828,0.009296262741,-0.019352376907));
#16886=CARTESIAN_POINT('',(-0.037202122033,0.009450493943,-0.019405766262));
#16887=CARTESIAN_POINT('',(-0.037347217206,0.009261696717,-0.019771728968));
#16888=CARTESIAN_POINT('',(-0.037525118351,0.009131050827,-0.019292111621));
#16889=CARTESIAN_POINT('',(-0.037137549676,0.009287907011,-0.019360578083));
#16890=CARTESIAN_POINT('',(-0.03726531073,0.009072543594,-0.019703469308));
#16891=CARTESIAN_POINT('',(-0.037455051799,0.009006209944,-0.019232012958));
#16892=CARTESIAN_POINT('',(-0.037080651573,0.009160611098,-0.01931215418));
#16893=CARTESIAN_POINT('',(-0.037195244178,0.008929642002,-0.01963527735));
#16894=CARTESIAN_POINT('',(-0.037343235527,0.00882937501,-0.019125190743));
#16895=CARTESIAN_POINT('',(-0.036986748025,0.008975129884,-0.019219634813));
#16896=CARTESIAN_POINT('',(-0.037083427906,0.008727272424,-0.019513936502));
#16897=CARTESIAN_POINT('',(-0.03730475018,0.008772089632,-0.019086679248));
#16898=CARTESIAN_POINT('',(-0.03695443279,0.00891491662900001,-0.019185945236));
#16899=CARTESIAN_POINT('',(-0.037044942559,0.008661723823,-0.019470171615));
#16900=CARTESIAN_POINT('',(-0.03722687049,0.008662929292,-0.019005550035));
#16901=CARTESIAN_POINT('',(-0.036888415857,0.008799116535,-0.019113533106));
#16902=CARTESIAN_POINT('',(-0.036967062869,0.008536835522,-0.01937794176));
#16903=CARTESIAN_POINT('',(-0.037187320072,0.008610791877,-0.018962790615));
#16904=CARTESIAN_POINT('',(-0.036854627768,0.008743216033,-0.019074796792));
#16905=CARTESIAN_POINT('',(-0.036927512451,0.008477195434,-0.019329315909));
#16906=CARTESIAN_POINT('',(-0.03706685504,0.008461415123,-0.018828228599));
#16907=CARTESIAN_POINT('',(-0.036751742399,0.008583033822,-0.018951988873));
#16908=CARTESIAN_POINT('',(-0.036807047419,0.008306352736,-0.019176249766));
#16909=CARTESIAN_POINT('',(-0.03698413842,0.00837115601,-0.018730193296));
#16910=CARTESIAN_POINT('',(-0.036679594089,0.008483158251,-0.018859845872));
#16911=CARTESIAN_POINT('',(-0.036724330798,0.008203164137,-0.019064679358));
#16912=CARTESIAN_POINT('',(-0.036813690053,0.008209181877,-0.018517719676));
#16913=CARTESIAN_POINT('',(-0.036528822624,0.008301119021,-0.018655023827));
#16914=CARTESIAN_POINT('',(-0.036553882432,0.008018087581,-0.018822772918));
#16915=CARTESIAN_POINT('',(-0.03672806298,0.008139470644,-0.018405905936));
#16916=CARTESIAN_POINT('',(-0.036452219097,0.00822060741400001,-0.018545456308));
#16917=CARTESIAN_POINT('',(-0.036468255359,0.007938489295,-0.018695425021));
#16918=CARTESIAN_POINT('',(-0.036556082968,0.008021465132,-0.01817201132));
#16919=CARTESIAN_POINT('',(-0.036296957641,0.00808193927900001,-0.018312490038));
#16920=CARTESIAN_POINT('',(-0.036296275347,0.00780388162,-0.018428951735));
#16921=CARTESIAN_POINT('',(-0.036469700557,0.007973146042,-0.018049892539));
#16922=CARTESIAN_POINT('',(-0.036218299035,0.008023023348,-0.018189430236));
#16923=CARTESIAN_POINT('',(-0.03620989256,0.007748843646,-0.018289782591));
#16924=CARTESIAN_POINT('',(-0.0363829297,0.007935966222,-0.017922392252));
#16925=CARTESIAN_POINT('',(-0.036137554584,0.007975350095,-0.01805745087));
#16926=CARTESIAN_POINT('',(-0.036123122079,0.007706601765,-0.018144438831));
#16927=CARTESIAN_POINT('',(-0.0387712812904561,1.29142889886801E-11,-1.90090771351648E-11));
#16928=CARTESIAN_POINT('',(-0.0363829297,0.019489230098,-0.002088447775));
#16929=CARTESIAN_POINT('',(-0.036137554584,0.019625886228,-0.002121869649));
#16930=CARTESIAN_POINT('',(-0.036123122079,0.019566845848,-0.00239810651));
#16931=CARTESIAN_POINT('',(-0.036296388628,0.019360563338,-0.002056979854));
#16932=CARTESIAN_POINT('',(-0.036059352191,0.019492100962,-0.002097943941));
#16933=CARTESIAN_POINT('',(-0.03603658062,0.019420241494,-0.00236211242));
#16934=CARTESIAN_POINT('',(-0.036211750879,0.019236205228,-0.002014072051));
#16935=CARTESIAN_POINT('',(-0.03598108599,0.019359587151,-0.002061252005));
#16936=CARTESIAN_POINT('',(-0.035951943258,0.019278561257,-0.002312976363));
#16937=CARTESIAN_POINT('',(-0.036046427611,0.01899593144,-0.001905705907));
#16938=CARTESIAN_POINT('',(-0.03582764111,0.019102466172,-0.00196200056));
#16939=CARTESIAN_POINT('',(-0.03578661999,0.019004843948,-0.002188783069));
#16940=CARTESIAN_POINT('',(-0.035965731891,0.018880003958,-0.001840264492));
#16941=CARTESIAN_POINT('',(-0.035752240428,0.018977419333,-0.001900058743));
#16942=CARTESIAN_POINT('',(-0.03570592427,0.018872794113,-0.002113745518));
#16943=CARTESIAN_POINT('',(-0.035867783855,0.018740766939,-0.001742981965));
#16944=CARTESIAN_POINT('',(-0.035659677357,0.018825445883,-0.00180418218));
#16945=CARTESIAN_POINT('',(-0.035607976234,0.018714208906,-0.002002145766));
#16946=CARTESIAN_POINT('',(-0.03584830488,0.018713153198,-0.001722699015));
#16947=CARTESIAN_POINT('',(-0.035641412325,0.018795533693,-0.001784265567));
#16948=CARTESIAN_POINT('',(-0.035588497259,0.018682758826,-0.001978875521));
#16949=CARTESIAN_POINT('',(-0.035810061793,0.018659082064,-0.0016809538));
#16950=CARTESIAN_POINT('',(-0.035605524332,0.018736905391,-0.0017430598));
#16951=CARTESIAN_POINT('',(-0.035550254172,0.018621177248,-0.001930977518));
#16952=CARTESIAN_POINT('',(-0.035791254693,0.018632563266,-0.001659452537));
#16953=CARTESIAN_POINT('',(-0.035587855191,0.018708112389,-0.001721737929));
#16954=CARTESIAN_POINT('',(-0.035531447072,0.018590975808,-0.001906305033));
#16955=CARTESIAN_POINT('',(-0.035735788251,0.018554552292,-0.001593061423));
#16956=CARTESIAN_POINT('',(-0.035535852231,0.018623571688,-0.001655788575));
#16957=CARTESIAN_POINT('',(-0.03547598063,0.018502133765,-0.001830115341));
#16958=CARTESIAN_POINT('',(-0.035700081089,0.018504601769,-0.00154628902));
#16959=CARTESIAN_POINT('',(-0.035502196601,0.018569127867,-0.001608840169));
#16960=CARTESIAN_POINT('',(-0.035440273468,0.018445251153,-0.001776431383));
#16961=CARTESIAN_POINT('',(-0.035596955729,0.01836101404,-0.001398258712));
#16962=CARTESIAN_POINT('',(-0.035405412743,0.018413252525,-0.001459938607));
#16963=CARTESIAN_POINT('',(-0.035337148108,0.018281744346,-0.001606500757));
#16964=CARTESIAN_POINT('',(-0.035533471872,0.018273557744,-0.001289394297));
#16965=CARTESIAN_POINT('',(-0.03534514464,0.018317127379,-0.001348630596));
#16966=CARTESIAN_POINT('',(-0.035273664252,0.018182166802,-0.001481497731));
#16967=CARTESIAN_POINT('',(-0.035462076716,0.01817592941,-0.001138664356));
#16968=CARTESIAN_POINT('',(-0.035277056499,0.018209299086,-0.001192172175));
#16969=CARTESIAN_POINT('',(-0.035202269094,0.018071016536,-0.001308380108));
#16970=CARTESIAN_POINT('',(-0.035448157312,0.018156936087,-0.00110767252));
#16971=CARTESIAN_POINT('',(-0.035263851039,0.018188427631,-0.001160131862));
#16972=CARTESIAN_POINT('',(-0.035188349691,0.018049393067,-0.001272783163));
#16973=CARTESIAN_POINT('',(-0.035421421576,0.018120522953,-0.001044695664));
#16974=CARTESIAN_POINT('',(-0.035238481118,0.01814840061,-0.001094908468));
#16975=CARTESIAN_POINT('',(-0.035161613954,0.018007938413,-0.001200444691));
#16976=CARTESIAN_POINT('',(-0.035408615027,0.01810311612,-0.001012747602));
#16977=CARTESIAN_POINT('',(-0.035226318844,0.018129247863,-0.001061759551));
#16978=CARTESIAN_POINT('',(-0.035148807406,0.017988121995,-0.001163745631));
#16979=CARTESIAN_POINT('',(-0.035371903227,0.018053301561,-0.000915516155));
#16980=CARTESIAN_POINT('',(-0.035191509303,0.018074518308,-0.000960895819));
#16981=CARTESIAN_POINT('',(-0.035112095605,0.01793141283,-0.001052049584));
#16982=CARTESIAN_POINT('',(-0.035349701075,0.018023292834,-0.000848849473));
#16983=CARTESIAN_POINT('',(-0.035170375015,0.018041410365,-0.000891381795));
#16984=CARTESIAN_POINT('',(-0.035089893455,0.017897252254,-0.000975458269));
#16985=CARTESIAN_POINT('',(-0.035310076825,0.017969873141,-0.000711689247));
#16986=CARTESIAN_POINT('',(-0.035132682741,0.01798250627,-0.00074809069));
#16987=CARTESIAN_POINT('',(-0.035050269204,0.01783644352,-0.000817866864));
#16988=CARTESIAN_POINT('',(-0.035292653375,0.01794646038,-0.000641196756));
#16989=CARTESIAN_POINT('',(-0.035116074086,0.017956629983,-0.000674242814));
#16990=CARTESIAN_POINT('',(-0.035032845755,0.017809793311,-0.000736867981));
#16991=CARTESIAN_POINT('',(-0.035270404132,0.017916617409,-0.000532382892));
#16992=CARTESIAN_POINT('',(-0.035094864144,0.017923641781,-0.000560006423));
#16993=CARTESIAN_POINT('',(-0.03501059651,0.017775824484,-0.00061182896));
#16994=CARTESIAN_POINT('',(-0.03526362249,0.017907532057,-0.000495486354));
#16995=CARTESIAN_POINT('',(-0.035088401673,0.017913601835,-0.000521272544));
#16996=CARTESIAN_POINT('',(-0.035003814869,0.017765483208,-0.000569429626));
#16997=CARTESIAN_POINT('',(-0.035251577427,0.017891408044,-0.000421626354));
#16998=CARTESIAN_POINT('',(-0.035076925826,0.017895786451,-0.000443697364));
#16999=CARTESIAN_POINT('',(-0.034991769806,0.017747130448,-0.000484552102));
#17000=CARTESIAN_POINT('',(-0.035246291308,0.01788433888,-0.000384573767));
#17001=CARTESIAN_POINT('',(-0.035071886429,0.017887970471,-0.000404748673));
#17002=CARTESIAN_POINT('',(-0.034986483687,0.017739084243,-0.000441971503));
#17003=CARTESIAN_POINT('',(-0.035223521483,0.017853905806,-0.00019870341));
#17004=CARTESIAN_POINT('',(-0.035050225188,0.017854392227,-0.000209670015));
#17005=CARTESIAN_POINT('',(-0.034963713862,0.017704445198,-0.000228366787));
#17006=CARTESIAN_POINT('',(-0.035216913712,0.017845112687,-4.808316E-5));
#17007=CARTESIAN_POINT('',(-0.035043883179,0.017844601077,-5.0495546E-5));
#17008=CARTESIAN_POINT('',(-0.034957106091,0.017694437363,-5.5260102E-5));
#17009=CARTESIAN_POINT('',(-0.035223876434,0.017854401084,0.000142705112));
#17010=CARTESIAN_POINT('',(-0.035050518048,0.017854867848,0.00015026669));
#17011=CARTESIAN_POINT('',(-0.034964068813,0.017705009213,0.000164006944));
#17012=CARTESIAN_POINT('',(-0.03522604562,0.017857295098,0.000181008826));
#17013=CARTESIAN_POINT('',(-0.035052587043,0.017858069693,0.000190597666));
#17014=CARTESIAN_POINT('',(-0.034966237999,0.01770830312,0.000208027982));
#17015=CARTESIAN_POINT('',(-0.035231850552,0.017865043926,0.000256731481));
#17016=CARTESIAN_POINT('',(-0.035058120997,0.017866638035,0.000270288381));
#17017=CARTESIAN_POINT('',(-0.034972042931,0.017717122731,0.00029505227));
#17018=CARTESIAN_POINT('',(-0.0352354894,0.01786990288,0.000294294755));
#17019=CARTESIAN_POINT('',(-0.035061591095,0.017872012494,0.000309815542));
#17020=CARTESIAN_POINT('',(-0.034975681779,0.01772265315,0.0003382214));
#17021=CARTESIAN_POINT('',(-0.035248550352,0.017887356278,0.000406114618));
#17022=CARTESIAN_POINT('',(-0.035074046816,0.017891317393,0.000427475545));
#17023=CARTESIAN_POINT('',(-0.034988742731,0.01774251863,0.000466726903));
#17024=CARTESIAN_POINT('',(-0.035260111701,0.017902819307,0.000479503556));
#17025=CARTESIAN_POINT('',(-0.035085080525,0.017908432544,0.000504635436));
#17026=CARTESIAN_POINT('',(-0.03500030408,0.017760118859,0.000551064032));
#17027=CARTESIAN_POINT('',(-0.035281577861,0.017931602322,0.000587901928));
#17028=CARTESIAN_POINT('',(-0.035105505104,0.017940189326,0.000618239168));
#17029=CARTESIAN_POINT('',(-0.03502177024,0.017792881061,0.000675626671));
#17030=CARTESIAN_POINT('',(-0.035289421938,0.017942130116,0.000623753285));
#17031=CARTESIAN_POINT('',(-0.035112977015,0.017951817298,0.000655825409));
#17032=CARTESIAN_POINT('',(-0.035029614317,0.017804864435,0.000716823028));
#17033=CARTESIAN_POINT('',(-0.035306476701,0.017965050902,0.000694894802));
#17034=CARTESIAN_POINT('',(-0.035129211644,0.017977114049,0.000730326682));
#17035=CARTESIAN_POINT('',(-0.03504666908,0.017830954681,0.000798568263));
#17036=CARTESIAN_POINT('',(-0.035315718145,0.017977485365,0.000730290044));
#17037=CARTESIAN_POINT('',(-0.035138009535,0.017990837846,0.000767363366));
#17038=CARTESIAN_POINT('',(-0.035055910524,0.017845108762,0.000839237874));
#17039=CARTESIAN_POINT('',(-0.035345244257,0.018017274364,0.000834778442));
#17040=CARTESIAN_POINT('',(-0.035166136457,0.018034776161,0.000876705266000001));
#17041=CARTESIAN_POINT('',(-0.035085436637,0.017890401172,0.000959292019));
#17042=CARTESIAN_POINT('',(-0.035367258146,0.018047016063,0.000902026906));
#17043=CARTESIAN_POINT('',(-0.035187092355,0.018067591645,0.000946845463));
#17044=CARTESIAN_POINT('',(-0.035107450524,0.017924257611,0.001036552565));
#17045=CARTESIAN_POINT('',(-0.035415540032,0.01811249853,0.001032054747));
#17046=CARTESIAN_POINT('',(-0.035232955499,0.018139667727,0.001082015991));
#17047=CARTESIAN_POINT('',(-0.035155732411,0.017998802798,0.001185925847));
#17048=CARTESIAN_POINT('',(-0.035441809443,0.018148241136,0.001094832722));
#17049=CARTESIAN_POINT('',(-0.035257918294,0.018179017227,0.001147092497));
#17050=CARTESIAN_POINT('',(-0.035182001822,0.018039493646,0.001258036973));
#17051=CARTESIAN_POINT('',(-0.035498359317,0.018225522805,0.001216100433));
#17052=CARTESIAN_POINT('',(-0.035311533473,0.018263877422,0.001272286645));
#17053=CARTESIAN_POINT('',(-0.035238551696,0.018127478563,0.001397318651));
#17054=CARTESIAN_POINT('',(-0.035528803299,0.018267288112,0.001274848098));
#17055=CARTESIAN_POINT('',(-0.035340397738,0.018309728944,0.001332693764));
#17056=CARTESIAN_POINT('',(-0.035268995678,0.01817503025,0.001464785336));
#17057=CARTESIAN_POINT('',(-0.035624302868,0.018398937175,0.001441946764));
#17058=CARTESIAN_POINT('',(-0.035431143853,0.018454527567,0.001504443888));
#17059=CARTESIAN_POINT('',(-0.035364495247,0.018324926454,0.001656660391));
#17060=CARTESIAN_POINT('',(-0.035693625065,0.018495301896,0.001541838752));
#17061=CARTESIAN_POINT('',(-0.035496770299,0.018560086634,0.001605426885));
#17062=CARTESIAN_POINT('',(-0.035433817443,0.018434657594,0.001771331198));
#17063=CARTESIAN_POINT('',(-0.035804878296,0.018651701588,0.001676100287));
#17064=CARTESIAN_POINT('',(-0.035600812464,0.018729153932,0.001738536628));
#17065=CARTESIAN_POINT('',(-0.035545070675,0.018612771043,0.001925410518));
#17066=CARTESIAN_POINT('',(-0.035843360668,0.01870607504,0.001718396961));
#17067=CARTESIAN_POINT('',(-0.035636958249,0.018788171317,0.001780300456));
#17068=CARTESIAN_POINT('',(-0.035583553047,0.018674696557,0.001973941769));
#17069=CARTESIAN_POINT('',(-0.035921655233,0.018817323726,0.001796776766));
#17070=CARTESIAN_POINT('',(-0.035710302083,0.018908539739,0.001856931323));
#17071=CARTESIAN_POINT('',(-0.035661847612,0.018801403665,0.002063858322));
#17072=CARTESIAN_POINT('',(-0.035961464931,0.018874192105,0.001832902387));
#17073=CARTESIAN_POINT('',(-0.035747535996,0.018969953338,0.00189179072));
#17074=CARTESIAN_POINT('',(-0.035701657309,0.018866177417,0.002105292476));
#17075=CARTESIAN_POINT('',(-0.036082708725,0.019048372444,0.001932563921));
#17076=CARTESIAN_POINT('',(-0.035861344783,0.019158636987,0.001987306041));
#17077=CARTESIAN_POINT('',(-0.035822901104,0.019064581187,0.00221957399));
#17078=CARTESIAN_POINT('',(-0.036165937985,0.019169231525,0.001987458368));
#17079=CARTESIAN_POINT('',(-0.035938765603,0.019288313365,0.002037355517));
#17080=CARTESIAN_POINT('',(-0.035906130364,0.019202261747,0.00228248524));
#17081=CARTESIAN_POINT('',(-0.036272749616,0.019326186492,0.002041954834));
#17082=CARTESIAN_POINT('',(-0.036036325391,0.019453445768,0.002083965382));
#17083=CARTESIAN_POINT('',(-0.036012941995,0.019381080036,0.002344895831));
#17084=CARTESIAN_POINT('',(-0.036294271622,0.019357902787,0.002052147118));
#17085=CARTESIAN_POINT('',(-0.036056160144,0.019487107185,0.002092585706));
#17086=CARTESIAN_POINT('',(-0.036034464001,0.019417215175,0.002356565423));
#17087=CARTESIAN_POINT('',(-0.036337241164,0.019421408713,0.002070948756));
#17088=CARTESIAN_POINT('',(-0.036095695252,0.019554376812,0.002108113551));
#17089=CARTESIAN_POINT('',(-0.036077433543,0.019489570721,0.002378086456));
#17090=CARTESIAN_POINT('',(-0.036358730845,0.019453260076,0.002079581263));
#17091=CARTESIAN_POINT('',(-0.03611543566,0.019588053885,0.00211503004));
#17092=CARTESIAN_POINT('',(-0.036098923223,0.019525861458,0.002387964418));
#17093=CARTESIAN_POINT('',(-0.036423211553,0.019549105164,0.002103217759));
#17094=CARTESIAN_POINT('',(-0.036174782484,0.019689559821,0.002133392794));
#17095=CARTESIAN_POINT('',(-0.036163403931,0.019635067732,0.002415001427));
#17096=CARTESIAN_POINT('',(-0.036466213928,0.019613389425,0.002115965485));
#17097=CARTESIAN_POINT('',(-0.036214084658,0.01975713597,0.002142252449));
#17098=CARTESIAN_POINT('',(-0.036206406307,0.019708316806,0.002429569065));
#17099=CARTESIAN_POINT('',(-0.036595254777,0.019807388917,0.002145346512));
#17100=CARTESIAN_POINT('',(-0.03633245937,0.019961690258,0.002159474874));
#17101=CARTESIAN_POINT('',(-0.036335447156,0.019929380277,0.002463096114));
#17102=CARTESIAN_POINT('',(-0.036681322249,0.019938243356,0.002153193167));
#17103=CARTESIAN_POINT('',(-0.036410235723,0.020097509831,0.00215769725));
#17104=CARTESIAN_POINT('',(-0.036421514628,0.020078502366,0.002471966356));
#17105=CARTESIAN_POINT('',(-0.03678899075,0.020103771553,0.002147749667));
#17106=CARTESIAN_POINT('',(-0.036505370032,0.020265213313,0.002139955671));
#17107=CARTESIAN_POINT('',(-0.036529183129,0.02026715354,0.002465549917));
#17108=CARTESIAN_POINT('',(-0.036810556304,0.020137018306,0.002145885901));
#17109=CARTESIAN_POINT('',(-0.036524605066,0.020299204976,0.002135530565));
#17110=CARTESIAN_POINT('',(-0.036550748683,0.020305045337,0.002463377054));
#17111=CARTESIAN_POINT('',(-0.036853337272,0.020203152393,0.00214063762));
#17112=CARTESIAN_POINT('',(-0.036562661331,0.020366616451,0.002125129214));
#17113=CARTESIAN_POINT('',(-0.036593529651,0.020380420704,0.002457286744));
#17114=CARTESIAN_POINT('',(-0.036874593816,0.020236102715,0.002137253074));
#17115=CARTESIAN_POINT('',(-0.036581516731,0.020400097569,0.002119135437));
#17116=CARTESIAN_POINT('',(-0.036614786195,0.020417976062,0.002453369195));
#17117=CARTESIAN_POINT('',(-0.036937968442,0.020334604047,0.002124834324));
#17118=CARTESIAN_POINT('',(-0.03663781018,0.020500286578,0.002098765055));
#17119=CARTESIAN_POINT('',(-0.03667816082,0.020530245644,0.002439018114));
#17120=CARTESIAN_POINT('',(-0.03697969206,0.020399806189,0.002113539669));
#17121=CARTESIAN_POINT('',(-0.036674489896,0.020565883365,0.002082096496));
#17122=CARTESIAN_POINT('',(-0.036719884461,0.020604564293,0.002425991486));
#17123=CARTESIAN_POINT('',(-0.037020900622,0.020464534491,0.002099215974));
#17124=CARTESIAN_POINT('',(-0.036710197303,0.02063001576,0.002062596704));
#17125=CARTESIAN_POINT('',(-0.036761093001,0.0206783452,0.002409490732));
#17126=CARTESIAN_POINT('',(-0.0370209006221877,0.0205293532570174,0.00239212983048223));
#17127=CARTESIAN_POINT('',(-0.0363829297001963,0.019417959879229,-0.00237985909232116));
#17128=CARTESIAN_POINT('',(-0.0370209006725265,0.0204645345703645,0.00209921595643747));
#17129=CARTESIAN_POINT('',(-0.0367101973471479,0.0206300158392919,0.00206259667989087));
#17130=CARTESIAN_POINT('',(-0.0367610930515268,0.0206783452904645,0.00240949071176802));
#17131=CARTESIAN_POINT('',(-0.037103317012847,0.0205939899421424,0.00207056883537586));
#17132=CARTESIAN_POINT('',(-0.0367834353017993,0.0207615550854043,0.00202260147516363));
#17133=CARTESIAN_POINT('',(-0.0368435097848469,0.0208259064844385,0.00237648933787403));
#17134=CARTESIAN_POINT('',(-0.0371836845969985,0.0207215678876372,0.00202989413701114));
#17135=CARTESIAN_POINT('',(-0.036852619292111,0.0208869959479472,0.00197074610137332));
#17136=CARTESIAN_POINT('',(-0.0369238769759985,0.0209713360532264,0.00232969336136768));
#17137=CARTESIAN_POINT('',(-0.037301116085,0.020909749705,0.001949233973));
#17138=CARTESIAN_POINT('',(-0.03695137278,0.021067368688,0.001875640572));
#17139=CARTESIAN_POINT('',(-0.037041308464,0.021185862625,0.002236969898));
#17140=CARTESIAN_POINT('',(-0.037339424126,0.020971441729,0.001919241095));
#17141=CARTESIAN_POINT('',(-0.036983551057,0.021126386976,0.001840720983));
#17142=CARTESIAN_POINT('',(-0.037079616505,0.021256193347,0.002202501046));
#17143=CARTESIAN_POINT('',(-0.037413681214,0.021091557342,0.001853560892));
#17144=CARTESIAN_POINT('',(-0.037045412802,0.021240237534,0.00176594903));
#17145=CARTESIAN_POINT('',(-0.037153873593,0.021393132117,0.002127037152));
#17146=CARTESIAN_POINT('',(-0.037449744946,0.021150164712,0.001817796718));
#17147=CARTESIAN_POINT('',(-0.037075133644,0.021295144276,0.001725939277));
#17148=CARTESIAN_POINT('',(-0.037189937325,0.021459949676,0.002085953763));
#17149=CARTESIAN_POINT('',(-0.037519742735,0.021264387507,0.001740283886));
#17150=CARTESIAN_POINT('',(-0.037132298021,0.021401075383,0.001640887915));
#17151=CARTESIAN_POINT('',(-0.037259935114,0.021590176641,0.001996928158));
#17152=CARTESIAN_POINT('',(-0.037553677068,0.021320003507,0.001698536285));
#17153=CARTESIAN_POINT('',(-0.037159681014,0.02145199347,0.001595792365));
#17154=CARTESIAN_POINT('',(-0.037293869447,0.021653586706,0.001948987157));
#17155=CARTESIAN_POINT('',(-0.037602938649,0.021401048787,0.001631194651));
#17156=CARTESIAN_POINT('',(-0.037198872381,0.02152506771,0.00152463845));
#17157=CARTESIAN_POINT('',(-0.037343131027,0.021745991586,0.001871665827));
#17158=CARTESIAN_POINT('',(-0.037619085386,0.02142766668,0.001607959283));
#17159=CARTESIAN_POINT('',(-0.037211691522,0.021549005368,0.00150017865));
#17160=CARTESIAN_POINT('',(-0.037359277765,0.02177634066,0.00184498875));
#17161=CARTESIAN_POINT('',(-0.037650817756,0.021480075164,0.001559853428));
#17162=CARTESIAN_POINT('',(-0.037236742776,0.021595846177,0.001449961208));
#17163=CARTESIAN_POINT('',(-0.037391010135,0.021836096115,0.001789760567));
#17164=CARTESIAN_POINT('',(-0.037666411882,0.021505880156,0.001534959604));
#17165=CARTESIAN_POINT('',(-0.037248972401,0.021618745415,0.001424178176));
#17166=CARTESIAN_POINT('',(-0.037406604261,0.02186551892,0.001761182687));
#17167=CARTESIAN_POINT('',(-0.037742059103,0.021631281365,0.001407777533));
#17168=CARTESIAN_POINT('',(-0.037308672836,0.021730666169,0.001291938074));
#17169=CARTESIAN_POINT('',(-0.037482251481,0.022008502436,0.001615186583));
#17170=CARTESIAN_POINT('',(-0.037795953594,0.021721337673,0.001296356849));
#17171=CARTESIAN_POINT('',(-0.037349209561,0.021807099305,0.001180907653));
#17172=CARTESIAN_POINT('',(-0.037536145973,0.022111189537,0.001487307464));
#17173=CARTESIAN_POINT('',(-0.037866774638,0.021840245218,0.001114117882));
#17174=CARTESIAN_POINT('',(-0.037401307565,0.021905583424,0.001005823865));
#17175=CARTESIAN_POINT('',(-0.037606967016,0.022246777496,0.001278179341));
#17176=CARTESIAN_POINT('',(-0.037888699602,0.021877166648,0.001050836305));
#17177=CARTESIAN_POINT('',(-0.037417279271,0.021935830648,0.000945510459000001));
#17178=CARTESIAN_POINT('',(-0.037628891981,0.022288878891,0.001205565251));
#17179=CARTESIAN_POINT('',(-0.037918925522,0.02192817688,0.000951846528));
#17180=CARTESIAN_POINT('',(-0.037439020962,0.02197705154,0.000852704956));
#17181=CARTESIAN_POINT('',(-0.037659117901,0.022347046289,0.001091983109));
#17182=CARTESIAN_POINT('',(-0.037928582819,0.021944495043,0.000918060305));
#17183=CARTESIAN_POINT('',(-0.037445936687,0.021990172249,0.000821156235));
#17184=CARTESIAN_POINT('',(-0.037668775198,0.022365654138,0.001053217373));
#17185=CARTESIAN_POINT('',(-0.037946745879,0.021975216494,0.000849950291));
#17186=CARTESIAN_POINT('',(-0.037458875717,0.022014733087,0.000757954616));
#17187=CARTESIAN_POINT('',(-0.037686938258,0.022400686439,0.000975070946));
#17188=CARTESIAN_POINT('',(-0.03795527555,0.021989660009,0.000815562116));
#17189=CARTESIAN_POINT('',(-0.037464908394,0.022026190993,0.000726256116));
#17190=CARTESIAN_POINT('',(-0.037695467929,0.022417156761,0.000935616373));
#17191=CARTESIAN_POINT('',(-0.037995201404,0.022057326114,0.000641970034));
#17192=CARTESIAN_POINT('',(-0.037493219634,0.022079985093,0.000565981045));
#17193=CARTESIAN_POINT('',(-0.037735393783,0.022494318522,0.000736453018));
#17194=CARTESIAN_POINT('',(-0.03801852767,0.022097046697,0.000497868621));
#17195=CARTESIAN_POINT('',(-0.037508976952,0.022109994265,0.000437585608));
#17196=CARTESIAN_POINT('',(-0.037758720049,0.022539614123,0.000571137177));
#17197=CARTESIAN_POINT('',(-0.038040144091,0.022133880348,0.000273494358));
#17198=CARTESIAN_POINT('',(-0.037523624808,0.022137893532,0.000239691086));
#17199=CARTESIAN_POINT('',(-0.03778033647,0.022581617712,0.000313739898));
#17200=CARTESIAN_POINT('',(-0.038045091154,0.022142319282,0.000196876647));
#17201=CARTESIAN_POINT('',(-0.037526947936,0.022144225738,0.000172467167));
#17202=CARTESIAN_POINT('',(-0.037785283533,0.022591241175,0.000225847199));
#17203=CARTESIAN_POINT('',(-0.038050108278,0.022150877972,4.490289E-5));
#17204=CARTESIAN_POINT('',(-0.037530327064,0.02215066466,3.9232862E-5));
#17205=CARTESIAN_POINT('',(-0.037790300657,0.022601001208,5.1510166E-5));
#17206=CARTESIAN_POINT('',(-0.038050243047,0.022151108018,-3.0848498E-5));
#17207=CARTESIAN_POINT('',(-0.037530417095,0.022150836255,-2.6937103E-5));
#17208=CARTESIAN_POINT('',(-0.037790435426,0.022601263544,-3.5387705E-5));
#17209=CARTESIAN_POINT('',(-0.038045857381,0.022143626267,-0.000181889416));
#17210=CARTESIAN_POINT('',(-0.037527464034,0.022145209129,-0.0001593195));
#17211=CARTESIAN_POINT('',(-0.03778604976,0.022592731617,-0.000208654509));
#17212=CARTESIAN_POINT('',(-0.038041336883,0.022135914342,-0.000257178939));
#17213=CARTESIAN_POINT('',(-0.037524429559,0.022139426771,-0.000225336654));
#17214=CARTESIAN_POINT('',(-0.037781529262,0.022583937206,-0.00029502343));
#17215=CARTESIAN_POINT('',(-0.038027559938,0.022112436159,-0.000407289281));
#17216=CARTESIAN_POINT('',(-0.037515080889,0.022121619859,-0.000357917185));
#17217=CARTESIAN_POINT('',(-0.037767752317,0.022557163628,-0.000467226346));
#17218=CARTESIAN_POINT('',(-0.038018235775,0.022096554907,-0.000482337755));
#17219=CARTESIAN_POINT('',(-0.037508746133,0.022109556097,-0.0004245063));
#17220=CARTESIAN_POINT('',(-0.037758428154,0.022539053331,-0.000553321539));
#17221=CARTESIAN_POINT('',(-0.037983863425,0.02203810395,-0.000701000035));
#17222=CARTESIAN_POINT('',(-0.037485152239,0.022064655445,-0.00061986836));
#17223=CARTESIAN_POINT('',(-0.037724055805,0.02247239886,-0.000804176493));
#17224=CARTESIAN_POINT('',(-0.03795238138,0.02198465813,-0.000840098316));
#17225=CARTESIAN_POINT('',(-0.037463427014,0.022023332813,-0.000746467815999999));
#17226=CARTESIAN_POINT('',(-0.037692573758,0.022411452447,-0.000963762793));
#17227=CARTESIAN_POINT('',(-0.037902538675,0.021900517993,-0.001005939698));
#17228=CARTESIAN_POINT('',(-0.037427207905,0.021954653006,-0.000903526131000001));
#17229=CARTESIAN_POINT('',(-0.037642731053,0.022315506605,-0.001154050109));
#17230=CARTESIAN_POINT('',(-0.0378920119,0.021882767369,-0.001038776136));
#17231=CARTESIAN_POINT('',(-0.037419583631,0.021940204178,-0.000934556427));
#17232=CARTESIAN_POINT('',(-0.037632204279,0.022295265496,-0.001191727817));
#17233=CARTESIAN_POINT('',(-0.037870126119,0.021845912259,-0.001102940053));
#17234=CARTESIAN_POINT('',(-0.037403612981,0.021909961403,-0.000995628931000001));
#17235=CARTESIAN_POINT('',(-0.037610318498,0.022253239734,-0.00126535394));
#17236=CARTESIAN_POINT('',(-0.037858748966,0.021826777042,-0.001134338201));
#17237=CARTESIAN_POINT('',(-0.037395262434,0.02189415934,-0.001025726311));
#17238=CARTESIAN_POINT('',(-0.037598941345,0.022231420035,-0.001301383433));
#17239=CARTESIAN_POINT('',(-0.037823348421,0.0217673224,-0.001226548649));
#17240=CARTESIAN_POINT('',(-0.037369172913,0.021844831934,-0.001114466748));
#17241=CARTESIAN_POINT('',(-0.0375635408,0.022163624967,-0.001407198685));
#17242=CARTESIAN_POINT('',(-0.037798059306,0.021724959312,-0.001285382135));
#17243=CARTESIAN_POINT('',(-0.037350277137,0.02180915864,-0.001172117618));
#17244=CARTESIAN_POINT('',(-0.037538251684,0.022115319692,-0.001474717154));
#17245=CARTESIAN_POINT('',(-0.037744193093,0.021635029507,-0.001397987973));
#17246=CARTESIAN_POINT('',(-0.037309379895,0.021732121338,-0.001284134039));
#17247=CARTESIAN_POINT('',(-0.037484385472,0.022012777321,-0.001603955958));
#17248=CARTESIAN_POINT('',(-0.037715615604,0.021587461967,-0.00145175957));
#17249=CARTESIAN_POINT('',(-0.037287455068,0.021690899144,-0.001338459922));
#17250=CARTESIAN_POINT('',(-0.037455807983,0.021958539283,-0.001665675424));
#17251=CARTESIAN_POINT('',(-0.037670271841,0.021512272175,-0.001528665498));
#17252=CARTESIAN_POINT('',(-0.037251993154,0.021624404365,-0.001417680399));
#17253=CARTESIAN_POINT('',(-0.03741046422,0.021872807115,-0.001753957271));
#17254=CARTESIAN_POINT('',(-0.037654725402,0.021486538245,-0.001553695464));
#17255=CARTESIAN_POINT('',(-0.037239813053,0.021601592947,-0.001443571051));
#17256=CARTESIAN_POINT('',(-0.037394917781,0.021843465289,-0.001782691183));
#17257=CARTESIAN_POINT('',(-0.037623119912,0.02143432279,-0.001602024868));
#17258=CARTESIAN_POINT('',(-0.037214887215,0.021554976073,-0.00149395412));
#17259=CARTESIAN_POINT('',(-0.037363312291,0.021783929826,-0.001838175481));
#17260=CARTESIAN_POINT('',(-0.037607024828,0.021407781395,-0.001625388759));
#17261=CARTESIAN_POINT('',(-0.037202122033,0.021531133535,-0.001518515298));
#17262=CARTESIAN_POINT('',(-0.037347217206,0.021753667921,-0.001864999845));
#17263=CARTESIAN_POINT('',(-0.037525118351,0.02127298417,-0.001738333831));
#17264=CARTESIAN_POINT('',(-0.037137549676,0.021410705958,-0.001636725622));
#17265=CARTESIAN_POINT('',(-0.03726531073,0.02159997676,-0.001994681424));
#17266=CARTESIAN_POINT('',(-0.037455051799,0.02115851676,-0.001816399876));
#17267=CARTESIAN_POINT('',(-0.037080651573,0.021305121671,-0.001722755165));
#17268=CARTESIAN_POINT('',(-0.037195244178,0.021469469996,-0.002084341855));
#17269=CARTESIAN_POINT('',(-0.037343235527,0.020977588541,-0.001916132313));
#17270=CARTESIAN_POINT('',(-0.036986748025,0.021132256941,-0.001837126924));
#17271=CARTESIAN_POINT('',(-0.037083427906,0.021263200951,-0.002198928626));
#17272=CARTESIAN_POINT('',(-0.03730475018,0.020915593919,-0.001946487158));
#17273=CARTESIAN_POINT('',(-0.03695443279,0.021072974284,-0.001872428345));
#17274=CARTESIAN_POINT('',(-0.037044942559,0.021192525146,-0.002233812936));
#17275=CARTESIAN_POINT('',(-0.03722687049,0.020790753789,-0.002000458179));
#17276=CARTESIAN_POINT('',(-0.036888415857,0.020952363493,-0.001936508103));
#17277=CARTESIAN_POINT('',(-0.036967062869,0.021050207598,-0.00229585445));
#17278=CARTESIAN_POINT('',(-0.037187320072,0.020727654338,-0.002024230796));
#17279=CARTESIAN_POINT('',(-0.036854627768,0.020890866611,-0.001965551201));
#17280=CARTESIAN_POINT('',(-0.036927512451,0.020978276332,-0.002323191356));
#17281=CARTESIAN_POINT('',(-0.03706685504,0.020536431836,-0.002086313851));
#17282=CARTESIAN_POINT('',(-0.036751742399,0.020704420727,-0.002042869105));
#17283=CARTESIAN_POINT('',(-0.036807047419,0.020760295815,-0.0023946124));
#17284=CARTESIAN_POINT('',(-0.03698413842,0.020406401217,-0.002115462885));
#17285=CARTESIAN_POINT('',(-0.036679594089,0.020574684762,-0.002083292386));
#17286=CARTESIAN_POINT('',(-0.036724330798,0.020612078707,-0.002428191144));
#17287=CARTESIAN_POINT('',(-0.036813690053,0.020141406598,-0.002149499788));
#17288=CARTESIAN_POINT('',(-0.036528822624,0.020306284053,-0.002138531962));
#17289=CARTESIAN_POINT('',(-0.036553882432,0.020310043308,-0.002467518924));
#17290=CARTESIAN_POINT('',(-0.03672806298,0.020009717442,-0.002153964617));
#17291=CARTESIAN_POINT('',(-0.036452219097,0.020171139995,-0.002153473299));
#17292=CARTESIAN_POINT('',(-0.036468255359,0.020159957651,-0.002472779113));
#17293=CARTESIAN_POINT('',(-0.036556082968,0.019748156007,-0.00213921308));
#17294=CARTESIAN_POINT('',(-0.036296957641,0.019900051219,-0.002157080292));
#17295=CARTESIAN_POINT('',(-0.036296275347,0.019861881178,-0.002456116136));
#17296=CARTESIAN_POINT('',(-0.036469700557,0.019618238496,-0.002119999249));
#17297=CARTESIAN_POINT('',(-0.036218299035,0.019764020339,-0.002146573084));
#17298=CARTESIAN_POINT('',(-0.03620989256,0.019713838176,-0.002434195848));
#17299=CARTESIAN_POINT('',(-0.0363829297,0.019489230098,-0.002088447775));
#17300=CARTESIAN_POINT('',(-0.036137554584,0.019625886228,-0.002121869649));
#17301=CARTESIAN_POINT('',(-0.036123122079,0.019566845848,-0.00239810651));
#17302=CARTESIAN_POINT('',(-0.0387712812776768,1.75917299243037E-11,-4.54757954297462E-17));
#17303=CARTESIAN_POINT('',(-0.0385114725585428,0.0237182560306759,0.00250334555505273));
#17304=CARTESIAN_POINT('',(-0.0385732886842286,0.0238313054539707,0.00245233227695023));
#17305=CARTESIAN_POINT('',(-0.0386752801539392,0.0238844424604606,0.00235430274800211));
#17306=CARTESIAN_POINT('',(-0.0387712812922245,0.0238935321467088,0.00225812345823692));
#17307=CARTESIAN_POINT('',(-0.087860759494,0.023594862995,0.002229896915));
#17308=CARTESIAN_POINT('',(-0.0363829297,0.011553263876,0.015833944478));
#17309=CARTESIAN_POINT('',(-0.036137554584,0.011650536133,0.015935581221));
#17310=CARTESIAN_POINT('',(-0.036123122079,0.011860244082,0.015746332321));
#17311=CARTESIAN_POINT('',(-0.036296388628,0.011461678478,0.015738249755));
#17312=CARTESIAN_POINT('',(-0.036059352191,0.01156292323,0.015831682636));
#17313=CARTESIAN_POINT('',(-0.03603658062,0.011755770109,0.015637366271));
#17314=CARTESIAN_POINT('',(-0.036211750879,0.011362340175,0.015652006375));
#17315=CARTESIAN_POINT('',(-0.03598108599,0.011464890175,0.015735268277));
#17316=CARTESIAN_POINT('',(-0.035951943258,0.011642376917,0.015539235616));
#17317=CARTESIAN_POINT('',(-0.036046427611,0.011148355448,0.015498106242));
#17318=CARTESIAN_POINT('',(-0.03582764111,0.011250375413,0.0155622207));
#17319=CARTESIAN_POINT('',(-0.03578661999,0.011397963715,0.015364286119));
#17320=CARTESIAN_POINT('',(-0.035965731891,0.011033717779,0.015430430805));
#17321=CARTESIAN_POINT('',(-0.035752240428,0.011134208806,0.015484897869));
#17322=CARTESIAN_POINT('',(-0.03570592427,0.011266954373,0.015287446383));
#17323=CARTESIAN_POINT('',(-0.035867783855,0.01087985013,0.015358489273));
#17324=CARTESIAN_POINT('',(-0.035659677357,0.010975190542,0.015401223282));
#17325=CARTESIAN_POINT('',(-0.035607976234,0.011091013549,0.015205907441));
#17326=CARTESIAN_POINT('',(-0.03584830488,0.010848477709,0.015344716547));
#17327=CARTESIAN_POINT('',(-0.035641412325,0.010942986155,0.015385276872));
#17328=CARTESIAN_POINT('',(-0.035588497259,0.011055135885,0.015190305996));
#17329=CARTESIAN_POINT('',(-0.035810061793,0.010785289725,0.015318762179));
#17330=CARTESIAN_POINT('',(-0.035605524332,0.010877986763,0.015355106157));
#17331=CARTESIAN_POINT('',(-0.035550254172,0.010982864209,0.015160923786));
#17332=CARTESIAN_POINT('',(-0.035791254693,0.010753409687,0.015306546858));
#17333=CARTESIAN_POINT('',(-0.035587855191,0.01084512498,0.015340831622));
#17334=CARTESIAN_POINT('',(-0.035531447072,0.01094639649,0.015147104814));
#17335=CARTESIAN_POINT('',(-0.035735788251,0.010656907808,0.015272182929));
#17336=CARTESIAN_POINT('',(-0.035535852231,0.010745740813,0.015300591903));
#17337=CARTESIAN_POINT('',(-0.03547598063,0.01083599326,0.015108260194));
#17338=CARTESIAN_POINT('',(-0.035700081089,0.010591426457,0.015252310709));
#17339=CARTESIAN_POINT('',(-0.035502196601,0.010677860391,0.015276916375));
#17340=CARTESIAN_POINT('',(-0.035440273468,0.010761060282,0.015085840387));
#17341=CARTESIAN_POINT('',(-0.035596955729,0.010391434585,0.015201975242));
#17342=CARTESIAN_POINT('',(-0.035405412743,0.010470970184,0.015216375149));
#17343=CARTESIAN_POINT('',(-0.035337148108,0.01053214264,0.01502920465));
#17344=CARTESIAN_POINT('',(-0.035533471872,0.010253427089,0.015180668075));
#17345=CARTESIAN_POINT('',(-0.03534514464,0.010326512046,0.015188782336));
#17346=CARTESIAN_POINT('',(-0.035273664252,0.010374098072,0.015005469481));
#17347=CARTESIAN_POINT('',(-0.035462076716,0.010074076964,0.015171484429));
#17348=CARTESIAN_POINT('',(-0.035277056499,0.010137100933,0.015173629506));
#17349=CARTESIAN_POINT('',(-0.035202269094,0.01016859868,0.014995769339));
#17350=CARTESIAN_POINT('',(-0.035448157312,0.010037740585,0.015170531646));
#17351=CARTESIAN_POINT('',(-0.035263851039,0.01009891748,0.015171574453));
#17352=CARTESIAN_POINT('',(-0.035188349691,0.010126959086,0.014994841338));
#17353=CARTESIAN_POINT('',(-0.035421421576,0.009964994461,0.015170485375));
#17354=CARTESIAN_POINT('',(-0.035238481118,0.010022418853,0.015169521732));
#17355=CARTESIAN_POINT('',(-0.035161613954,0.010043584805,0.01499510979));
#17356=CARTESIAN_POINT('',(-0.035408615027,0.009928623211,0.015171384646));
#17357=CARTESIAN_POINT('',(-0.035226318844,0.009984134676,0.015169509426));
#17358=CARTESIAN_POINT('',(-0.035148807406,0.010001894278,0.014996297799));
#17359=CARTESIAN_POINT('',(-0.035371903227,0.009819511029,0.015176859697));
#17360=CARTESIAN_POINT('',(-0.035191509303,0.009869419344,0.015172544106));
#17361=CARTESIAN_POINT('',(-0.035112095605,0.00987680808,0.015003034244));
#17362=CARTESIAN_POINT('',(-0.035349701075,0.009746771624,0.015184204718));
#17363=CARTESIAN_POINT('',(-0.035170375015,0.009792664461,0.015178628799));
#17364=CARTESIAN_POINT('',(-0.035089893455,0.009793397768,0.015011745976));
#17365=CARTESIAN_POINT('',(-0.035310076825,0.009601277538,0.015206522019));
#17366=CARTESIAN_POINT('',(-0.035132682741,0.009639118677,0.015199261909));
#17367=CARTESIAN_POINT('',(-0.035050269204,0.009626515241,0.01503787977));
#17368=CARTESIAN_POINT('',(-0.035292653375,0.00952852287,0.015221492219));
#17369=CARTESIAN_POINT('',(-0.035116074086,0.009562226397,0.015213776324));
#17370=CARTESIAN_POINT('',(-0.035032845755,0.009543043046,0.015055299453));
#17371=CARTESIAN_POINT('',(-0.035270404132,0.009419365813,0.015250054381));
#17372=CARTESIAN_POINT('',(-0.035094864144,0.00944680067900001,0.015242325899));
#17373=CARTESIAN_POINT('',(-0.03501059651,0.009417771664,0.015088401097));
#17374=CARTESIAN_POINT('',(-0.03526362249,0.009382869798,0.015260634503));
#17375=CARTESIAN_POINT('',(-0.035088401673,0.009408236182,0.01525299799));
#17376=CARTESIAN_POINT('',(-0.035003814869,0.009375882126,0.015100644955));
#17377=CARTESIAN_POINT('',(-0.035251577427,0.009310843156,0.015283600698));
#17378=CARTESIAN_POINT('',(-0.035076925826,0.009332146415,0.015276357005));
#17379=CARTESIAN_POINT('',(-0.034991769806,0.009293199654,0.015127189761));
#17380=CARTESIAN_POINT('',(-0.035246291308,0.009275220092,0.015296004916));
#17381=CARTESIAN_POINT('',(-0.035071886429,0.009294507868,0.015289062514));
#17382=CARTESIAN_POINT('',(-0.034986483687,0.009252300671,0.015141511843));
#17383=CARTESIAN_POINT('',(-0.035223521483,0.009099035104,0.015362584279));
#17384=CARTESIAN_POINT('',(-0.035050225188,0.009108775673,0.01535752223));
#17385=CARTESIAN_POINT('',(-0.034963713862,0.009049994038,0.015218315908));
#17386=CARTESIAN_POINT('',(-0.035216913712,0.008964197582,0.015430279341));
#17387=CARTESIAN_POINT('',(-0.035043883179,0.008966030964,0.01542863008));
#17388=CARTESIAN_POINT('',(-0.034957106091,0.008895075333,0.015296202211));
#17389=CARTESIAN_POINT('',(-0.035223876434,0.00880361429,0.015533717464));
#17390=CARTESIAN_POINT('',(-0.035050518048,0.008797299153,0.015537902482));
#17391=CARTESIAN_POINT('',(-0.034964068813,0.008710470427,0.015414991225));
#17392=CARTESIAN_POINT('',(-0.03522604562,0.008771889308,0.015555375611));
#17393=CARTESIAN_POINT('',(-0.035052587043,0.008763972426,0.01556084085));
#17394=CARTESIAN_POINT('',(-0.034966237999,0.008673994043,0.015439854351));
#17395=CARTESIAN_POINT('',(-0.035231850552,0.008710185979,0.01559994762));
#17396=CARTESIAN_POINT('',(-0.035058120997,0.008699242413,0.015608106609));
#17397=CARTESIAN_POINT('',(-0.034972042931,0.008603038604,0.015491004502));
#17398=CARTESIAN_POINT('',(-0.0352354894,0.008680084706,0.015622937235));
#17399=CARTESIAN_POINT('',(-0.035061591095,0.00866769811700001,0.015632524608));
#17400=CARTESIAN_POINT('',(-0.034975681779,0.008568418251,0.01551737855));
#17401=CARTESIAN_POINT('',(-0.035248550352,0.008591972563,0.015693962252));
#17402=CARTESIAN_POINT('',(-0.035074046816,0.00857545401500001,0.015708073142));
#17403=CARTESIAN_POINT('',(-0.034988742731,0.008467061961,0.015598835312));
#17404=CARTESIAN_POINT('',(-0.035260111701,0.008536147393,0.015744048097));
#17405=CARTESIAN_POINT('',(-0.035085080525,0.008517189165,0.015761475243));
#17406=CARTESIAN_POINT('',(-0.03500030408,0.008402823979,0.015656246123));
#17407=CARTESIAN_POINT('',(-0.035281577861,0.008456663156,0.015823174106));
#17408=CARTESIAN_POINT('',(-0.035105505104,0.008434683838,0.015845779289));
#17409=CARTESIAN_POINT('',(-0.03502177024,0.00831133067,0.015746900341));
#17410=CARTESIAN_POINT('',(-0.035289421938,0.008430878868,0.015850217121));
#17411=CARTESIAN_POINT('',(-0.035112977015,0.008407947185,0.015874642529));
#17412=CARTESIAN_POINT('',(-0.035029614317,0.008281645265,0.015777876425));
#17413=CARTESIAN_POINT('',(-0.035306476701,0.008380728899,0.015905637862));
#17414=CARTESIAN_POINT('',(-0.035129211644,0.008356075565,0.015933800795));
#17415=CARTESIAN_POINT('',(-0.03504666908,0.008223896938,0.015841343859));
#17416=CARTESIAN_POINT('',(-0.035315718145,0.008356292952,0.015934104044));
#17417=CARTESIAN_POINT('',(-0.035138009535,0.008330862754,0.015964204293));
#17418=CARTESIAN_POINT('',(-0.035055910524,0.008195753062,0.015873936458));
#17419=CARTESIAN_POINT('',(-0.035345244257,0.008285697845,0.016020806527));
#17420=CARTESIAN_POINT('',(-0.035166136457,0.008258139049,0.01605692694));
#17421=CARTESIAN_POINT('',(-0.035085436637,0.008114429329,0.015973187908));
#17422=CARTESIAN_POINT('',(-0.035367258146,0.008242329816,0.016080187826));
#17423=CARTESIAN_POINT('',(-0.035187092355,0.00821380359800001,0.016120416082));
#17424=CARTESIAN_POINT('',(-0.035107450524,0.008064447951,0.016041138718));
#17425=CARTESIAN_POINT('',(-0.035415540032,0.008162463636,0.016201911227));
#17426=CARTESIAN_POINT('',(-0.035232955499,0.008132780528,0.016250421064));
#17427=CARTESIAN_POINT('',(-0.035155732411,0.007972359488,0.016180383385));
#17428=CARTESIAN_POINT('',(-0.035441809443,0.008125967618,0.016264254219));
#17429=CARTESIAN_POINT('',(-0.035257918294,0.008096097371,0.016317036983));
#17430=CARTESIAN_POINT('',(-0.035182001822,0.007930254845,0.016251678255));
#17431=CARTESIAN_POINT('',(-0.035498359317,0.008059587534,0.016391815963));
#17432=CARTESIAN_POINT('',(-0.035311533473,0.00803010615599999,0.016453125142));
#17433=CARTESIAN_POINT('',(-0.035238551696,0.007853625833,0.016397516267));
#17434=CARTESIAN_POINT('',(-0.035528803299,0.008029593217,0.016457359612));
#17435=CARTESIAN_POINT('',(-0.035340397738,0.008000717817,0.016523037284));
#17436=CARTESIAN_POINT('',(-0.035268995678,0.007818973813,0.016472430579));
#17437=CARTESIAN_POINT('',(-0.035624302868,0.007950706059,0.016654920378));
#17438=CARTESIAN_POINT('',(-0.035431143853,0.00792437715800001,0.016734311632));
#17439=CARTESIAN_POINT('',(-0.035364495247,0.007727753242,0.016698182027));
#17440=CARTESIAN_POINT('',(-0.035693625065,0.00791237942,0.016788320669));
#17441=CARTESIAN_POINT('',(-0.035496770299,0.007889702851,0.016876219964));
#17442=CARTESIAN_POINT('',(-0.035433817443,0.007683310981,0.016850547386));
#17443=CARTESIAN_POINT('',(-0.035804878296,0.007874305366,0.016990897542));
#17444=CARTESIAN_POINT('',(-0.035600812464,0.007858960081,0.01708919141));
#17445=CARTESIAN_POINT('',(-0.035545070675,0.0076389311,0.017081837817));
#17446=CARTESIAN_POINT('',(-0.035843360668,0.007864862098,0.01705913467));
#17447=CARTESIAN_POINT('',(-0.035636958249,0.007852300237,0.017161183879));
#17448=CARTESIAN_POINT('',(-0.035583553047,0.007627864561,0.017159732511));
#17449=CARTESIAN_POINT('',(-0.035921655233,0.007852607539,0.017194668761));
#17450=CARTESIAN_POINT('',(-0.035710302083,0.00784612017,0.017303741424));
#17451=CARTESIAN_POINT('',(-0.035661847612,0.007613348096,0.017314422362));
#17452=CARTESIAN_POINT('',(-0.035961464931,0.007849756022,0.017261981032));
#17453=CARTESIAN_POINT('',(-0.035747535996,0.007846637847,0.017374356859));
#17454=CARTESIAN_POINT('',(-0.035701657309,0.007609851942,0.017391235154));
#17455=CARTESIAN_POINT('',(-0.036082708725,0.007850536771,0.017462656398));
#17456=CARTESIAN_POINT('',(-0.035861344783,0.007858260977,0.017585519353));
#17457=CARTESIAN_POINT('',(-0.035822901104,0.007610083132,0.017620198615));
#17458=CARTESIAN_POINT('',(-0.036165937985,0.007863426326,0.017594770655));
#17459=CARTESIAN_POINT('',(-0.035938765603,0.00787975504900001,0.017722847129));
#17460=CARTESIAN_POINT('',(-0.035906130364,0.007624440672,0.017770889103));
#17461=CARTESIAN_POINT('',(-0.036272749616,0.007894708486,0.017757945878));
#17462=CARTESIAN_POINT('',(-0.036036325391,0.00792195592300001,0.017889160917));
#17463=CARTESIAN_POINT('',(-0.036012941995,0.007659800659,0.017956955579));
#17464=CARTESIAN_POINT('',(-0.036294271622,0.007901739857,0.017790509137));
#17465=CARTESIAN_POINT('',(-0.036056160144,0.007931321211,0.017922622722));
#17466=CARTESIAN_POINT('',(-0.036034464001,0.007667762066,0.017994084324));
#17467=CARTESIAN_POINT('',(-0.036337241164,0.007917210124,0.017854907701));
#17468=CARTESIAN_POINT('',(-0.036095695252,0.00795150851699999,0.01798864385));
#17469=CARTESIAN_POINT('',(-0.036077433543,0.007685302077,0.018067506581));
#17470=CARTESIAN_POINT('',(-0.036358730845,0.007925659835,0.017886808044));
#17471=CARTESIAN_POINT('',(-0.03611543566,0.00796235719799999,0.018021267296));
#17472=CARTESIAN_POINT('',(-0.036098923223,0.00769489288,0.018103874262));
#17473=CARTESIAN_POINT('',(-0.036423211553,0.007953112573,0.017981630573));
#17474=CARTESIAN_POINT('',(-0.036174782484,0.007997207555,0.018118355391));
#17475=CARTESIAN_POINT('',(-0.036163403931,0.00772608128,0.018211968175));
#17476=CARTESIAN_POINT('',(-0.036466213928,0.007974214849,0.018043676239));
#17477=CARTESIAN_POINT('',(-0.036214084658,0.008023322943,0.01818130788));
#17478=CARTESIAN_POINT('',(-0.036206406307,0.007750089872,0.018282687553));
#17479=CARTESIAN_POINT('',(-0.036595254777,0.008045769879,0.018226375241));
#17480=CARTESIAN_POINT('',(-0.03633245937,0.00811068502900001,0.018367068303));
#17481=CARTESIAN_POINT('',(-0.036335447156,0.007831586332,0.018490897658));
#17482=CARTESIAN_POINT('',(-0.036681322249,0.008104401696,0.018343621837));
#17483=CARTESIAN_POINT('',(-0.036410235723,0.00818013428299999,0.018483802691));
#17484=CARTESIAN_POINT('',(-0.036421514628,0.007898465521,0.018624476296));
#17485=CARTESIAN_POINT('',(-0.03678899075,0.008191880004,0.01848425171));
#17486=CARTESIAN_POINT('',(-0.036505370032,0.008279350682,0.018620167377));
#17487=CARTESIAN_POINT('',(-0.036529183129,0.007998347907,0.018784644787));
#17488=CARTESIAN_POINT('',(-0.036810556304,0.008210117449,0.01851211236));
#17489=CARTESIAN_POINT('',(-0.036524605066,0.00830017876799999,0.018647392468));
#17490=CARTESIAN_POINT('',(-0.036550748683,0.00801917556,0.018816373614));
#17491=CARTESIAN_POINT('',(-0.036853337272,0.008247729637,0.018566762019));
#17492=CARTESIAN_POINT('',(-0.036562661331,0.00834289234,0.018700571843));
#17493=CARTESIAN_POINT('',(-0.036593529651,0.008062137607,0.018878605442));
#17494=CARTESIAN_POINT('',(-0.036874593816,0.008267135902,0.018593605562));
#17495=CARTESIAN_POINT('',(-0.036581516731,0.008364823662,0.018726570453));
#17496=CARTESIAN_POINT('',(-0.036614786195,0.008084307983,0.018909170561));
#17497=CARTESIAN_POINT('',(-0.036937968442,0.00832714152,0.018672700842));
#17498=CARTESIAN_POINT('',(-0.03663781018,0.008432559434,0.018803151489));
#17499=CARTESIAN_POINT('',(-0.03667816082,0.008152871175,0.01899922333));
#17500=CARTESIAN_POINT('',(-0.03697969206,0.008369524049,0.018723520226));
#17501=CARTESIAN_POINT('',(-0.036674489896,0.00847979322399999,0.018851625693));
#17502=CARTESIAN_POINT('',(-0.036719884461,0.00820131189,0.019057071854));
#17503=CARTESIAN_POINT('',(-0.037020900622,0.008414292884,0.018772414733));
#17504=CARTESIAN_POINT('',(-0.036710197303,0.008528746736,0.01889741608));
#17505=CARTESIAN_POINT('',(-0.036761093001,0.008252492416,0.019112717618));
#17506=CARTESIAN_POINT('',(-0.0370209006225329,0.00819303142614902,0.0189750063603988));
#17507=CARTESIAN_POINT('',(-0.036382929700134,0.0117699983702051,0.0156265169988629));
#17508=CARTESIAN_POINT('',(-0.0370209006725265,0.00841429293889186,0.0187724147929504));
#17509=CARTESIAN_POINT('',(-0.0367101973471479,0.00852874679652508,0.0188974161366142));
#17510=CARTESIAN_POINT('',(-0.0367610930515268,0.00825249247875368,0.0191127176862286));
#17511=CARTESIAN_POINT('',(-0.037103317012847,0.00850382975946811,0.0188702028728446));
#17512=CARTESIAN_POINT('',(-0.0367834353017993,0.00862915328424696,0.0189913348642332));
#17513=CARTESIAN_POINT('',(-0.0368435097848469,0.00835485310428282,0.0192240087409122));
#17514=CARTESIAN_POINT('',(-0.0371836845969985,0.00860284405433526,0.018960351265708));
#17515=CARTESIAN_POINT('',(-0.036852619292111,0.00873678178590861,0.0190740421504255));
#17516=CARTESIAN_POINT('',(-0.0369238769759985,0.0084680943925531,0.0193265564529946));
#17517=CARTESIAN_POINT('',(-0.037301116085,0.008766788714,0.019082991418));
#17518=CARTESIAN_POINT('',(-0.03695137278,0.00890933196,0.019182696761));
#17519=CARTESIAN_POINT('',(-0.037041308464,0.008655658553,0.019465980183));
#17520=CARTESIAN_POINT('',(-0.037339424126,0.008823609321,0.019121421839));
#17521=CARTESIAN_POINT('',(-0.036983551057,0.008969082356,0.019216348303));
#17522=CARTESIAN_POINT('',(-0.037079616505,0.008720674816,0.019509653949));
#17523=CARTESIAN_POINT('',(-0.037413681214,0.008940547851,0.01919260491));
#17524=CARTESIAN_POINT('',(-0.037045412802,0.009090762045,0.019277559802));
#17525=CARTESIAN_POINT('',(-0.037153873593,0.00885449785,0.019590514456));
#17526=CARTESIAN_POINT('',(-0.037449744946,0.00900082422,0.019225478294));
#17527=CARTESIAN_POINT('',(-0.037075133644,0.00915286487800001,0.019305105559));
#17528=CARTESIAN_POINT('',(-0.037189937325,0.008923485888,0.019627838465));
#17529=CARTESIAN_POINT('',(-0.037519742735,0.009125063699,0.01928564172));
#17530=CARTESIAN_POINT('',(-0.0371322980209999,0.009279487072,0.019354318908));
#17531=CARTESIAN_POINT('',(-0.037259935114,0.009065697806,0.019696105522));
#17532=CARTESIAN_POINT('',(-0.037553677068,0.009189026182,0.019312932788));
#17533=CARTESIAN_POINT('',(-0.037159681014,0.009344000008,0.019375867489));
#17534=CARTESIAN_POINT('',(-0.037293869447,0.009138920963,0.019727049749));
#17535=CARTESIAN_POINT('',(-0.037602938649,0.009287868388,0.019349449243));
#17536=CARTESIAN_POINT('',(-0.037198872381,0.009442158226,0.01940357468));
#17537=CARTESIAN_POINT('',(-0.037343131027,0.009252085639,0.019768414058));
#17538=CARTESIAN_POINT('',(-0.037619085386,0.009321299752,0.01936088333));
#17539=CARTESIAN_POINT('',(-0.037211691522,0.00947530986300001,0.0194120754));
#17540=CARTESIAN_POINT('',(-0.037359277765,0.009290363203,0.019781358588));
#17541=CARTESIAN_POINT('',(-0.037650817756,0.009389164887,0.019382217481));
#17542=CARTESIAN_POINT('',(-0.037236742776,0.00954221984800001,0.019427532009));
#17543=CARTESIAN_POINT('',(-0.037391010135,0.00936806994,0.019805494239));
#17544=CARTESIAN_POINT('',(-0.037666411882,0.009423626067,0.019392118348));
#17545=CARTESIAN_POINT('',(-0.037248972401,0.00957599822699999,0.019434471815));
#17546=CARTESIAN_POINT('',(-0.037406604261,0.009407530512,0.019816686195));
#17547=CARTESIAN_POINT('',(-0.037742059103,0.009596469576,0.019437127945));
#17548=CARTESIAN_POINT('',(-0.037308672836,0.009746481892,0.019465277981));
#17549=CARTESIAN_POINT('',(-0.037482251481,0.009605458605,0.0198675155));
#17550=CARTESIAN_POINT('',(-0.037795953594,0.009737990873,0.019459408654));
#17551=CARTESIAN_POINT('',(-0.037349209561,0.00988085362500001,0.019475955808));
#17552=CARTESIAN_POINT('',(-0.037536145973,0.009767548722,0.019892505579));
#17553=CARTESIAN_POINT('',(-0.037866774638,0.00995526822,0.019471266124));
#17554=CARTESIAN_POINT('',(-0.037401307565,0.010081722694,0.019473703662));
#17555=CARTESIAN_POINT('',(-0.037606967016,0.010016452968,0.019905364135));
#17556=CARTESIAN_POINT('',(-0.037888699602,0.010028532389,0.019471600233));
#17557=CARTESIAN_POINT('',(-0.037417279271,0.010149079247,0.019469741824));
#17558=CARTESIAN_POINT('',(-0.037628891981,0.010100389312,0.019905517967));
#17559=CARTESIAN_POINT('',(-0.037918925522,0.010139765166,0.0194662815));
#17560=CARTESIAN_POINT('',(-0.037439020962,0.010250061616,0.019459037412));
#17561=CARTESIAN_POINT('',(-0.037659117901,0.010227838031,0.01989910134));
#17562=CARTESIAN_POINT('',(-0.037928582819,0.010177183975,0.019463520333));
#17563=CARTESIAN_POINT('',(-0.037445936687,0.010283943964,0.019454625919));
#17564=CARTESIAN_POINT('',(-0.037668775198,0.010270714068,0.019895833342));
#17565=CARTESIAN_POINT('',(-0.037946745879,0.010251529703,0.019456070883));
#17566=CARTESIAN_POINT('',(-0.037458875717,0.010350958591,0.019444295419));
#17567=CARTESIAN_POINT('',(-0.037686938258,0.01035590701,0.019887098991));
#17568=CARTESIAN_POINT('',(-0.03795527555,0.010288532493,0.019451385246));
#17569=CARTESIAN_POINT('',(-0.0374649083939999,0.010384139251,0.019438369006));
#17570=CARTESIAN_POINT('',(-0.037695467929,0.010398310834,0.019881635422));
#17571=CARTESIAN_POINT('',(-0.037995201404,0.0104727007,0.019423189771));
#17572=CARTESIAN_POINT('',(-0.037493219634,0.010549838583,0.019404818528));
#17573=CARTESIAN_POINT('',(-0.037735393783,0.010609372239,0.01984887779));
#17574=CARTESIAN_POINT('',(-0.03801852767,0.010617356474,0.019385538099));
#17575=CARTESIAN_POINT('',(-0.0375089769519999,0.010676036879,0.019366609516));
#17576=CARTESIAN_POINT('',(-0.037758720049,0.010775187757,0.01980544701));
#17577=CARTESIAN_POINT('',(-0.038040144091,0.010830087113,0.019305249844));
#17578=CARTESIAN_POINT('',(-0.037523624808,0.010861368197,0.019291823728));
#17579=CARTESIAN_POINT('',(-0.03778033647,0.011019102134,0.019713124546));
#17580=CARTESIAN_POINT('',(-0.038045091154,0.010900659463,0.01927424932));
#17581=CARTESIAN_POINT('',(-0.037526947936,0.010922751921,0.019263695619));
#17582=CARTESIAN_POINT('',(-0.037785283533,0.011100031176,0.01967751236));
#17583=CARTESIAN_POINT('',(-0.038050108278,0.011036551943,0.019205674484));
#17584=CARTESIAN_POINT('',(-0.037530327064,0.011041355675,0.019202654737));
#17585=CARTESIAN_POINT('',(-0.037790300657,0.011255891492,0.01959879628));
#17586=CARTESIAN_POINT('',(-0.038050243047,0.011102269591,0.019167998017));
#17587=CARTESIAN_POINT('',(-0.037530417095,0.011098746343,0.01916971836));
#17588=CARTESIAN_POINT('',(-0.037790435426,0.011331278423,0.019555574534));
#17589=CARTESIAN_POINT('',(-0.038045857381,0.011229333988,0.019085998172));
#17590=CARTESIAN_POINT('',(-0.037527464034,0.011210579299,0.019098653928));
#17591=CARTESIAN_POINT('',(-0.03778604976,0.011477065914,0.019461552266));
#17592=CARTESIAN_POINT('',(-0.038041336883,0.011290680666,0.019041674687));
#17593=CARTESIAN_POINT('',(-0.037524429559,0.011264860653,0.019060637682));
#17594=CARTESIAN_POINT('',(-0.037781529262,0.011547466388,0.019410751623));
#17595=CARTESIAN_POINT('',(-0.038027559938,0.011408940944,0.018946286813));
#17596=CARTESIAN_POINT('',(-0.037515080889,0.011370775304,0.018978926179));
#17597=CARTESIAN_POINT('',(-0.037767752317,0.011683211699,0.019301463566));
#17598=CARTESIAN_POINT('',(-0.038018235775,0.011465994202,0.018895009009));
#17599=CARTESIAN_POINT('',(-0.037508746133,0.011422411288,0.018935184096));
#17600=CARTESIAN_POINT('',(-0.037758428154,0.011748717175,0.019242731993));
#17601=CARTESIAN_POINT('',(-0.037983863425,0.011626135813,0.018735057854));
#17602=CARTESIAN_POINT('',(-0.037485152239,0.011569149469,0.018798617961));
#17603=CARTESIAN_POINT('',(-0.037724055805,0.011932636702,0.01905958005));
#17604=CARTESIAN_POINT('',(-0.03795238138,0.011719875549,0.018619223276));
#17605=CARTESIAN_POINT('',(-0.037463427014,0.011658126499,0.018699531784));
#17606=CARTESIAN_POINT('',(-0.037692573758,0.012040369285,0.018927005758));
#17607=CARTESIAN_POINT('',(-0.037902538675,0.01182142833,0.018463435089));
#17608=CARTESIAN_POINT('',(-0.037427207905,0.011759803085,0.018561524169));
#17609=CARTESIAN_POINT('',(-0.037642731053,0.012157190014,0.018748770563));
#17610=CARTESIAN_POINT('',(-0.0378920119,0.011840990207,0.018431644379));
#17611=CARTESIAN_POINT('',(-0.037419583631,0.011779451696,0.018533495969));
#17612=CARTESIAN_POINT('',(-0.037632204279,0.012179699312,0.018712402395));
#17613=CARTESIAN_POINT('',(-0.037870126119,0.011878130234,0.018367644958));
#17614=CARTESIAN_POINT('',(-0.037403612981,0.011817220648,0.018476768706));
#17615=CARTESIAN_POINT('',(-0.037610318498,0.012222448524,0.018639193956));
#17616=CARTESIAN_POINT('',(-0.037858748966,0.011895754219,0.018335374301));
#17617=CARTESIAN_POINT('',(-0.037395262434,0.011835384713,0.018448035028));
#17618=CARTESIAN_POINT('',(-0.037598941345,0.012242741131,0.018602282796));
#17619=CARTESIAN_POINT('',(-0.037823348421,0.011945883489,0.018237779846));
#17620=CARTESIAN_POINT('',(-0.037369172913,0.011887572482,0.018360946022));
#17621=CARTESIAN_POINT('',(-0.0375635408,0.012300482293,0.018490662919));
#17622=CARTESIAN_POINT('',(-0.037798059306,0.011975653238,0.018171675593));
#17623=CARTESIAN_POINT('',(-0.037350277137,0.011919662954,0.018301226609));
#17624=CARTESIAN_POINT('',(-0.037538251684,0.012334802364,0.01841507009));
#17625=CARTESIAN_POINT('',(-0.037744193093,0.012028207852,0.018037491178));
#17626=CARTESIAN_POINT('',(-0.037309379895,0.011978153369,0.018178502137));
#17627=CARTESIAN_POINT('',(-0.037484385472,0.012395455267,0.018261646389));
#17628=CARTESIAN_POINT('',(-0.037715615604,0.012050991651,0.017969410681));
#17629=CARTESIAN_POINT('',(-0.037287455068,0.012004589867,0.018115639729));
#17630=CARTESIAN_POINT('',(-0.037455807983,0.012421786873,0.018183815137));
#17631=CARTESIAN_POINT('',(-0.037670271841,0.012079999243,0.017865841447));
#17632=CARTESIAN_POINT('',(-0.037251993154,0.012039949422,0.018018443323));
#17633=CARTESIAN_POINT('',(-0.03741046422,0.012455375111,0.018065427979));
#17634=CARTESIAN_POINT('',(-0.037654725402,0.012088808864,0.017831040227));
#17635=CARTESIAN_POINT('',(-0.037239813053,0.012050965676,0.017985742729));
#17636=CARTESIAN_POINT('',(-0.037394917781,0.012465588496,0.018025650255));
#17637=CARTESIAN_POINT('',(-0.037623119912,0.012104555629,0.017761655615));
#17638=CARTESIAN_POINT('',(-0.037214887215,0.012071290256,0.017920179797));
#17639=CARTESIAN_POINT('',(-0.037363312291,0.012483871576,0.017946348883));
#17640=CARTESIAN_POINT('',(-0.037607024828,0.012111518654,0.017726988147));
#17641=CARTESIAN_POINT('',(-0.037202122033,0.012080639592,0.017887250964));
#17642=CARTESIAN_POINT('',(-0.037347217206,0.012491971204,0.017906729123));
#17643=CARTESIAN_POINT('',(-0.037525118351,0.012141933343,0.01755377779));
#17644=CARTESIAN_POINT('',(-0.037137549676,0.012122798947,0.017723852461));
#17645=CARTESIAN_POINT('',(-0.03726531073,0.012527433166,0.017708787883));
#17646=CARTESIAN_POINT('',(-0.037455051799,0.012152306816,0.017415613082));
#17647=CARTESIAN_POINT('',(-0.037080651573,0.012144510573,0.017589399015));
#17648=CARTESIAN_POINT('',(-0.037195244178,0.012539827994,0.017550935495));
#17649=CARTESIAN_POINT('',(-0.037343235527,0.012148213531,0.01720905843));
#17650=CARTESIAN_POINT('',(-0.036986748025,0.012157127057,0.017382507888));
#17651=CARTESIAN_POINT('',(-0.037083427906,0.012535928527,0.017315007876));
#17652=CARTESIAN_POINT('',(-0.03730475018,0.012143504287,0.01714019209));
#17653=CARTESIAN_POINT('',(-0.03695443279,0.012158057656,0.017313516891));
#17654=CARTESIAN_POINT('',(-0.037044942559,0.012530801323,0.017236358679));
#17655=CARTESIAN_POINT('',(-0.03722687049,0.012127824497,0.017005091856));
#17656=CARTESIAN_POINT('',(-0.036888415857,0.012153246959,0.017177025003));
#17657=CARTESIAN_POINT('',(-0.036967062869,0.012513372076,0.01708208731));
#17658=CARTESIAN_POINT('',(-0.037187320072,0.012116862461,0.016938559819));
#17659=CARTESIAN_POINT('',(-0.036854627768,0.012147650578,0.017109245591));
#17660=CARTESIAN_POINT('',(-0.036927512451,0.012501080898,0.017006124553));
#17661=CARTESIAN_POINT('',(-0.03706685504,0.012075016713,0.016741914748));
#17662=CARTESIAN_POINT('',(-0.036751742399,0.012121386905,0.016909119768));
#17663=CARTESIAN_POINT('',(-0.036807047419,0.012453943078,0.016781637365));
#17664=CARTESIAN_POINT('',(-0.03698413842,0.012035245207,0.016614730411));
#17665=CARTESIAN_POINT('',(-0.036679594089,0.012091526511,0.016776553485));
#17666=CARTESIAN_POINT('',(-0.036724330798,0.01240891457,0.016636488213));
#17667=CARTESIAN_POINT('',(-0.036813690053,0.011932224721,0.016368219888));
#17668=CARTESIAN_POINT('',(-0.036528822624,0.012005165032,0.016516491866));
#17669=CARTESIAN_POINT('',(-0.036553882432,0.012291955726,0.016355253995));
#17670=CARTESIAN_POINT('',(-0.03672806298,0.011870246798,0.016251941319));
#17671=CARTESIAN_POINT('',(-0.036452219097,0.011950532581,0.016391983009));
#17672=CARTESIAN_POINT('',(-0.036468255359,0.012221468356,0.016222645908));
#17673=CARTESIAN_POINT('',(-0.036556082968,0.011726690875,0.01603279824));
#17674=CARTESIAN_POINT('',(-0.036296957641,0.01181811194,0.016155409747));
#17675=CARTESIAN_POINT('',(-0.036296275347,0.012057999557,0.015972835599));
#17676=CARTESIAN_POINT('',(-0.036469700557,0.011645092454,0.01592989329));
#17677=CARTESIAN_POINT('',(-0.036218299035,0.011740996991,0.016042857153));
#17678=CARTESIAN_POINT('',(-0.03620989256,0.011964994531,0.015855586742));
#17679=CARTESIAN_POINT('',(-0.0363829297,0.011553263876,0.015833944478));
#17680=CARTESIAN_POINT('',(-0.036137554584,0.011650536133,0.015935581221));
#17681=CARTESIAN_POINT('',(-0.036123122079,0.011860244082,0.015746332321));
#17682=CARTESIAN_POINT('',(-0.0387712812904556,1.29145419960524E-11,1.90093214813058E-11));
#17683=CARTESIAN_POINT('',(-0.0363829297,-0.007935966222,0.017922392252));
#17684=CARTESIAN_POINT('',(-0.036137554584,-0.00797535009500001,0.01805745087));
#17685=CARTESIAN_POINT('',(-0.036123122079,-0.007706601765,0.018144438831));
#17686=CARTESIAN_POINT('',(-0.036296388628,-0.00789888486,0.017795229609));
#17687=CARTESIAN_POINT('',(-0.036059352191,-0.00792917773300001,0.017929626577));
#17688=CARTESIAN_POINT('',(-0.03603658062,-0.007664471384,0.017999478691));
#17689=CARTESIAN_POINT('',(-0.036211750879,-0.007873865053,0.017666078425));
#17690=CARTESIAN_POINT('',(-0.03598108599,-0.007894696976,0.017796520282));
#17691=CARTESIAN_POINT('',(-0.035951943258,-0.00763618434,0.017852211978));
#17692=CARTESIAN_POINT('',(-0.036046427611,-0.007847575992,0.017403812149));
#17693=CARTESIAN_POINT('',(-0.03582764111,-0.007852090759,0.01752422126));
#17694=CARTESIAN_POINT('',(-0.03578661999,-0.007606880233,0.017553069188));
#17695=CARTESIAN_POINT('',(-0.035965731891,-0.007846286179,0.017270695297));
#17696=CARTESIAN_POINT('',(-0.035752240428,-0.007843210526,0.017384956612));
#17697=CARTESIAN_POINT('',(-0.03570592427,-0.00760583974,0.017401191901));
#17698=CARTESIAN_POINT('',(-0.035867783855,-0.007860916809,0.017101471238));
#17699=CARTESIAN_POINT('',(-0.035659677357,-0.00785025534,0.017205405462));
#17700=CARTESIAN_POINT('',(-0.035607976234,-0.007623195358,0.017208053208));
#17701=CARTESIAN_POINT('',(-0.03584830488,-0.007864675489,0.017067415562));
#17702=CARTESIAN_POINT('',(-0.035641412325,-0.00785254753800001,0.017169542439));
#17703=CARTESIAN_POINT('',(-0.035588497259,-0.007627622941,0.017169181517));
#17704=CARTESIAN_POINT('',(-0.035810061793,-0.007873792339,0.016999715979));
#17705=CARTESIAN_POINT('',(-0.035605524332,-0.007858918629,0.017098165957));
#17706=CARTESIAN_POINT('',(-0.035550254172,-0.007638313039,0.017091901304));
#17707=CARTESIAN_POINT('',(-0.035791254693,-0.00787915358,0.016965999395));
#17708=CARTESIAN_POINT('',(-0.035587855191,-0.00786298741,0.01706256955));
#17709=CARTESIAN_POINT('',(-0.035531447072,-0.007644579318,0.017053409847));
#17710=CARTESIAN_POINT('',(-0.035735788251,-0.007897644484,0.016865244352));
#17711=CARTESIAN_POINT('',(-0.035535852231,-0.00787783087500001,0.016956380478));
#17712=CARTESIAN_POINT('',(-0.03547598063,-0.007666140505,0.016938375535));
#17713=CARTESIAN_POINT('',(-0.035700081089,-0.007913175312,0.016798599729));
#17714=CARTESIAN_POINT('',(-0.035502196601,-0.007891267476,0.016885756544));
#17715=CARTESIAN_POINT('',(-0.035440273468,-0.007684190871,0.016862271769));
#17716=CARTESIAN_POINT('',(-0.035596955729,-0.007969579454,0.016600233953));
#17717=CARTESIAN_POINT('',(-0.035405412743,-0.007942282341,0.016676313757));
#17718=CARTESIAN_POINT('',(-0.035337148108,-0.007749601706,0.016635705408));
#17719=CARTESIAN_POINT('',(-0.035533471872,-0.008020130655,0.016470062373));
#17720=CARTESIAN_POINT('',(-0.03534514464,-0.007990615333,0.016537412932));
#17721=CARTESIAN_POINT('',(-0.035273664252,-0.00780806873,0.016486967212));
#17722=CARTESIAN_POINT('',(-0.035462076716,-0.008101852446,0.016310148785));
#17723=CARTESIAN_POINT('',(-0.035277056499,-0.008072198153,0.016365801681));
#17724=CARTESIAN_POINT('',(-0.035202269094,-0.007902417857,0.016304149447));
#17725=CARTESIAN_POINT('',(-0.035448157312,-0.008119195502,0.016278204166));
#17726=CARTESIAN_POINT('',(-0.035263851039,-0.00808951015200001,0.016331706315));
#17727=CARTESIAN_POINT('',(-0.035188349691,-0.007922433981,0.016267624501));
#17728=CARTESIAN_POINT('',(-0.035421421576,-0.008155528492,0.01621518104));
#17729=CARTESIAN_POINT('',(-0.035238481118,-0.008125981757,0.0162644302));
#17730=CARTESIAN_POINT('',(-0.035161613954,-0.007964353608,0.016195554481));
#17731=CARTESIAN_POINT('',(-0.035408615027,-0.008174492909,0.016184132248));
#17732=CARTESIAN_POINT('',(-0.035226318844,-0.008145113188,0.016231268977));
#17733=CARTESIAN_POINT('',(-0.035148807406,-0.007986227718,0.01616004343));
#17734=CARTESIAN_POINT('',(-0.035371903227,-0.008233790533,0.016092375852));
#17735=CARTESIAN_POINT('',(-0.035191509303,-0.008205098964,0.016133439925));
#17736=CARTESIAN_POINT('',(-0.035112095605,-0.008054604749,0.016055083828));
#17737=CARTESIAN_POINT('',(-0.035349701075,-0.00827652121,0.01603305419));
#17738=CARTESIAN_POINT('',(-0.035170375015,-0.008248745904,0.016070010593));
#17739=CARTESIAN_POINT('',(-0.035089893455,-0.008103854486,0.015987204245));
#17740=CARTESIAN_POINT('',(-0.035310076825,-0.008368595603,0.015918211266));
#17741=CARTESIAN_POINT('',(-0.035132682741,-0.008343387593,0.015947352599));
#17742=CARTESIAN_POINT('',(-0.035050269204,-0.008209928279,0.015855746634));
#17743=CARTESIAN_POINT('',(-0.035292653375,-0.008417937511,0.015862688976));
#17744=CARTESIAN_POINT('',(-0.035116074086,-0.008394403586,0.015888019139));
#17745=CARTESIAN_POINT('',(-0.035032845755,-0.008266750265,0.015792167434));
#17746=CARTESIAN_POINT('',(-0.035270404132,-0.008497251596,0.015782437272));
#17747=CARTESIAN_POINT('',(-0.035094864144,-0.00847684110199999,0.015802332322));
#17748=CARTESIAN_POINT('',(-0.03501059651,-0.00835805282,0.015700230057));
#17749=CARTESIAN_POINT('',(-0.03526362249,-0.008524662259,0.015756120857));
#17750=CARTESIAN_POINT('',(-0.035088401673,-0.008505365652,0.015774270534));
#17751=CARTESIAN_POINT('',(-0.035003814869,-0.008389601082,0.015670074582));
#17752=CARTESIAN_POINT('',(-0.035251577427,-0.008580564888,0.015705227052));
#17753=CARTESIAN_POINT('',(-0.035076925826,-0.008563640037,0.01572005437));
#17754=CARTESIAN_POINT('',(-0.034991769806,-0.008453930794,0.015611741863));
#17755=CARTESIAN_POINT('',(-0.035246291308,-0.008609118788,0.015680578683));
#17756=CARTESIAN_POINT('',(-0.035071886429,-0.008593462603,0.015693811186));
#17757=CARTESIAN_POINT('',(-0.034986483687,-0.008486783572,0.015583483346));
#17758=CARTESIAN_POINT('',(-0.035223521483,-0.008754870702,0.01556128769));
#17759=CARTESIAN_POINT('',(-0.035050225188,-0.008745616554,0.015567192245));
#17760=CARTESIAN_POINT('',(-0.034963713862,-0.008654451161,0.015446682695));
#17761=CARTESIAN_POINT('',(-0.035216913712,-0.008880915106,0.0154783625));
#17762=CARTESIAN_POINT('',(-0.035043883179,-0.008878570113,0.015479125626));
#17763=CARTESIAN_POINT('',(-0.034957106091,-0.00879936203,0.015351462313));
#17764=CARTESIAN_POINT('',(-0.035223876434,-0.009050786794,0.015391012352));
#17765=CARTESIAN_POINT('',(-0.035050518048,-0.00905756869499999,0.015387635792));
#17766=CARTESIAN_POINT('',(-0.034964068813,-0.008994538787,0.015250984281));
#17767=CARTESIAN_POINT('',(-0.03522604562,-0.00908540579,0.015374366785));
#17768=CARTESIAN_POINT('',(-0.035052587043,-0.009094097267,0.015370243184));
#17769=CARTESIAN_POINT('',(-0.034966237999,-0.009034309077,0.015231826369));
#17770=CARTESIAN_POINT('',(-0.035231850552,-0.009154857947,0.015343216139));
#17771=CARTESIAN_POINT('',(-0.035058120997,-0.00916739562200001,0.015337818228));
#17772=CARTESIAN_POINT('',(-0.034972042931,-0.009114084127,0.015195952232));
#17773=CARTESIAN_POINT('',(-0.0352354894,-0.009189818174,0.015328642479));
#17774=CARTESIAN_POINT('',(-0.035061591095,-0.009204314377,0.015322709066));
#17775=CARTESIAN_POINT('',(-0.034975681779,-0.009154234899,0.01517915715));
#17776=CARTESIAN_POINT('',(-0.035248550352,-0.009295383715,0.015287847634));
#17777=CARTESIAN_POINT('',(-0.035074046816,-0.00931586337799999,0.015280597597));
#17778=CARTESIAN_POINT('',(-0.034988742731,-0.009275456669,0.01513210841));
#17779=CARTESIAN_POINT('',(-0.035260111701,-0.009366671914,0.015264544541));
#17780=CARTESIAN_POINT('',(-0.035085080525,-0.009391243379,0.015256839807));
#17781=CARTESIAN_POINT('',(-0.03500030408,-0.009357294881,0.01510518209));
#17782=CARTESIAN_POINT('',(-0.035281577861,-0.009474939166,0.015235272178));
#17783=CARTESIAN_POINT('',(-0.035105505104,-0.00950550548799999,0.015227540121));
#17784=CARTESIAN_POINT('',(-0.03502177024,-0.009481550391,0.01507127367));
#17785=CARTESIAN_POINT('',(-0.035289421938,-0.009511251248,0.015226463836));
#17786=CARTESIAN_POINT('',(-0.035112977015,-0.00954387011300001,0.01521881712));
#17787=CARTESIAN_POINT('',(-0.035029614317,-0.009523219169,0.015061053398));
#17788=CARTESIAN_POINT('',(-0.035306476701,-0.009584322003,0.01521074306));
#17789=CARTESIAN_POINT('',(-0.035129211644,-0.009621038485,0.015203474112));
#17790=CARTESIAN_POINT('',(-0.03504666908,-0.009607057743,0.015042775596));
#17791=CARTESIAN_POINT('',(-0.035315718145,-0.009621192412,0.015203814));
#17792=CARTESIAN_POINT('',(-0.035138009535,-0.009659975092,0.015196840927));
#17793=CARTESIAN_POINT('',(-0.035055910524,-0.0096493557,0.015034698584));
#17794=CARTESIAN_POINT('',(-0.035345244257,-0.009731576519,0.015186028085));
#17795=CARTESIAN_POINT('',(-0.035166136457,-0.009776637113,0.015180221674));
#17796=CARTESIAN_POINT('',(-0.035085436637,-0.009775971844,0.01501389589));
#17797=CARTESIAN_POINT('',(-0.035367258146,-0.009804686247,0.01517816092));
#17798=CARTESIAN_POINT('',(-0.035187092355,-0.00985378804700001,0.015173570618));
#17799=CARTESIAN_POINT('',(-0.035107450524,-0.009859809659,0.015004586152));
#17800=CARTESIAN_POINT('',(-0.035415540032,-0.009950034894,0.01516985648));
#17801=CARTESIAN_POINT('',(-0.035232955499,-0.010006887199,0.015168405072));
#17802=CARTESIAN_POINT('',(-0.035155732411,-0.01002644331,0.014994457537));
#17803=CARTESIAN_POINT('',(-0.035441809443,-0.010022273518,0.015169421497));
#17804=CARTESIAN_POINT('',(-0.035257918294,-0.010082919856,0.015169944486));
#17805=CARTESIAN_POINT('',(-0.035182001822,-0.0101092388,0.014993641282));
#17806=CARTESIAN_POINT('',(-0.035498359317,-0.010165935271,0.01517571553));
#17807=CARTESIAN_POINT('',(-0.035311533473,-0.010233771266,0.015180838497));
#17808=CARTESIAN_POINT('',(-0.035238551696,-0.01027385273,0.015000197616));
#17809=CARTESIAN_POINT('',(-0.035528803299,-0.010237694895,0.015182511514));
#17810=CARTESIAN_POINT('',(-0.035340397738,-0.010309011127,0.01519034352));
#17811=CARTESIAN_POINT('',(-0.035268995678,-0.010356056437,0.015007645243));
#17812=CARTESIAN_POINT('',(-0.035624302868,-0.010448231116,0.015212973614));
#17813=CARTESIAN_POINT('',(-0.035431143853,-0.010530150409,0.015229867744));
#17814=CARTESIAN_POINT('',(-0.035364495247,-0.010597173211,0.015041521636));
#17815=CARTESIAN_POINT('',(-0.035693625065,-0.010582922476,0.015246481917));
#17816=CARTESIAN_POINT('',(-0.035496770299,-0.010670383783,0.015270793079));
#17817=CARTESIAN_POINT('',(-0.035433817443,-0.010751346613,0.015079216188));
#17818=CARTESIAN_POINT('',(-0.035804878296,-0.010777396222,0.015314797255));
#17819=CARTESIAN_POINT('',(-0.035600812464,-0.010870193851,0.015350654782));
#17820=CARTESIAN_POINT('',(-0.035545070675,-0.010973839943,0.015156427299));
#17821=CARTESIAN_POINT('',(-0.035843360668,-0.010841212942,0.01534073771));
#17822=CARTESIAN_POINT('',(-0.035636958249,-0.01093587108,0.015380883423));
#17823=CARTESIAN_POINT('',(-0.035583553047,-0.011046831996,0.015185790742));
#17824=CARTESIAN_POINT('',(-0.035921655233,-0.010964716188,0.015397891995));
#17825=CARTESIAN_POINT('',(-0.035710302083,-0.011062419569,0.015446810101));
#17826=CARTESIAN_POINT('',(-0.035661847612,-0.011188055569,0.01525056404));
#17827=CARTESIAN_POINT('',(-0.035961464931,-0.011024436082,0.015429078645));
#17828=CARTESIAN_POINT('',(-0.035747535996,-0.011123315491,0.015482566139));
#17829=CARTESIAN_POINT('',(-0.035701657309,-0.011256325476,0.015285942678));
#17830=CARTESIAN_POINT('',(-0.036082708725,-0.011197835672,0.015530092476));
#17831=CARTESIAN_POINT('',(-0.035861344783,-0.01130037601,0.015598213312));
#17832=CARTESIAN_POINT('',(-0.035822901104,-0.011454498054,0.015400624625));
#17833=CARTESIAN_POINT('',(-0.036165937985,-0.011305805198,0.015607312287));
#17834=CARTESIAN_POINT('',(-0.035938765603,-0.011408558316,0.015685491612));
#17835=CARTESIAN_POINT('',(-0.035906130364,-0.011577821075,0.015488403863));
#17836=CARTESIAN_POINT('',(-0.036272749616,-0.011431478006,0.015715991043));
#17837=CARTESIAN_POINT('',(-0.036036325391,-0.011531489845,0.015805195535));
#17838=CARTESIAN_POINT('',(-0.036012941995,-0.011721279377,0.015612059748));
#17839=CARTESIAN_POINT('',(-0.036294271622,-0.011456162931,0.015738362019));
#17840=CARTESIAN_POINT('',(-0.036056160144,-0.011555785974,0.015830037016));
#17841=CARTESIAN_POINT('',(-0.036034464001,-0.011749453109,0.015637518901));
#17842=CARTESIAN_POINT('',(-0.036337241164,-0.011504198589,0.015783958945));
#17843=CARTESIAN_POINT('',(-0.036095695252,-0.011602868295,0.015880530299));
#17844=CARTESIAN_POINT('',(-0.036077433543,-0.011804268644,0.015689420125));
#17845=CARTESIAN_POINT('',(-0.036358730845,-0.011527600241,0.015807226781));
#17846=CARTESIAN_POINT('',(-0.03611543566,-0.011625696687,0.015906237255));
#17847=CARTESIAN_POINT('',(-0.036098923223,-0.011830968578,0.015715909844));
#17848=CARTESIAN_POINT('',(-0.036423211553,-0.011595992591,0.015878412814));
#17849=CARTESIAN_POINT('',(-0.036174782484,-0.011692352266,0.015984962597));
#17850=CARTESIAN_POINT('',(-0.036163403931,-0.011908986452,0.015796966748));
#17851=CARTESIAN_POINT('',(-0.036466213928,-0.011639174576,0.015927710753));
#17852=CARTESIAN_POINT('',(-0.036214084658,-0.011733813027,0.016039055431));
#17853=CARTESIAN_POINT('',(-0.036206406307,-0.011958226934,0.015853118487));
#17854=CARTESIAN_POINT('',(-0.036595254777,-0.011761619038,0.016081028728));
#17855=CARTESIAN_POINT('',(-0.03633245937,-0.011851005228,0.016207593429));
#17856=CARTESIAN_POINT('',(-0.036335447156,-0.012097793945,0.016027801545));
#17857=CARTESIAN_POINT('',(-0.036681322249,-0.01183384166,0.01619042867));
#17858=CARTESIAN_POINT('',(-0.036410235723,-0.011917375548,0.016326105441));
#17859=CARTESIAN_POINT('',(-0.036421514628,-0.012180036844,0.016152509941));
#17860=CARTESIAN_POINT('',(-0.03678899075,-0.011911891549,0.016336502043));
#17861=CARTESIAN_POINT('',(-0.036505370032,-0.01198586263,0.016480211706));
#17862=CARTESIAN_POINT('',(-0.036529183129,-0.012268805633,0.016319094869));
#17863=CARTESIAN_POINT('',(-0.036810556304,-0.011926900857,0.016366226459));
#17864=CARTESIAN_POINT('',(-0.036524605066,-0.011999026208,0.016511861903));
#17865=CARTESIAN_POINT('',(-0.036550748683,-0.012285869776,0.016352996559));
#17866=CARTESIAN_POINT('',(-0.036853337272,-0.011955422756,0.016426124399));
#17867=CARTESIAN_POINT('',(-0.036562661331,-0.012023724111,0.016575442629));
#17868=CARTESIAN_POINT('',(-0.036593529651,-0.012318283097,0.016421318697));
#17869=CARTESIAN_POINT('',(-0.036874593816,-0.011968966814,0.016456352488));
#17870=CARTESIAN_POINT('',(-0.036581516731,-0.012035273907,0.016607435016));
#17871=CARTESIAN_POINT('',(-0.036614786195,-0.012333668079,0.016455801366));
#17872=CARTESIAN_POINT('',(-0.036937968442,-0.012007462527,0.016547866518));
#17873=CARTESIAN_POINT('',(-0.03663781018,-0.012067727143,0.016704386433));
#17874=CARTESIAN_POINT('',(-0.03667816082,-0.012377374469,0.016560205216));
#17875=CARTESIAN_POINT('',(-0.03697969206,-0.01203028214,0.016609980557));
#17876=CARTESIAN_POINT('',(-0.036674489896,-0.012086090141,0.016769529197));
#17877=CARTESIAN_POINT('',(-0.036719884461,-0.012403252403,0.016631080369));
#17878=CARTESIAN_POINT('',(-0.037020900622,-0.012050241607,0.016673198758));
#17879=CARTESIAN_POINT('',(-0.036710197303,-0.012101269023,0.016834819376));
#17880=CARTESIAN_POINT('',(-0.036761093001,-0.012425852784,0.016703226885));
#17881=CARTESIAN_POINT('',(-0.0370209006219633,-0.0123363218309527,0.0165828765281445));
#17882=CARTESIAN_POINT('',(-0.0363829297000878,-0.00764796150808045,0.0180063760900247));
#17883=CARTESIAN_POINT('',(-0.0370209006725265,-0.0120502416314727,0.016673198835513));
#17884=CARTESIAN_POINT('',(-0.0367101973471479,-0.0121012690417669,0.0168348194567234));
#17885=CARTESIAN_POINT('',(-0.0367610930515268,-0.0124258528117109,0.0167032269734606));
#17886=CARTESIAN_POINT('',(-0.037103317012847,-0.0120901601826742,0.0167996340374687));
#17887=CARTESIAN_POINT('',(-0.0367834353017993,-0.0121324018021573,0.0169687333890696));
#17888=CARTESIAN_POINT('',(-0.0368435097848469,-0.0124710533801557,0.0168475194030382));
#17889=CARTESIAN_POINT('',(-0.0371836845969985,-0.012118723833302,0.0169304571286969));
#17890=CARTESIAN_POINT('',(-0.036852619292111,-0.0121502141620385,0.0171032960490522));
#17891=CARTESIAN_POINT('',(-0.0369238769759985,-0.0125032416596733,0.016996863092627));
#17892=CARTESIAN_POINT('',(-0.037301116085,-0.012142960991,0.017133757444));
#17893=CARTESIAN_POINT('',(-0.03695137278,-0.012158036728,0.017307056189));
#17894=CARTESIAN_POINT('',(-0.037041308464,-0.012530204072,0.017229010285));
#17895=CARTESIAN_POINT('',(-0.037339424126,-0.012147832408,0.017202180744));
#17896=CARTESIAN_POINT('',(-0.036983551057,-0.01215730462,0.01737562732));
#17897=CARTESIAN_POINT('',(-0.037079616505,-0.012535518531,0.017307152903));
#17898=CARTESIAN_POINT('',(-0.037413681214,-0.012151009491,0.017339044018));
#17899=CARTESIAN_POINT('',(-0.037045412802,-0.012149475489,0.017511610772));
#17900=CARTESIAN_POINT('',(-0.037153873593,-0.012538634267,0.017463477304));
#17901=CARTESIAN_POINT('',(-0.037449744946,-0.012149340492,0.017407681576));
#17902=CARTESIAN_POINT('',(-0.037075133644,-0.012142279398,0.017579166281));
#17903=CARTESIAN_POINT('',(-0.037189937325,-0.012536463788,0.017541884702));
#17904=CARTESIAN_POINT('',(-0.037519742735,-0.012139323808,0.017545357834));
#17905=CARTESIAN_POINT('',(-0.037132298021,-0.012121588311,0.017713430993));
#17906=CARTESIAN_POINT('',(-0.037259935114,-0.012524478835,0.017699177365));
#17907=CARTESIAN_POINT('',(-0.037553677068,-0.012130977326,0.017614396504));
#17908=CARTESIAN_POINT('',(-0.037159681014,-0.012107993462,0.017780075124));
#17909=CARTESIAN_POINT('',(-0.037293869447,-0.012514665743,0.017778062592));
#17910=CARTESIAN_POINT('',(-0.037602938649,-0.0121131804,0.017718254592));
#17911=CARTESIAN_POINT('',(-0.037198872381,-0.012082909484,0.01787893623));
#17912=CARTESIAN_POINT('',(-0.037343131027,-0.012493905947,0.017896748231));
#17913=CARTESIAN_POINT('',(-0.037619085386,-0.012106366928,0.017752924047));
#17914=CARTESIAN_POINT('',(-0.037211691522,-0.012073695505,0.01791189675));
#17915=CARTESIAN_POINT('',(-0.037359277765,-0.012485977458,0.017936369838));
#17916=CARTESIAN_POINT('',(-0.037650817756,-0.012090910276,0.017822364053));
#17917=CARTESIAN_POINT('',(-0.037236742776,-0.012053626329,0.017977570801));
#17918=CARTESIAN_POINT('',(-0.037391010135,-0.012468026175,0.018015733672));
#17919=CARTESIAN_POINT('',(-0.037666411882,-0.012082254089,0.017857158743));
#17920=CARTESIAN_POINT('',(-0.037248972401,-0.012042747188,0.018010293639));
#17921=CARTESIAN_POINT('',(-0.037406604261,-0.012457988408,0.018055503508));
#17922=CARTESIAN_POINT('',(-0.037742059103,-0.012034811789,0.018029350412));
#17923=CARTESIAN_POINT('',(-0.037308672836,-0.011984184277,0.018173339907));
#17924=CARTESIAN_POINT('',(-0.037482251481,-0.012403043831,0.018252328917));
#17925=CARTESIAN_POINT('',(-0.037795953594,-0.0119833468,0.018163051804));
#17926=CARTESIAN_POINT('',(-0.037349209561,-0.01192624568,0.018295048154));
#17927=CARTESIAN_POINT('',(-0.037536145973,-0.012343640815,0.018405198115));
#17928=CARTESIAN_POINT('',(-0.037866774638,-0.011884976998,0.018357148242));
#17929=CARTESIAN_POINT('',(-0.037401307565,-0.01182386073,0.018467879798));
#17930=CARTESIAN_POINT('',(-0.037606967016,-0.012230324528,0.018627184794));
#17931=CARTESIAN_POINT('',(-0.037888699602,-0.011848634259,0.018420763928));
#17932=CARTESIAN_POINT('',(-0.037417279271,-0.011786751401,0.018524231365));
#17933=CARTESIAN_POINT('',(-0.037628891981,-0.012188489579,0.018699952716));
#17934=CARTESIAN_POINT('',(-0.037918925522,-0.011788411713,0.018514434973));
#17935=CARTESIAN_POINT('',(-0.037439020962,-0.011726989924,0.018606332456));
#17936=CARTESIAN_POINT('',(-0.037659117901,-0.012119208257,0.018807118231));
#17937=CARTESIAN_POINT('',(-0.037928582819,-0.011767311068,0.018545460028));
#17938=CARTESIAN_POINT('',(-0.037445936687,-0.011706228285,0.018633469683));
#17939=CARTESIAN_POINT('',(-0.037668775198,-0.01209494007,0.018842615969));
#17940=CARTESIAN_POINT('',(-0.037946745879,-0.011723686791,0.018606120592));
#17941=CARTESIAN_POINT('',(-0.037458875717,-0.011663774496,0.018686340803));
#17942=CARTESIAN_POINT('',(-0.037686938258,-0.012044779429,0.018912028045));
#17943=CARTESIAN_POINT('',(-0.03795527555,-0.011701127516,0.01863582313));
#17944=CARTESIAN_POINT('',(-0.037464908394,-0.011642051742,0.018712112891));
#17945=CARTESIAN_POINT('',(-0.037695467929,-0.012018845928,0.018946019049));
#17946=CARTESIAN_POINT('',(-0.037995201404,-0.011584625415,0.018781219738));
#17947=CARTESIAN_POINT('',(-0.037493219634,-0.01153014651,0.018838837483));
#17948=CARTESIAN_POINT('',(-0.037735393783,-0.011884946284,0.019112424772));
#17949=CARTESIAN_POINT('',(-0.03801852767,-0.011479690222,0.018887669477));
#17950=CARTESIAN_POINT('',(-0.037508976952,-0.011433957386,0.018929023907));
#17951=CARTESIAN_POINT('',(-0.037758720049,-0.011764426365,0.019234309833));
#17952=CARTESIAN_POINT('',(-0.038040144091,-0.011303793235,0.019031755487));
#17953=CARTESIAN_POINT('',(-0.037523624808,-0.011276525335,0.019052132642));
#17954=CARTESIAN_POINT('',(-0.03778033647,-0.011562515578,0.019399384648));
#17955=CARTESIAN_POINT('',(-0.038045091154,-0.011241659818,0.019077372673));
#17956=CARTESIAN_POINT('',(-0.037526947936,-0.011221473817,0.019091228452));
#17957=CARTESIAN_POINT('',(-0.037785283533,-0.011491209999,0.019451665162));
#17958=CARTESIAN_POINT('',(-0.038050108278,-0.011114326029,0.019160771595));
#17959=CARTESIAN_POINT('',(-0.037530327064,-0.011109308985,0.019163421876));
#17960=CARTESIAN_POINT('',(-0.037790300657,-0.011345109716,0.019547286114));
#17961=CARTESIAN_POINT('',(-0.038050243047,-0.011048838426,0.019198846514));
#17962=CARTESIAN_POINT('',(-0.037530417095,-0.011052089911,0.019196655463));
#17963=CARTESIAN_POINT('',(-0.037790435426,-0.011269985121,0.019590962239));
#17964=CARTESIAN_POINT('',(-0.038045857381,-0.010914292279,0.019267887587));
#17965=CARTESIAN_POINT('',(-0.037527464034,-0.01093462983,0.019257973428));
#17966=CARTESIAN_POINT('',(-0.03778604976,-0.011115665703,0.019670206775));
#17967=CARTESIAN_POINT('',(-0.038041336883,-0.010845233676,0.019298853626));
#17968=CARTESIAN_POINT('',(-0.037524429559,-0.010874566119,0.019285974336));
#17969=CARTESIAN_POINT('',(-0.037781529262,-0.011036470818,0.019705775052));
#17970=CARTESIAN_POINT('',(-0.038027559938,-0.010703495215,0.019353576094));
#17971=CARTESIAN_POINT('',(-0.037515080889,-0.010750844555,0.019336843363));
#17972=CARTESIAN_POINT('',(-0.037767752317,-0.010873951929,0.019768689912));
#17973=CARTESIAN_POINT('',(-0.038018235775,-0.010630560705,0.019377346763));
#17974=CARTESIAN_POINT('',(-0.037508746133,-0.010687144809,0.019359690396));
#17975=CARTESIAN_POINT('',(-0.037758428154,-0.010790336157,0.019796053532));
#17976=CARTESIAN_POINT('',(-0.037983863425,-0.010411968137,0.019436057889));
#17977=CARTESIAN_POINT('',(-0.037485152239,-0.010495505976,0.019418486321));
#17978=CARTESIAN_POINT('',(-0.037724055805,-0.010539762158,0.019863756543));
#17979=CARTESIAN_POINT('',(-0.03795238138,-0.010264782581,0.019459321592));
#17980=CARTESIAN_POINT('',(-0.037463427014,-0.010365206315,0.0194459996));
#17981=CARTESIAN_POINT('',(-0.037692573758,-0.010371083162,0.019890768551));
#17982=CARTESIAN_POINT('',(-0.037902538675,-0.010079089663,0.019469374787));
#17983=CARTESIAN_POINT('',(-0.037427207905,-0.010194849921,0.0194650503));
#17984=CARTESIAN_POINT('',(-0.037642731053,-0.010158316591,0.019902820673));
#17985=CARTESIAN_POINT('',(-0.0378920119,-0.010041777162,0.019470420515));
#17986=CARTESIAN_POINT('',(-0.037419583631,-0.010160752482,0.019468052396));
#17987=CARTESIAN_POINT('',(-0.037632204279,-0.010115566184,0.019904130213));
#17988=CARTESIAN_POINT('',(-0.037870126119,-0.009967782025,0.019470585011));
#17989=CARTESIAN_POINT('',(-0.0374036129810001,-0.010092740755,0.019472397637));
#17990=CARTESIAN_POINT('',(-0.037610318498,-0.01003079121,0.019904547896));
#17991=CARTESIAN_POINT('',(-0.037858748966,-0.009931022823,0.019469712501));
#17992=CARTESIAN_POINT('',(-0.037395262434,-0.010058774628,0.019473761339));
#17993=CARTESIAN_POINT('',(-0.037598941345,-0.009988678904,0.019903666229));
#17994=CARTESIAN_POINT('',(-0.037823348421,-0.009821438911,0.019464328495));
#17995=CARTESIAN_POINT('',(-0.037369172913,-0.009957259452,0.01947541277));
#17996=CARTESIAN_POINT('',(-0.0375635408,-0.009863142675,0.019897861604));
#17997=CARTESIAN_POINT('',(-0.037798059306,-0.009749306074,0.019457057728));
#17998=CARTESIAN_POINT('',(-0.037350277137,-0.009889495687,0.019473344227));
#17999=CARTESIAN_POINT('',(-0.037538251684,-0.009780517328,0.019889787243));
#18000=CARTESIAN_POINT('',(-0.037744193093,-0.009606821654,0.019435479151));
#18001=CARTESIAN_POINT('',(-0.037309379895,-0.00975396796900001,0.019462636177));
#18002=CARTESIAN_POINT('',(-0.037484385472,-0.009617322054,0.019865602347));
#18003=CARTESIAN_POINT('',(-0.037715615604,-0.009536470315,0.019421170251));
#18004=CARTESIAN_POINT('',(-0.037287455068,-0.009686309278,0.019454099651));
#18005=CARTESIAN_POINT('',(-0.037455807983,-0.00953675241,0.019849490561));
#18006=CARTESIAN_POINT('',(-0.037670271841,-0.009432272932,0.019394506946));
#18007=CARTESIAN_POINT('',(-0.037251993154,-0.009584454943,0.019436123721));
#18008=CARTESIAN_POINT('',(-0.03741046422,-0.009417432004,0.019819385249));
#18009=CARTESIAN_POINT('',(-0.037654725402,-0.009397729381,0.019384735691));
#18010=CARTESIAN_POINT('',(-0.037239813053,-0.009550627271,0.01942931378));
#18011=CARTESIAN_POINT('',(-0.037394917781,-0.009377876793,0.019808341439));
#18012=CARTESIAN_POINT('',(-0.037623119912,-0.009329767162,0.019363680484));
#18013=CARTESIAN_POINT('',(-0.037214887215,-0.00948368581700001,0.019414133917));
#18014=CARTESIAN_POINT('',(-0.037363312291,-0.00930005825,0.019784524364));
#18015=CARTESIAN_POINT('',(-0.037607024828,-0.009296262741,0.019352376907));
#18016=CARTESIAN_POINT('',(-0.037202122033,-0.00945049394300001,0.019405766262));
#18017=CARTESIAN_POINT('',(-0.037347217206,-0.009261696717,0.019771728968));
#18018=CARTESIAN_POINT('',(-0.037525118351,-0.009131050827,0.019292111621));
#18019=CARTESIAN_POINT('',(-0.037137549676,-0.009287907011,0.019360578083));
#18020=CARTESIAN_POINT('',(-0.03726531073,-0.009072543594,0.019703469308));
#18021=CARTESIAN_POINT('',(-0.037455051799,-0.009006209944,0.019232012958));
#18022=CARTESIAN_POINT('',(-0.037080651573,-0.009160611098,0.01931215418));
#18023=CARTESIAN_POINT('',(-0.037195244178,-0.008929642002,0.01963527735));
#18024=CARTESIAN_POINT('',(-0.037343235527,-0.00882937501,0.019125190743));
#18025=CARTESIAN_POINT('',(-0.036986748025,-0.008975129884,0.019219634813));
#18026=CARTESIAN_POINT('',(-0.037083427906,-0.008727272424,0.019513936502));
#18027=CARTESIAN_POINT('',(-0.03730475018,-0.008772089632,0.019086679248));
#18028=CARTESIAN_POINT('',(-0.03695443279,-0.008914916629,0.019185945236));
#18029=CARTESIAN_POINT('',(-0.037044942559,-0.008661723823,0.019470171615));
#18030=CARTESIAN_POINT('',(-0.03722687049,-0.008662929292,0.019005550035));
#18031=CARTESIAN_POINT('',(-0.036888415857,-0.00879911653500001,0.019113533106));
#18032=CARTESIAN_POINT('',(-0.036967062869,-0.008536835522,0.01937794176));
#18033=CARTESIAN_POINT('',(-0.037187320072,-0.008610791877,0.018962790615));
#18034=CARTESIAN_POINT('',(-0.036854627768,-0.008743216033,0.019074796792));
#18035=CARTESIAN_POINT('',(-0.036927512451,-0.008477195434,0.019329315909));
#18036=CARTESIAN_POINT('',(-0.03706685504,-0.008461415123,0.018828228599));
#18037=CARTESIAN_POINT('',(-0.036751742399,-0.00858303382199999,0.018951988873));
#18038=CARTESIAN_POINT('',(-0.036807047419,-0.008306352736,0.019176249766));
#18039=CARTESIAN_POINT('',(-0.03698413842,-0.00837115601,0.018730193296));
#18040=CARTESIAN_POINT('',(-0.036679594089,-0.00848315825100001,0.018859845872));
#18041=CARTESIAN_POINT('',(-0.036724330798,-0.008203164137,0.019064679358));
#18042=CARTESIAN_POINT('',(-0.036813690053,-0.008209181877,0.018517719676));
#18043=CARTESIAN_POINT('',(-0.036528822624,-0.00830111902100001,0.018655023827));
#18044=CARTESIAN_POINT('',(-0.036553882432,-0.008018087581,0.018822772918));
#18045=CARTESIAN_POINT('',(-0.03672806298,-0.008139470644,0.018405905936));
#18046=CARTESIAN_POINT('',(-0.0364522190969999,-0.00822060741400001,0.018545456308));
#18047=CARTESIAN_POINT('',(-0.036468255359,-0.007938489295,0.018695425021));
#18048=CARTESIAN_POINT('',(-0.036556082968,-0.008021465132,0.01817201132));
#18049=CARTESIAN_POINT('',(-0.036296957641,-0.008081939279,0.018312490038));
#18050=CARTESIAN_POINT('',(-0.036296275347,-0.00780388162,0.018428951735));
#18051=CARTESIAN_POINT('',(-0.036469700557,-0.007973146042,0.018049892539));
#18052=CARTESIAN_POINT('',(-0.036218299035,-0.008023023348,0.018189430236));
#18053=CARTESIAN_POINT('',(-0.03620989256,-0.007748843646,0.018289782591));
#18054=CARTESIAN_POINT('',(-0.0363829297,-0.007935966222,0.017922392252));
#18055=CARTESIAN_POINT('',(-0.036137554584,-0.00797535009500001,0.01805745087));
#18056=CARTESIAN_POINT('',(-0.036123122079,-0.007706601765,0.018144438831));
#18057=CARTESIAN_POINT('',(-0.0387712812904549,-1.29145307733547E-11,1.90092953692937E-11));
#18058=CARTESIAN_POINT('',(-0.0363829297,-0.019489230098,0.002088447775));
#18059=CARTESIAN_POINT('',(-0.036137554584,-0.019625886228,0.002121869649));
#18060=CARTESIAN_POINT('',(-0.036123122079,-0.019566845848,0.00239810651));
#18061=CARTESIAN_POINT('',(-0.036296388628,-0.019360563338,0.002056979854));
#18062=CARTESIAN_POINT('',(-0.036059352191,-0.019492100962,0.002097943941));
#18063=CARTESIAN_POINT('',(-0.03603658062,-0.019420241494,0.00236211242));
#18064=CARTESIAN_POINT('',(-0.036211750879,-0.019236205228,0.002014072051));
#18065=CARTESIAN_POINT('',(-0.03598108599,-0.019359587151,0.002061252005));
#18066=CARTESIAN_POINT('',(-0.035951943258,-0.019278561257,0.002312976363));
#18067=CARTESIAN_POINT('',(-0.036046427611,-0.01899593144,0.001905705907));
#18068=CARTESIAN_POINT('',(-0.03582764111,-0.019102466172,0.00196200056));
#18069=CARTESIAN_POINT('',(-0.03578661999,-0.019004843948,0.002188783069));
#18070=CARTESIAN_POINT('',(-0.035965731891,-0.018880003958,0.001840264492));
#18071=CARTESIAN_POINT('',(-0.035752240428,-0.018977419333,0.001900058743));
#18072=CARTESIAN_POINT('',(-0.03570592427,-0.018872794113,0.002113745518));
#18073=CARTESIAN_POINT('',(-0.035867783855,-0.018740766939,0.001742981965));
#18074=CARTESIAN_POINT('',(-0.035659677357,-0.018825445883,0.00180418218));
#18075=CARTESIAN_POINT('',(-0.035607976234,-0.018714208906,0.002002145766));
#18076=CARTESIAN_POINT('',(-0.03584830488,-0.018713153198,0.001722699015));
#18077=CARTESIAN_POINT('',(-0.035641412325,-0.018795533693,0.001784265567));
#18078=CARTESIAN_POINT('',(-0.035588497259,-0.018682758826,0.001978875521));
#18079=CARTESIAN_POINT('',(-0.035810061793,-0.018659082064,0.0016809538));
#18080=CARTESIAN_POINT('',(-0.035605524332,-0.018736905391,0.0017430598));
#18081=CARTESIAN_POINT('',(-0.035550254172,-0.018621177248,0.001930977518));
#18082=CARTESIAN_POINT('',(-0.035791254693,-0.018632563266,0.001659452537));
#18083=CARTESIAN_POINT('',(-0.035587855191,-0.018708112389,0.001721737929));
#18084=CARTESIAN_POINT('',(-0.035531447072,-0.018590975808,0.001906305033));
#18085=CARTESIAN_POINT('',(-0.035735788251,-0.018554552292,0.001593061423));
#18086=CARTESIAN_POINT('',(-0.035535852231,-0.018623571688,0.001655788575));
#18087=CARTESIAN_POINT('',(-0.03547598063,-0.018502133765,0.001830115341));
#18088=CARTESIAN_POINT('',(-0.035700081089,-0.018504601769,0.00154628902));
#18089=CARTESIAN_POINT('',(-0.035502196601,-0.018569127867,0.001608840169));
#18090=CARTESIAN_POINT('',(-0.035440273468,-0.018445251153,0.001776431383));
#18091=CARTESIAN_POINT('',(-0.035596955729,-0.01836101404,0.001398258712));
#18092=CARTESIAN_POINT('',(-0.035405412743,-0.018413252525,0.001459938607));
#18093=CARTESIAN_POINT('',(-0.035337148108,-0.018281744346,0.001606500757));
#18094=CARTESIAN_POINT('',(-0.035533471872,-0.018273557744,0.001289394297));
#18095=CARTESIAN_POINT('',(-0.03534514464,-0.018317127379,0.001348630596));
#18096=CARTESIAN_POINT('',(-0.035273664252,-0.018182166802,0.001481497731));
#18097=CARTESIAN_POINT('',(-0.035462076716,-0.01817592941,0.001138664356));
#18098=CARTESIAN_POINT('',(-0.035277056499,-0.018209299086,0.001192172175));
#18099=CARTESIAN_POINT('',(-0.035202269094,-0.018071016536,0.001308380108));
#18100=CARTESIAN_POINT('',(-0.035448157312,-0.018156936087,0.00110767252));
#18101=CARTESIAN_POINT('',(-0.035263851039,-0.018188427631,0.001160131862));
#18102=CARTESIAN_POINT('',(-0.035188349691,-0.018049393067,0.001272783163));
#18103=CARTESIAN_POINT('',(-0.035421421576,-0.018120522953,0.001044695664));
#18104=CARTESIAN_POINT('',(-0.035238481118,-0.01814840061,0.001094908468));
#18105=CARTESIAN_POINT('',(-0.035161613954,-0.018007938413,0.001200444691));
#18106=CARTESIAN_POINT('',(-0.035408615027,-0.01810311612,0.001012747602));
#18107=CARTESIAN_POINT('',(-0.035226318844,-0.018129247863,0.001061759551));
#18108=CARTESIAN_POINT('',(-0.035148807406,-0.017988121995,0.001163745631));
#18109=CARTESIAN_POINT('',(-0.035371903227,-0.018053301561,0.000915516155));
#18110=CARTESIAN_POINT('',(-0.035191509303,-0.018074518308,0.000960895819));
#18111=CARTESIAN_POINT('',(-0.035112095605,-0.01793141283,0.001052049584));
#18112=CARTESIAN_POINT('',(-0.035349701075,-0.018023292834,0.000848849473));
#18113=CARTESIAN_POINT('',(-0.035170375015,-0.018041410365,0.000891381795));
#18114=CARTESIAN_POINT('',(-0.035089893455,-0.017897252254,0.000975458269));
#18115=CARTESIAN_POINT('',(-0.035310076825,-0.017969873141,0.000711689247));
#18116=CARTESIAN_POINT('',(-0.035132682741,-0.01798250627,0.00074809069));
#18117=CARTESIAN_POINT('',(-0.035050269204,-0.01783644352,0.000817866864));
#18118=CARTESIAN_POINT('',(-0.035292653375,-0.01794646038,0.000641196756));
#18119=CARTESIAN_POINT('',(-0.035116074086,-0.017956629983,0.000674242814));
#18120=CARTESIAN_POINT('',(-0.035032845755,-0.017809793311,0.000736867981));
#18121=CARTESIAN_POINT('',(-0.035270404132,-0.017916617409,0.000532382892));
#18122=CARTESIAN_POINT('',(-0.035094864144,-0.017923641781,0.000560006423));
#18123=CARTESIAN_POINT('',(-0.03501059651,-0.017775824484,0.00061182896));
#18124=CARTESIAN_POINT('',(-0.03526362249,-0.017907532057,0.000495486354));
#18125=CARTESIAN_POINT('',(-0.035088401673,-0.017913601835,0.000521272544));
#18126=CARTESIAN_POINT('',(-0.035003814869,-0.017765483208,0.000569429626));
#18127=CARTESIAN_POINT('',(-0.035251577427,-0.017891408044,0.000421626354));
#18128=CARTESIAN_POINT('',(-0.035076925826,-0.017895786451,0.000443697364));
#18129=CARTESIAN_POINT('',(-0.034991769806,-0.017747130448,0.000484552102));
#18130=CARTESIAN_POINT('',(-0.035246291308,-0.01788433888,0.000384573767));
#18131=CARTESIAN_POINT('',(-0.035071886429,-0.017887970471,0.000404748673));
#18132=CARTESIAN_POINT('',(-0.034986483687,-0.017739084243,0.000441971503));
#18133=CARTESIAN_POINT('',(-0.035223521483,-0.017853905806,0.00019870341));
#18134=CARTESIAN_POINT('',(-0.035050225188,-0.017854392227,0.000209670015));
#18135=CARTESIAN_POINT('',(-0.034963713862,-0.017704445198,0.000228366787));
#18136=CARTESIAN_POINT('',(-0.035216913712,-0.017845112687,4.808316E-5));
#18137=CARTESIAN_POINT('',(-0.035043883179,-0.017844601077,5.0495546E-5));
#18138=CARTESIAN_POINT('',(-0.034957106091,-0.017694437363,5.5260102E-5));
#18139=CARTESIAN_POINT('',(-0.035223876434,-0.017854401084,-0.000142705112));
#18140=CARTESIAN_POINT('',(-0.035050518048,-0.017854867848,-0.00015026669));
#18141=CARTESIAN_POINT('',(-0.034964068813,-0.017705009213,-0.000164006944));
#18142=CARTESIAN_POINT('',(-0.03522604562,-0.017857295098,-0.000181008826));
#18143=CARTESIAN_POINT('',(-0.035052587043,-0.017858069693,-0.000190597666));
#18144=CARTESIAN_POINT('',(-0.034966237999,-0.01770830312,-0.000208027982));
#18145=CARTESIAN_POINT('',(-0.035231850552,-0.017865043926,-0.000256731481));
#18146=CARTESIAN_POINT('',(-0.035058120997,-0.017866638035,-0.000270288381));
#18147=CARTESIAN_POINT('',(-0.034972042931,-0.017717122731,-0.00029505227));
#18148=CARTESIAN_POINT('',(-0.0352354894,-0.01786990288,-0.000294294755));
#18149=CARTESIAN_POINT('',(-0.035061591095,-0.017872012494,-0.000309815542));
#18150=CARTESIAN_POINT('',(-0.034975681779,-0.01772265315,-0.0003382214));
#18151=CARTESIAN_POINT('',(-0.035248550352,-0.017887356278,-0.000406114618));
#18152=CARTESIAN_POINT('',(-0.035074046816,-0.017891317393,-0.000427475545));
#18153=CARTESIAN_POINT('',(-0.034988742731,-0.01774251863,-0.000466726903));
#18154=CARTESIAN_POINT('',(-0.035260111701,-0.017902819307,-0.000479503556));
#18155=CARTESIAN_POINT('',(-0.035085080525,-0.017908432544,-0.000504635436));
#18156=CARTESIAN_POINT('',(-0.03500030408,-0.017760118859,-0.000551064032));
#18157=CARTESIAN_POINT('',(-0.035281577861,-0.017931602322,-0.000587901928));
#18158=CARTESIAN_POINT('',(-0.035105505104,-0.017940189326,-0.000618239168));
#18159=CARTESIAN_POINT('',(-0.03502177024,-0.017792881061,-0.000675626671));
#18160=CARTESIAN_POINT('',(-0.035289421938,-0.017942130116,-0.000623753285));
#18161=CARTESIAN_POINT('',(-0.035112977015,-0.017951817298,-0.000655825409));
#18162=CARTESIAN_POINT('',(-0.035029614317,-0.017804864435,-0.000716823028));
#18163=CARTESIAN_POINT('',(-0.035306476701,-0.017965050902,-0.000694894802));
#18164=CARTESIAN_POINT('',(-0.035129211644,-0.017977114049,-0.000730326682));
#18165=CARTESIAN_POINT('',(-0.03504666908,-0.017830954681,-0.000798568263));
#18166=CARTESIAN_POINT('',(-0.035315718145,-0.017977485365,-0.000730290044));
#18167=CARTESIAN_POINT('',(-0.035138009535,-0.017990837846,-0.000767363366));
#18168=CARTESIAN_POINT('',(-0.035055910524,-0.017845108762,-0.000839237874));
#18169=CARTESIAN_POINT('',(-0.035345244257,-0.018017274364,-0.000834778442));
#18170=CARTESIAN_POINT('',(-0.035166136457,-0.018034776161,-0.000876705266000001));
#18171=CARTESIAN_POINT('',(-0.035085436637,-0.017890401172,-0.000959292019));
#18172=CARTESIAN_POINT('',(-0.035367258146,-0.018047016063,-0.000902026906));
#18173=CARTESIAN_POINT('',(-0.035187092355,-0.018067591645,-0.000946845463));
#18174=CARTESIAN_POINT('',(-0.035107450524,-0.017924257611,-0.001036552565));
#18175=CARTESIAN_POINT('',(-0.035415540032,-0.01811249853,-0.001032054747));
#18176=CARTESIAN_POINT('',(-0.035232955499,-0.018139667727,-0.001082015991));
#18177=CARTESIAN_POINT('',(-0.035155732411,-0.017998802798,-0.001185925847));
#18178=CARTESIAN_POINT('',(-0.035441809443,-0.018148241136,-0.001094832722));
#18179=CARTESIAN_POINT('',(-0.035257918294,-0.018179017227,-0.001147092497));
#18180=CARTESIAN_POINT('',(-0.035182001822,-0.018039493646,-0.001258036973));
#18181=CARTESIAN_POINT('',(-0.035498359317,-0.018225522805,-0.001216100433));
#18182=CARTESIAN_POINT('',(-0.035311533473,-0.018263877422,-0.001272286645));
#18183=CARTESIAN_POINT('',(-0.035238551696,-0.018127478563,-0.001397318651));
#18184=CARTESIAN_POINT('',(-0.035528803299,-0.018267288112,-0.001274848098));
#18185=CARTESIAN_POINT('',(-0.035340397738,-0.018309728944,-0.001332693764));
#18186=CARTESIAN_POINT('',(-0.035268995678,-0.01817503025,-0.001464785336));
#18187=CARTESIAN_POINT('',(-0.035624302868,-0.018398937175,-0.001441946764));
#18188=CARTESIAN_POINT('',(-0.035431143853,-0.018454527567,-0.001504443888));
#18189=CARTESIAN_POINT('',(-0.035364495247,-0.018324926454,-0.001656660391));
#18190=CARTESIAN_POINT('',(-0.035693625065,-0.018495301896,-0.001541838752));
#18191=CARTESIAN_POINT('',(-0.035496770299,-0.018560086634,-0.001605426885));
#18192=CARTESIAN_POINT('',(-0.035433817443,-0.018434657594,-0.001771331198));
#18193=CARTESIAN_POINT('',(-0.035804878296,-0.018651701588,-0.001676100287));
#18194=CARTESIAN_POINT('',(-0.035600812464,-0.018729153932,-0.001738536628));
#18195=CARTESIAN_POINT('',(-0.035545070675,-0.018612771043,-0.001925410518));
#18196=CARTESIAN_POINT('',(-0.035843360668,-0.01870607504,-0.001718396961));
#18197=CARTESIAN_POINT('',(-0.035636958249,-0.018788171317,-0.001780300456));
#18198=CARTESIAN_POINT('',(-0.035583553047,-0.018674696557,-0.001973941769));
#18199=CARTESIAN_POINT('',(-0.035921655233,-0.018817323726,-0.001796776766));
#18200=CARTESIAN_POINT('',(-0.035710302083,-0.018908539739,-0.001856931323));
#18201=CARTESIAN_POINT('',(-0.035661847612,-0.018801403665,-0.002063858322));
#18202=CARTESIAN_POINT('',(-0.035961464931,-0.018874192105,-0.001832902387));
#18203=CARTESIAN_POINT('',(-0.035747535996,-0.018969953338,-0.00189179072));
#18204=CARTESIAN_POINT('',(-0.035701657309,-0.018866177417,-0.002105292476));
#18205=CARTESIAN_POINT('',(-0.036082708725,-0.019048372444,-0.001932563921));
#18206=CARTESIAN_POINT('',(-0.035861344783,-0.019158636987,-0.001987306041));
#18207=CARTESIAN_POINT('',(-0.035822901104,-0.019064581187,-0.00221957399));
#18208=CARTESIAN_POINT('',(-0.036165937985,-0.019169231525,-0.001987458368));
#18209=CARTESIAN_POINT('',(-0.035938765603,-0.019288313365,-0.002037355517));
#18210=CARTESIAN_POINT('',(-0.035906130364,-0.019202261747,-0.00228248524));
#18211=CARTESIAN_POINT('',(-0.036272749616,-0.019326186492,-0.002041954834));
#18212=CARTESIAN_POINT('',(-0.036036325391,-0.019453445768,-0.002083965382));
#18213=CARTESIAN_POINT('',(-0.036012941995,-0.019381080036,-0.002344895831));
#18214=CARTESIAN_POINT('',(-0.036294271622,-0.019357902787,-0.002052147118));
#18215=CARTESIAN_POINT('',(-0.036056160144,-0.019487107185,-0.002092585706));
#18216=CARTESIAN_POINT('',(-0.036034464001,-0.019417215175,-0.002356565423));
#18217=CARTESIAN_POINT('',(-0.036337241164,-0.019421408713,-0.002070948756));
#18218=CARTESIAN_POINT('',(-0.036095695252,-0.019554376812,-0.002108113551));
#18219=CARTESIAN_POINT('',(-0.036077433543,-0.019489570721,-0.002378086456));
#18220=CARTESIAN_POINT('',(-0.036358730845,-0.019453260076,-0.002079581263));
#18221=CARTESIAN_POINT('',(-0.03611543566,-0.019588053885,-0.00211503004));
#18222=CARTESIAN_POINT('',(-0.036098923223,-0.019525861458,-0.002387964418));
#18223=CARTESIAN_POINT('',(-0.036423211553,-0.019549105164,-0.002103217759));
#18224=CARTESIAN_POINT('',(-0.036174782484,-0.019689559821,-0.002133392794));
#18225=CARTESIAN_POINT('',(-0.036163403931,-0.019635067732,-0.002415001427));
#18226=CARTESIAN_POINT('',(-0.036466213928,-0.019613389425,-0.002115965485));
#18227=CARTESIAN_POINT('',(-0.036214084658,-0.01975713597,-0.002142252449));
#18228=CARTESIAN_POINT('',(-0.036206406307,-0.019708316806,-0.002429569065));
#18229=CARTESIAN_POINT('',(-0.036595254777,-0.019807388917,-0.002145346512));
#18230=CARTESIAN_POINT('',(-0.03633245937,-0.019961690258,-0.002159474874));
#18231=CARTESIAN_POINT('',(-0.036335447156,-0.019929380277,-0.002463096114));
#18232=CARTESIAN_POINT('',(-0.036681322249,-0.019938243356,-0.002153193167));
#18233=CARTESIAN_POINT('',(-0.036410235723,-0.020097509831,-0.00215769725));
#18234=CARTESIAN_POINT('',(-0.036421514628,-0.020078502366,-0.002471966356));
#18235=CARTESIAN_POINT('',(-0.03678899075,-0.020103771553,-0.002147749667));
#18236=CARTESIAN_POINT('',(-0.036505370032,-0.020265213313,-0.002139955671));
#18237=CARTESIAN_POINT('',(-0.036529183129,-0.02026715354,-0.002465549917));
#18238=CARTESIAN_POINT('',(-0.036810556304,-0.020137018306,-0.002145885901));
#18239=CARTESIAN_POINT('',(-0.036524605066,-0.020299204976,-0.002135530565));
#18240=CARTESIAN_POINT('',(-0.036550748683,-0.020305045337,-0.002463377054));
#18241=CARTESIAN_POINT('',(-0.036853337272,-0.020203152393,-0.00214063762));
#18242=CARTESIAN_POINT('',(-0.036562661331,-0.020366616451,-0.002125129214));
#18243=CARTESIAN_POINT('',(-0.036593529651,-0.020380420704,-0.002457286744));
#18244=CARTESIAN_POINT('',(-0.036874593816,-0.020236102715,-0.002137253074));
#18245=CARTESIAN_POINT('',(-0.036581516731,-0.020400097569,-0.002119135437));
#18246=CARTESIAN_POINT('',(-0.036614786195,-0.020417976062,-0.002453369195));
#18247=CARTESIAN_POINT('',(-0.036937968442,-0.020334604047,-0.002124834324));
#18248=CARTESIAN_POINT('',(-0.03663781018,-0.020500286578,-0.002098765055));
#18249=CARTESIAN_POINT('',(-0.03667816082,-0.020530245644,-0.002439018114));
#18250=CARTESIAN_POINT('',(-0.03697969206,-0.020399806189,-0.002113539669));
#18251=CARTESIAN_POINT('',(-0.036674489896,-0.020565883365,-0.002082096496));
#18252=CARTESIAN_POINT('',(-0.036719884461,-0.020604564293,-0.002425991486));
#18253=CARTESIAN_POINT('',(-0.037020900622,-0.020464534491,-0.002099215974));
#18254=CARTESIAN_POINT('',(-0.036710197303,-0.02063001576,-0.002062596704));
#18255=CARTESIAN_POINT('',(-0.036761093001,-0.0206783452,-0.002409490732));
#18256=CARTESIAN_POINT('',(-0.0370209006221877,-0.0205293532570174,-0.00239212983048223));
#18257=CARTESIAN_POINT('',(-0.0363829297001963,-0.019417959879229,0.00237985909232116));
#18258=CARTESIAN_POINT('',(-0.0370209006725265,-0.0204645345703645,-0.00209921595643747));
#18259=CARTESIAN_POINT('',(-0.0367101973471479,-0.0206300158392919,-0.00206259667989087));
#18260=CARTESIAN_POINT('',(-0.0367610930515268,-0.0206783452904645,-0.00240949071176802));
#18261=CARTESIAN_POINT('',(-0.037103317012847,-0.0205939899421424,-0.00207056883537586));
#18262=CARTESIAN_POINT('',(-0.0367834353017993,-0.0207615550854043,-0.00202260147516363));
#18263=CARTESIAN_POINT('',(-0.0368435097848469,-0.0208259064844385,-0.00237648933787403));
#18264=CARTESIAN_POINT('',(-0.0371836845969985,-0.0207215678876372,-0.00202989413701114));
#18265=CARTESIAN_POINT('',(-0.036852619292111,-0.0208869959479472,-0.00197074610137332));
#18266=CARTESIAN_POINT('',(-0.0369238769759985,-0.0209713360532264,-0.00232969336136768));
#18267=CARTESIAN_POINT('',(-0.037301116085,-0.020909749705,-0.001949233973));
#18268=CARTESIAN_POINT('',(-0.03695137278,-0.021067368688,-0.001875640572));
#18269=CARTESIAN_POINT('',(-0.037041308464,-0.021185862625,-0.002236969898));
#18270=CARTESIAN_POINT('',(-0.037339424126,-0.020971441729,-0.001919241095));
#18271=CARTESIAN_POINT('',(-0.036983551057,-0.021126386976,-0.001840720983));
#18272=CARTESIAN_POINT('',(-0.037079616505,-0.021256193347,-0.002202501046));
#18273=CARTESIAN_POINT('',(-0.037413681214,-0.021091557342,-0.001853560892));
#18274=CARTESIAN_POINT('',(-0.037045412802,-0.021240237534,-0.00176594903));
#18275=CARTESIAN_POINT('',(-0.037153873593,-0.021393132117,-0.002127037152));
#18276=CARTESIAN_POINT('',(-0.037449744946,-0.021150164712,-0.001817796718));
#18277=CARTESIAN_POINT('',(-0.037075133644,-0.021295144276,-0.001725939277));
#18278=CARTESIAN_POINT('',(-0.037189937325,-0.021459949676,-0.002085953763));
#18279=CARTESIAN_POINT('',(-0.037519742735,-0.021264387507,-0.001740283886));
#18280=CARTESIAN_POINT('',(-0.037132298021,-0.021401075383,-0.001640887915));
#18281=CARTESIAN_POINT('',(-0.037259935114,-0.021590176641,-0.001996928158));
#18282=CARTESIAN_POINT('',(-0.037553677068,-0.021320003507,-0.001698536285));
#18283=CARTESIAN_POINT('',(-0.037159681014,-0.02145199347,-0.001595792365));
#18284=CARTESIAN_POINT('',(-0.037293869447,-0.021653586706,-0.001948987157));
#18285=CARTESIAN_POINT('',(-0.037602938649,-0.021401048787,-0.001631194651));
#18286=CARTESIAN_POINT('',(-0.037198872381,-0.02152506771,-0.00152463845));
#18287=CARTESIAN_POINT('',(-0.037343131027,-0.021745991586,-0.001871665827));
#18288=CARTESIAN_POINT('',(-0.037619085386,-0.02142766668,-0.001607959283));
#18289=CARTESIAN_POINT('',(-0.037211691522,-0.021549005368,-0.00150017865));
#18290=CARTESIAN_POINT('',(-0.037359277765,-0.02177634066,-0.00184498875));
#18291=CARTESIAN_POINT('',(-0.037650817756,-0.021480075164,-0.001559853428));
#18292=CARTESIAN_POINT('',(-0.037236742776,-0.021595846177,-0.001449961208));
#18293=CARTESIAN_POINT('',(-0.037391010135,-0.021836096115,-0.001789760567));
#18294=CARTESIAN_POINT('',(-0.037666411882,-0.021505880156,-0.001534959604));
#18295=CARTESIAN_POINT('',(-0.037248972401,-0.021618745415,-0.001424178176));
#18296=CARTESIAN_POINT('',(-0.037406604261,-0.02186551892,-0.001761182687));
#18297=CARTESIAN_POINT('',(-0.037742059103,-0.021631281365,-0.001407777533));
#18298=CARTESIAN_POINT('',(-0.037308672836,-0.021730666169,-0.001291938074));
#18299=CARTESIAN_POINT('',(-0.037482251481,-0.022008502436,-0.001615186583));
#18300=CARTESIAN_POINT('',(-0.037795953594,-0.021721337673,-0.001296356849));
#18301=CARTESIAN_POINT('',(-0.037349209561,-0.021807099305,-0.001180907653));
#18302=CARTESIAN_POINT('',(-0.037536145973,-0.022111189537,-0.001487307464));
#18303=CARTESIAN_POINT('',(-0.037866774638,-0.021840245218,-0.001114117882));
#18304=CARTESIAN_POINT('',(-0.037401307565,-0.021905583424,-0.001005823865));
#18305=CARTESIAN_POINT('',(-0.037606967016,-0.022246777496,-0.001278179341));
#18306=CARTESIAN_POINT('',(-0.037888699602,-0.021877166648,-0.001050836305));
#18307=CARTESIAN_POINT('',(-0.037417279271,-0.021935830648,-0.000945510459000001));
#18308=CARTESIAN_POINT('',(-0.037628891981,-0.022288878891,-0.001205565251));
#18309=CARTESIAN_POINT('',(-0.037918925522,-0.02192817688,-0.000951846528));
#18310=CARTESIAN_POINT('',(-0.037439020962,-0.02197705154,-0.000852704956));
#18311=CARTESIAN_POINT('',(-0.037659117901,-0.022347046289,-0.001091983109));
#18312=CARTESIAN_POINT('',(-0.037928582819,-0.021944495043,-0.000918060305));
#18313=CARTESIAN_POINT('',(-0.037445936687,-0.021990172249,-0.000821156235));
#18314=CARTESIAN_POINT('',(-0.037668775198,-0.022365654138,-0.001053217373));
#18315=CARTESIAN_POINT('',(-0.037946745879,-0.021975216494,-0.000849950291));
#18316=CARTESIAN_POINT('',(-0.037458875717,-0.022014733087,-0.000757954616));
#18317=CARTESIAN_POINT('',(-0.037686938258,-0.022400686439,-0.000975070946));
#18318=CARTESIAN_POINT('',(-0.03795527555,-0.021989660009,-0.000815562116));
#18319=CARTESIAN_POINT('',(-0.037464908394,-0.022026190993,-0.000726256116));
#18320=CARTESIAN_POINT('',(-0.037695467929,-0.022417156761,-0.000935616373));
#18321=CARTESIAN_POINT('',(-0.037995201404,-0.022057326114,-0.000641970034));
#18322=CARTESIAN_POINT('',(-0.037493219634,-0.022079985093,-0.000565981045));
#18323=CARTESIAN_POINT('',(-0.037735393783,-0.022494318522,-0.000736453018));
#18324=CARTESIAN_POINT('',(-0.03801852767,-0.022097046697,-0.000497868621));
#18325=CARTESIAN_POINT('',(-0.037508976952,-0.022109994265,-0.000437585608));
#18326=CARTESIAN_POINT('',(-0.037758720049,-0.022539614123,-0.000571137177));
#18327=CARTESIAN_POINT('',(-0.038040144091,-0.022133880348,-0.000273494358));
#18328=CARTESIAN_POINT('',(-0.037523624808,-0.022137893532,-0.000239691086));
#18329=CARTESIAN_POINT('',(-0.03778033647,-0.022581617712,-0.000313739898));
#18330=CARTESIAN_POINT('',(-0.038045091154,-0.022142319282,-0.000196876647));
#18331=CARTESIAN_POINT('',(-0.037526947936,-0.022144225738,-0.000172467167));
#18332=CARTESIAN_POINT('',(-0.037785283533,-0.022591241175,-0.000225847199));
#18333=CARTESIAN_POINT('',(-0.038050108278,-0.022150877972,-4.490289E-5));
#18334=CARTESIAN_POINT('',(-0.037530327064,-0.02215066466,-3.9232862E-5));
#18335=CARTESIAN_POINT('',(-0.037790300657,-0.022601001208,-5.1510166E-5));
#18336=CARTESIAN_POINT('',(-0.038050243047,-0.022151108018,3.0848498E-5));
#18337=CARTESIAN_POINT('',(-0.037530417095,-0.022150836255,2.6937103E-5));
#18338=CARTESIAN_POINT('',(-0.037790435426,-0.022601263544,3.5387705E-5));
#18339=CARTESIAN_POINT('',(-0.038045857381,-0.022143626267,0.000181889416));
#18340=CARTESIAN_POINT('',(-0.037527464034,-0.022145209129,0.0001593195));
#18341=CARTESIAN_POINT('',(-0.03778604976,-0.022592731617,0.000208654509));
#18342=CARTESIAN_POINT('',(-0.038041336883,-0.022135914342,0.000257178939));
#18343=CARTESIAN_POINT('',(-0.037524429559,-0.022139426771,0.000225336654));
#18344=CARTESIAN_POINT('',(-0.037781529262,-0.022583937206,0.00029502343));
#18345=CARTESIAN_POINT('',(-0.038027559938,-0.022112436159,0.000407289281));
#18346=CARTESIAN_POINT('',(-0.037515080889,-0.022121619859,0.000357917185));
#18347=CARTESIAN_POINT('',(-0.037767752317,-0.022557163628,0.000467226346));
#18348=CARTESIAN_POINT('',(-0.038018235775,-0.022096554907,0.000482337755));
#18349=CARTESIAN_POINT('',(-0.037508746133,-0.022109556097,0.0004245063));
#18350=CARTESIAN_POINT('',(-0.037758428154,-0.022539053331,0.000553321539));
#18351=CARTESIAN_POINT('',(-0.037983863425,-0.02203810395,0.000701000035));
#18352=CARTESIAN_POINT('',(-0.037485152239,-0.022064655445,0.00061986836));
#18353=CARTESIAN_POINT('',(-0.037724055805,-0.02247239886,0.000804176493));
#18354=CARTESIAN_POINT('',(-0.03795238138,-0.02198465813,0.000840098316));
#18355=CARTESIAN_POINT('',(-0.037463427014,-0.022023332813,0.000746467815999999));
#18356=CARTESIAN_POINT('',(-0.037692573758,-0.022411452447,0.000963762793));
#18357=CARTESIAN_POINT('',(-0.037902538675,-0.021900517993,0.001005939698));
#18358=CARTESIAN_POINT('',(-0.037427207905,-0.021954653006,0.000903526131000001));
#18359=CARTESIAN_POINT('',(-0.037642731053,-0.022315506605,0.001154050109));
#18360=CARTESIAN_POINT('',(-0.0378920119,-0.021882767369,0.001038776136));
#18361=CARTESIAN_POINT('',(-0.037419583631,-0.021940204178,0.000934556427));
#18362=CARTESIAN_POINT('',(-0.037632204279,-0.022295265496,0.001191727817));
#18363=CARTESIAN_POINT('',(-0.037870126119,-0.021845912259,0.001102940053));
#18364=CARTESIAN_POINT('',(-0.037403612981,-0.021909961403,0.000995628931000001));
#18365=CARTESIAN_POINT('',(-0.037610318498,-0.022253239734,0.00126535394));
#18366=CARTESIAN_POINT('',(-0.037858748966,-0.021826777042,0.001134338201));
#18367=CARTESIAN_POINT('',(-0.037395262434,-0.02189415934,0.001025726311));
#18368=CARTESIAN_POINT('',(-0.037598941345,-0.022231420035,0.001301383433));
#18369=CARTESIAN_POINT('',(-0.037823348421,-0.0217673224,0.001226548649));
#18370=CARTESIAN_POINT('',(-0.037369172913,-0.021844831934,0.001114466748));
#18371=CARTESIAN_POINT('',(-0.0375635408,-0.022163624967,0.001407198685));
#18372=CARTESIAN_POINT('',(-0.037798059306,-0.021724959312,0.001285382135));
#18373=CARTESIAN_POINT('',(-0.037350277137,-0.02180915864,0.001172117618));
#18374=CARTESIAN_POINT('',(-0.037538251684,-0.022115319692,0.001474717154));
#18375=CARTESIAN_POINT('',(-0.037744193093,-0.021635029507,0.001397987973));
#18376=CARTESIAN_POINT('',(-0.037309379895,-0.021732121338,0.001284134039));
#18377=CARTESIAN_POINT('',(-0.037484385472,-0.022012777321,0.001603955958));
#18378=CARTESIAN_POINT('',(-0.037715615604,-0.021587461967,0.00145175957));
#18379=CARTESIAN_POINT('',(-0.037287455068,-0.021690899144,0.001338459922));
#18380=CARTESIAN_POINT('',(-0.037455807983,-0.021958539283,0.001665675424));
#18381=CARTESIAN_POINT('',(-0.037670271841,-0.021512272175,0.001528665498));
#18382=CARTESIAN_POINT('',(-0.037251993154,-0.021624404365,0.001417680399));
#18383=CARTESIAN_POINT('',(-0.03741046422,-0.021872807115,0.001753957271));
#18384=CARTESIAN_POINT('',(-0.037654725402,-0.021486538245,0.001553695464));
#18385=CARTESIAN_POINT('',(-0.037239813053,-0.021601592947,0.001443571051));
#18386=CARTESIAN_POINT('',(-0.037394917781,-0.021843465289,0.001782691183));
#18387=CARTESIAN_POINT('',(-0.037623119912,-0.02143432279,0.001602024868));
#18388=CARTESIAN_POINT('',(-0.037214887215,-0.021554976073,0.00149395412));
#18389=CARTESIAN_POINT('',(-0.037363312291,-0.021783929826,0.001838175481));
#18390=CARTESIAN_POINT('',(-0.037607024828,-0.021407781395,0.001625388759));
#18391=CARTESIAN_POINT('',(-0.037202122033,-0.021531133535,0.001518515298));
#18392=CARTESIAN_POINT('',(-0.037347217206,-0.021753667921,0.001864999845));
#18393=CARTESIAN_POINT('',(-0.037525118351,-0.02127298417,0.001738333831));
#18394=CARTESIAN_POINT('',(-0.037137549676,-0.021410705958,0.001636725622));
#18395=CARTESIAN_POINT('',(-0.03726531073,-0.02159997676,0.001994681424));
#18396=CARTESIAN_POINT('',(-0.037455051799,-0.02115851676,0.001816399876));
#18397=CARTESIAN_POINT('',(-0.037080651573,-0.021305121671,0.001722755165));
#18398=CARTESIAN_POINT('',(-0.037195244178,-0.021469469996,0.002084341855));
#18399=CARTESIAN_POINT('',(-0.037343235527,-0.020977588541,0.001916132313));
#18400=CARTESIAN_POINT('',(-0.036986748025,-0.021132256941,0.001837126924));
#18401=CARTESIAN_POINT('',(-0.037083427906,-0.021263200951,0.002198928626));
#18402=CARTESIAN_POINT('',(-0.03730475018,-0.020915593919,0.001946487158));
#18403=CARTESIAN_POINT('',(-0.03695443279,-0.021072974284,0.001872428345));
#18404=CARTESIAN_POINT('',(-0.037044942559,-0.021192525146,0.002233812936));
#18405=CARTESIAN_POINT('',(-0.03722687049,-0.020790753789,0.002000458179));
#18406=CARTESIAN_POINT('',(-0.036888415857,-0.020952363493,0.001936508103));
#18407=CARTESIAN_POINT('',(-0.036967062869,-0.021050207598,0.00229585445));
#18408=CARTESIAN_POINT('',(-0.037187320072,-0.020727654338,0.002024230796));
#18409=CARTESIAN_POINT('',(-0.036854627768,-0.020890866611,0.001965551201));
#18410=CARTESIAN_POINT('',(-0.036927512451,-0.020978276332,0.002323191356));
#18411=CARTESIAN_POINT('',(-0.03706685504,-0.020536431836,0.002086313851));
#18412=CARTESIAN_POINT('',(-0.036751742399,-0.020704420727,0.002042869105));
#18413=CARTESIAN_POINT('',(-0.036807047419,-0.020760295815,0.0023946124));
#18414=CARTESIAN_POINT('',(-0.03698413842,-0.020406401217,0.002115462885));
#18415=CARTESIAN_POINT('',(-0.036679594089,-0.020574684762,0.002083292386));
#18416=CARTESIAN_POINT('',(-0.036724330798,-0.020612078707,0.002428191144));
#18417=CARTESIAN_POINT('',(-0.036813690053,-0.020141406598,0.002149499788));
#18418=CARTESIAN_POINT('',(-0.036528822624,-0.020306284053,0.002138531962));
#18419=CARTESIAN_POINT('',(-0.036553882432,-0.020310043308,0.002467518924));
#18420=CARTESIAN_POINT('',(-0.03672806298,-0.020009717442,0.002153964617));
#18421=CARTESIAN_POINT('',(-0.036452219097,-0.020171139995,0.002153473299));
#18422=CARTESIAN_POINT('',(-0.036468255359,-0.020159957651,0.002472779113));
#18423=CARTESIAN_POINT('',(-0.036556082968,-0.019748156007,0.00213921308));
#18424=CARTESIAN_POINT('',(-0.036296957641,-0.019900051219,0.002157080292));
#18425=CARTESIAN_POINT('',(-0.036296275347,-0.019861881178,0.002456116136));
#18426=CARTESIAN_POINT('',(-0.036469700557,-0.019618238496,0.002119999249));
#18427=CARTESIAN_POINT('',(-0.036218299035,-0.019764020339,0.002146573084));
#18428=CARTESIAN_POINT('',(-0.03620989256,-0.019713838176,0.002434195848));
#18429=CARTESIAN_POINT('',(-0.0363829297,-0.019489230098,0.002088447775));
#18430=CARTESIAN_POINT('',(-0.036137554584,-0.019625886228,0.002121869649));
#18431=CARTESIAN_POINT('',(-0.036123122079,-0.019566845848,0.00239810651));
#18432=CARTESIAN_POINT('',(-0.0387712812776744,-1.75917835919922E-11,3.89705915929546E-17));
#18433=CARTESIAN_POINT('',(-0.0363829297,-0.011553263876,-0.015833944478));
#18434=CARTESIAN_POINT('',(-0.036137554584,-0.011650536133,-0.015935581221));
#18435=CARTESIAN_POINT('',(-0.036123122079,-0.011860244082,-0.015746332321));
#18436=CARTESIAN_POINT('',(-0.036296388628,-0.011461678478,-0.015738249755));
#18437=CARTESIAN_POINT('',(-0.036059352191,-0.01156292323,-0.015831682636));
#18438=CARTESIAN_POINT('',(-0.03603658062,-0.011755770109,-0.015637366271));
#18439=CARTESIAN_POINT('',(-0.036211750879,-0.011362340175,-0.015652006375));
#18440=CARTESIAN_POINT('',(-0.03598108599,-0.011464890175,-0.015735268277));
#18441=CARTESIAN_POINT('',(-0.035951943258,-0.011642376917,-0.015539235616));
#18442=CARTESIAN_POINT('',(-0.036046427611,-0.011148355448,-0.015498106242));
#18443=CARTESIAN_POINT('',(-0.03582764111,-0.011250375413,-0.0155622207));
#18444=CARTESIAN_POINT('',(-0.03578661999,-0.011397963715,-0.015364286119));
#18445=CARTESIAN_POINT('',(-0.035965731891,-0.011033717779,-0.015430430805));
#18446=CARTESIAN_POINT('',(-0.035752240428,-0.011134208806,-0.015484897869));
#18447=CARTESIAN_POINT('',(-0.03570592427,-0.011266954373,-0.015287446383));
#18448=CARTESIAN_POINT('',(-0.035867783855,-0.01087985013,-0.015358489273));
#18449=CARTESIAN_POINT('',(-0.035659677357,-0.010975190542,-0.015401223282));
#18450=CARTESIAN_POINT('',(-0.035607976234,-0.011091013549,-0.015205907441));
#18451=CARTESIAN_POINT('',(-0.03584830488,-0.010848477709,-0.015344716547));
#18452=CARTESIAN_POINT('',(-0.035641412325,-0.010942986155,-0.015385276872));
#18453=CARTESIAN_POINT('',(-0.035588497259,-0.011055135885,-0.015190305996));
#18454=CARTESIAN_POINT('',(-0.035810061793,-0.010785289725,-0.015318762179));
#18455=CARTESIAN_POINT('',(-0.035605524332,-0.010877986763,-0.015355106157));
#18456=CARTESIAN_POINT('',(-0.035550254172,-0.010982864209,-0.015160923786));
#18457=CARTESIAN_POINT('',(-0.035791254693,-0.010753409687,-0.015306546858));
#18458=CARTESIAN_POINT('',(-0.035587855191,-0.01084512498,-0.015340831622));
#18459=CARTESIAN_POINT('',(-0.035531447072,-0.01094639649,-0.015147104814));
#18460=CARTESIAN_POINT('',(-0.035735788251,-0.010656907808,-0.015272182929));
#18461=CARTESIAN_POINT('',(-0.035535852231,-0.010745740813,-0.015300591903));
#18462=CARTESIAN_POINT('',(-0.03547598063,-0.01083599326,-0.015108260194));
#18463=CARTESIAN_POINT('',(-0.035700081089,-0.010591426457,-0.015252310709));
#18464=CARTESIAN_POINT('',(-0.035502196601,-0.010677860391,-0.015276916375));
#18465=CARTESIAN_POINT('',(-0.035440273468,-0.010761060282,-0.015085840387));
#18466=CARTESIAN_POINT('',(-0.035596955729,-0.010391434585,-0.015201975242));
#18467=CARTESIAN_POINT('',(-0.035405412743,-0.010470970184,-0.015216375149));
#18468=CARTESIAN_POINT('',(-0.035337148108,-0.01053214264,-0.01502920465));
#18469=CARTESIAN_POINT('',(-0.035533471872,-0.010253427089,-0.015180668075));
#18470=CARTESIAN_POINT('',(-0.03534514464,-0.010326512046,-0.015188782336));
#18471=CARTESIAN_POINT('',(-0.035273664252,-0.010374098072,-0.015005469481));
#18472=CARTESIAN_POINT('',(-0.035462076716,-0.010074076964,-0.015171484429));
#18473=CARTESIAN_POINT('',(-0.035277056499,-0.010137100933,-0.015173629506));
#18474=CARTESIAN_POINT('',(-0.035202269094,-0.01016859868,-0.014995769339));
#18475=CARTESIAN_POINT('',(-0.035448157312,-0.010037740585,-0.015170531646));
#18476=CARTESIAN_POINT('',(-0.035263851039,-0.01009891748,-0.015171574453));
#18477=CARTESIAN_POINT('',(-0.035188349691,-0.010126959086,-0.014994841338));
#18478=CARTESIAN_POINT('',(-0.035421421576,-0.009964994461,-0.015170485375));
#18479=CARTESIAN_POINT('',(-0.035238481118,-0.010022418853,-0.015169521732));
#18480=CARTESIAN_POINT('',(-0.035161613954,-0.010043584805,-0.01499510979));
#18481=CARTESIAN_POINT('',(-0.035408615027,-0.009928623211,-0.015171384646));
#18482=CARTESIAN_POINT('',(-0.035226318844,-0.00998413467599999,-0.015169509426));
#18483=CARTESIAN_POINT('',(-0.035148807406,-0.010001894278,-0.014996297799));
#18484=CARTESIAN_POINT('',(-0.035371903227,-0.009819511029,-0.015176859697));
#18485=CARTESIAN_POINT('',(-0.035191509303,-0.009869419344,-0.015172544106));
#18486=CARTESIAN_POINT('',(-0.035112095605,-0.00987680808,-0.015003034244));
#18487=CARTESIAN_POINT('',(-0.035349701075,-0.009746771624,-0.015184204718));
#18488=CARTESIAN_POINT('',(-0.035170375015,-0.009792664461,-0.015178628799));
#18489=CARTESIAN_POINT('',(-0.035089893455,-0.009793397768,-0.015011745976));
#18490=CARTESIAN_POINT('',(-0.035310076825,-0.009601277538,-0.015206522019));
#18491=CARTESIAN_POINT('',(-0.035132682741,-0.009639118677,-0.015199261909));
#18492=CARTESIAN_POINT('',(-0.035050269204,-0.009626515241,-0.01503787977));
#18493=CARTESIAN_POINT('',(-0.035292653375,-0.00952852287,-0.015221492219));
#18494=CARTESIAN_POINT('',(-0.035116074086,-0.009562226397,-0.015213776324));
#18495=CARTESIAN_POINT('',(-0.035032845755,-0.009543043046,-0.015055299453));
#18496=CARTESIAN_POINT('',(-0.035270404132,-0.009419365813,-0.015250054381));
#18497=CARTESIAN_POINT('',(-0.035094864144,-0.009446800679,-0.015242325899));
#18498=CARTESIAN_POINT('',(-0.03501059651,-0.009417771664,-0.015088401097));
#18499=CARTESIAN_POINT('',(-0.03526362249,-0.009382869798,-0.015260634503));
#18500=CARTESIAN_POINT('',(-0.035088401673,-0.009408236182,-0.01525299799));
#18501=CARTESIAN_POINT('',(-0.035003814869,-0.009375882126,-0.015100644955));
#18502=CARTESIAN_POINT('',(-0.035251577427,-0.009310843156,-0.015283600698));
#18503=CARTESIAN_POINT('',(-0.035076925826,-0.00933214641500001,-0.015276357005));
#18504=CARTESIAN_POINT('',(-0.034991769806,-0.009293199654,-0.015127189761));
#18505=CARTESIAN_POINT('',(-0.035246291308,-0.009275220092,-0.015296004916));
#18506=CARTESIAN_POINT('',(-0.035071886429,-0.009294507868,-0.015289062514));
#18507=CARTESIAN_POINT('',(-0.034986483687,-0.009252300671,-0.015141511843));
#18508=CARTESIAN_POINT('',(-0.035223521483,-0.009099035104,-0.015362584279));
#18509=CARTESIAN_POINT('',(-0.035050225188,-0.00910877567300001,-0.01535752223));
#18510=CARTESIAN_POINT('',(-0.034963713862,-0.009049994038,-0.015218315908));
#18511=CARTESIAN_POINT('',(-0.035216913712,-0.008964197582,-0.015430279341));
#18512=CARTESIAN_POINT('',(-0.035043883179,-0.008966030964,-0.01542863008));
#18513=CARTESIAN_POINT('',(-0.034957106091,-0.008895075333,-0.015296202211));
#18514=CARTESIAN_POINT('',(-0.035223876434,-0.00880361429,-0.015533717464));
#18515=CARTESIAN_POINT('',(-0.035050518048,-0.008797299153,-0.015537902482));
#18516=CARTESIAN_POINT('',(-0.034964068813,-0.008710470427,-0.015414991225));
#18517=CARTESIAN_POINT('',(-0.03522604562,-0.008771889308,-0.015555375611));
#18518=CARTESIAN_POINT('',(-0.035052587043,-0.008763972426,-0.01556084085));
#18519=CARTESIAN_POINT('',(-0.034966237999,-0.008673994043,-0.015439854351));
#18520=CARTESIAN_POINT('',(-0.035231850552,-0.008710185979,-0.01559994762));
#18521=CARTESIAN_POINT('',(-0.035058120997,-0.008699242413,-0.015608106609));
#18522=CARTESIAN_POINT('',(-0.034972042931,-0.008603038604,-0.015491004502));
#18523=CARTESIAN_POINT('',(-0.0352354894,-0.008680084706,-0.015622937235));
#18524=CARTESIAN_POINT('',(-0.035061591095,-0.008667698117,-0.015632524608));
#18525=CARTESIAN_POINT('',(-0.034975681779,-0.008568418251,-0.01551737855));
#18526=CARTESIAN_POINT('',(-0.035248550352,-0.008591972563,-0.015693962252));
#18527=CARTESIAN_POINT('',(-0.035074046816,-0.008575454015,-0.015708073142));
#18528=CARTESIAN_POINT('',(-0.034988742731,-0.008467061961,-0.015598835312));
#18529=CARTESIAN_POINT('',(-0.035260111701,-0.008536147393,-0.015744048097));
#18530=CARTESIAN_POINT('',(-0.035085080525,-0.008517189165,-0.015761475243));
#18531=CARTESIAN_POINT('',(-0.03500030408,-0.008402823979,-0.015656246123));
#18532=CARTESIAN_POINT('',(-0.035281577861,-0.008456663156,-0.015823174106));
#18533=CARTESIAN_POINT('',(-0.035105505104,-0.008434683838,-0.015845779289));
#18534=CARTESIAN_POINT('',(-0.03502177024,-0.00831133067,-0.015746900341));
#18535=CARTESIAN_POINT('',(-0.035289421938,-0.008430878868,-0.015850217121));
#18536=CARTESIAN_POINT('',(-0.035112977015,-0.008407947185,-0.015874642529));
#18537=CARTESIAN_POINT('',(-0.035029614317,-0.008281645265,-0.015777876425));
#18538=CARTESIAN_POINT('',(-0.035306476701,-0.008380728899,-0.015905637862));
#18539=CARTESIAN_POINT('',(-0.035129211644,-0.008356075565,-0.015933800795));
#18540=CARTESIAN_POINT('',(-0.03504666908,-0.008223896938,-0.015841343859));
#18541=CARTESIAN_POINT('',(-0.035315718145,-0.008356292952,-0.015934104044));
#18542=CARTESIAN_POINT('',(-0.035138009535,-0.00833086275400001,-0.015964204293));
#18543=CARTESIAN_POINT('',(-0.035055910524,-0.008195753062,-0.015873936458));
#18544=CARTESIAN_POINT('',(-0.035345244257,-0.008285697845,-0.016020806527));
#18545=CARTESIAN_POINT('',(-0.035166136457,-0.00825813904900001,-0.01605692694));
#18546=CARTESIAN_POINT('',(-0.035085436637,-0.008114429329,-0.015973187908));
#18547=CARTESIAN_POINT('',(-0.035367258146,-0.008242329816,-0.016080187826));
#18548=CARTESIAN_POINT('',(-0.035187092355,-0.008213803598,-0.016120416082));
#18549=CARTESIAN_POINT('',(-0.035107450524,-0.008064447951,-0.016041138718));
#18550=CARTESIAN_POINT('',(-0.035415540032,-0.008162463636,-0.016201911227));
#18551=CARTESIAN_POINT('',(-0.035232955499,-0.008132780528,-0.016250421064));
#18552=CARTESIAN_POINT('',(-0.035155732411,-0.007972359488,-0.016180383385));
#18553=CARTESIAN_POINT('',(-0.035441809443,-0.008125967618,-0.016264254219));
#18554=CARTESIAN_POINT('',(-0.035257918294,-0.008096097371,-0.016317036983));
#18555=CARTESIAN_POINT('',(-0.035182001822,-0.007930254845,-0.016251678255));
#18556=CARTESIAN_POINT('',(-0.035498359317,-0.008059587534,-0.016391815963));
#18557=CARTESIAN_POINT('',(-0.035311533473,-0.00803010615599999,-0.016453125142));
#18558=CARTESIAN_POINT('',(-0.035238551696,-0.007853625833,-0.016397516267));
#18559=CARTESIAN_POINT('',(-0.035528803299,-0.008029593217,-0.016457359612));
#18560=CARTESIAN_POINT('',(-0.035340397738,-0.008000717817,-0.016523037284));
#18561=CARTESIAN_POINT('',(-0.035268995678,-0.007818973813,-0.016472430579));
#18562=CARTESIAN_POINT('',(-0.035624302868,-0.007950706059,-0.016654920378));
#18563=CARTESIAN_POINT('',(-0.035431143853,-0.00792437715800001,-0.016734311632));
#18564=CARTESIAN_POINT('',(-0.035364495247,-0.007727753242,-0.016698182027));
#18565=CARTESIAN_POINT('',(-0.035693625065,-0.00791237942,-0.016788320669));
#18566=CARTESIAN_POINT('',(-0.035496770299,-0.00788970285099999,-0.016876219964));
#18567=CARTESIAN_POINT('',(-0.035433817443,-0.007683310981,-0.016850547386));
#18568=CARTESIAN_POINT('',(-0.035804878296,-0.007874305366,-0.016990897542));
#18569=CARTESIAN_POINT('',(-0.035600812464,-0.007858960081,-0.01708919141));
#18570=CARTESIAN_POINT('',(-0.035545070675,-0.0076389311,-0.017081837817));
#18571=CARTESIAN_POINT('',(-0.035843360668,-0.007864862098,-0.01705913467));
#18572=CARTESIAN_POINT('',(-0.035636958249,-0.007852300237,-0.017161183879));
#18573=CARTESIAN_POINT('',(-0.035583553047,-0.007627864561,-0.017159732511));
#18574=CARTESIAN_POINT('',(-0.035921655233,-0.007852607539,-0.017194668761));
#18575=CARTESIAN_POINT('',(-0.035710302083,-0.00784612017,-0.017303741424));
#18576=CARTESIAN_POINT('',(-0.035661847612,-0.007613348096,-0.017314422362));
#18577=CARTESIAN_POINT('',(-0.035961464931,-0.007849756022,-0.017261981032));
#18578=CARTESIAN_POINT('',(-0.035747535996,-0.00784663784700001,-0.017374356859));
#18579=CARTESIAN_POINT('',(-0.035701657309,-0.007609851942,-0.017391235154));
#18580=CARTESIAN_POINT('',(-0.036082708725,-0.007850536771,-0.017462656398));
#18581=CARTESIAN_POINT('',(-0.035861344783,-0.007858260977,-0.017585519353));
#18582=CARTESIAN_POINT('',(-0.035822901104,-0.007610083132,-0.017620198615));
#18583=CARTESIAN_POINT('',(-0.036165937985,-0.007863426326,-0.017594770655));
#18584=CARTESIAN_POINT('',(-0.035938765603,-0.00787975504899999,-0.017722847129));
#18585=CARTESIAN_POINT('',(-0.035906130364,-0.007624440672,-0.017770889103));
#18586=CARTESIAN_POINT('',(-0.036272749616,-0.007894708486,-0.017757945878));
#18587=CARTESIAN_POINT('',(-0.036036325391,-0.007921955923,-0.017889160917));
#18588=CARTESIAN_POINT('',(-0.036012941995,-0.007659800659,-0.017956955579));
#18589=CARTESIAN_POINT('',(-0.036294271622,-0.007901739857,-0.017790509137));
#18590=CARTESIAN_POINT('',(-0.036056160144,-0.00793132121100001,-0.017922622722));
#18591=CARTESIAN_POINT('',(-0.036034464001,-0.007667762066,-0.017994084324));
#18592=CARTESIAN_POINT('',(-0.036337241164,-0.007917210124,-0.017854907701));
#18593=CARTESIAN_POINT('',(-0.036095695252,-0.007951508517,-0.01798864385));
#18594=CARTESIAN_POINT('',(-0.036077433543,-0.007685302077,-0.018067506581));
#18595=CARTESIAN_POINT('',(-0.036358730845,-0.007925659835,-0.017886808044));
#18596=CARTESIAN_POINT('',(-0.03611543566,-0.007962357198,-0.018021267296));
#18597=CARTESIAN_POINT('',(-0.036098923223,-0.00769489288,-0.018103874262));
#18598=CARTESIAN_POINT('',(-0.036423211553,-0.007953112573,-0.017981630573));
#18599=CARTESIAN_POINT('',(-0.036174782484,-0.007997207555,-0.018118355391));
#18600=CARTESIAN_POINT('',(-0.036163403931,-0.00772608128,-0.018211968175));
#18601=CARTESIAN_POINT('',(-0.036466213928,-0.007974214849,-0.018043676239));
#18602=CARTESIAN_POINT('',(-0.036214084658,-0.008023322943,-0.01818130788));
#18603=CARTESIAN_POINT('',(-0.036206406307,-0.007750089872,-0.018282687553));
#18604=CARTESIAN_POINT('',(-0.036595254777,-0.008045769879,-0.018226375241));
#18605=CARTESIAN_POINT('',(-0.03633245937,-0.008110685029,-0.018367068303));
#18606=CARTESIAN_POINT('',(-0.036335447156,-0.007831586332,-0.018490897658));
#18607=CARTESIAN_POINT('',(-0.036681322249,-0.008104401696,-0.018343621837));
#18608=CARTESIAN_POINT('',(-0.036410235723,-0.00818013428299999,-0.018483802691));
#18609=CARTESIAN_POINT('',(-0.036421514628,-0.007898465521,-0.018624476296));
#18610=CARTESIAN_POINT('',(-0.03678899075,-0.008191880004,-0.01848425171));
#18611=CARTESIAN_POINT('',(-0.036505370032,-0.008279350682,-0.018620167377));
#18612=CARTESIAN_POINT('',(-0.036529183129,-0.007998347907,-0.018784644787));
#18613=CARTESIAN_POINT('',(-0.036810556304,-0.008210117449,-0.01851211236));
#18614=CARTESIAN_POINT('',(-0.036524605066,-0.00830017876800001,-0.018647392468));
#18615=CARTESIAN_POINT('',(-0.036550748683,-0.00801917556,-0.018816373614));
#18616=CARTESIAN_POINT('',(-0.036853337272,-0.008247729637,-0.018566762019));
#18617=CARTESIAN_POINT('',(-0.036562661331,-0.00834289234,-0.018700571843));
#18618=CARTESIAN_POINT('',(-0.036593529651,-0.008062137607,-0.018878605442));
#18619=CARTESIAN_POINT('',(-0.036874593816,-0.008267135902,-0.018593605562));
#18620=CARTESIAN_POINT('',(-0.036581516731,-0.008364823662,-0.018726570453));
#18621=CARTESIAN_POINT('',(-0.036614786195,-0.008084307983,-0.018909170561));
#18622=CARTESIAN_POINT('',(-0.036937968442,-0.00832714152,-0.018672700842));
#18623=CARTESIAN_POINT('',(-0.03663781018,-0.008432559434,-0.018803151489));
#18624=CARTESIAN_POINT('',(-0.03667816082,-0.008152871175,-0.01899922333));
#18625=CARTESIAN_POINT('',(-0.03697969206,-0.008369524049,-0.018723520226));
#18626=CARTESIAN_POINT('',(-0.036674489896,-0.008479793224,-0.018851625693));
#18627=CARTESIAN_POINT('',(-0.036719884461,-0.00820131189,-0.019057071854));
#18628=CARTESIAN_POINT('',(-0.037020900622,-0.008414292884,-0.018772414733));
#18629=CARTESIAN_POINT('',(-0.036710197303,-0.008528746736,-0.01889741608));
#18630=CARTESIAN_POINT('',(-0.036761093001,-0.008252492416,-0.019112717618));
#18631=CARTESIAN_POINT('',(-0.0370209006225329,-0.00819303142614902,-0.0189750063603988));
#18632=CARTESIAN_POINT('',(-0.036382929700134,-0.0117699983702051,-0.0156265169988628));
#18633=CARTESIAN_POINT('',(-0.0370209006725265,-0.00841429293889186,-0.0187724147929504));
#18634=CARTESIAN_POINT('',(-0.0367101973471479,-0.00852874679652509,-0.0188974161366143));
#18635=CARTESIAN_POINT('',(-0.0367610930515268,-0.00825249247875368,-0.0191127176862286));
#18636=CARTESIAN_POINT('',(-0.037103317012847,-0.00850382975946811,-0.0188702028728446));
#18637=CARTESIAN_POINT('',(-0.0367834353017993,-0.00862915328424695,-0.0189913348642332));
#18638=CARTESIAN_POINT('',(-0.0368435097848469,-0.00835485310428282,-0.0192240087409122));
#18639=CARTESIAN_POINT('',(-0.0371836845969985,-0.00860284405433526,-0.018960351265708));
#18640=CARTESIAN_POINT('',(-0.036852619292111,-0.00873678178590861,-0.0190740421504255));
#18641=CARTESIAN_POINT('',(-0.0369238769759985,-0.0084680943925531,-0.0193265564529946));
#18642=CARTESIAN_POINT('',(-0.037301116085,-0.008766788714,-0.019082991418));
#18643=CARTESIAN_POINT('',(-0.03695137278,-0.00890933196000001,-0.019182696761));
#18644=CARTESIAN_POINT('',(-0.037041308464,-0.008655658553,-0.019465980183));
#18645=CARTESIAN_POINT('',(-0.037339424126,-0.008823609321,-0.019121421839));
#18646=CARTESIAN_POINT('',(-0.036983551057,-0.00896908235600001,-0.019216348303));
#18647=CARTESIAN_POINT('',(-0.037079616505,-0.008720674816,-0.019509653949));
#18648=CARTESIAN_POINT('',(-0.037413681214,-0.008940547851,-0.01919260491));
#18649=CARTESIAN_POINT('',(-0.037045412802,-0.00909076204500001,-0.019277559802));
#18650=CARTESIAN_POINT('',(-0.037153873593,-0.00885449785,-0.019590514456));
#18651=CARTESIAN_POINT('',(-0.037449744946,-0.00900082422,-0.019225478294));
#18652=CARTESIAN_POINT('',(-0.037075133644,-0.009152864878,-0.019305105559));
#18653=CARTESIAN_POINT('',(-0.037189937325,-0.008923485888,-0.019627838465));
#18654=CARTESIAN_POINT('',(-0.037519742735,-0.009125063699,-0.01928564172));
#18655=CARTESIAN_POINT('',(-0.037132298021,-0.00927948707199999,-0.019354318908));
#18656=CARTESIAN_POINT('',(-0.037259935114,-0.009065697806,-0.019696105522));
#18657=CARTESIAN_POINT('',(-0.037553677068,-0.009189026182,-0.019312932788));
#18658=CARTESIAN_POINT('',(-0.037159681014,-0.00934400000800001,-0.019375867489));
#18659=CARTESIAN_POINT('',(-0.037293869447,-0.009138920963,-0.019727049749));
#18660=CARTESIAN_POINT('',(-0.037602938649,-0.009287868388,-0.019349449243));
#18661=CARTESIAN_POINT('',(-0.037198872381,-0.009442158226,-0.01940357468));
#18662=CARTESIAN_POINT('',(-0.037343131027,-0.009252085639,-0.019768414058));
#18663=CARTESIAN_POINT('',(-0.037619085386,-0.009321299752,-0.01936088333));
#18664=CARTESIAN_POINT('',(-0.037211691522,-0.009475309863,-0.0194120754));
#18665=CARTESIAN_POINT('',(-0.037359277765,-0.009290363203,-0.019781358588));
#18666=CARTESIAN_POINT('',(-0.037650817756,-0.009389164887,-0.019382217481));
#18667=CARTESIAN_POINT('',(-0.037236742776,-0.009542219848,-0.019427532009));
#18668=CARTESIAN_POINT('',(-0.037391010135,-0.00936806994,-0.019805494239));
#18669=CARTESIAN_POINT('',(-0.037666411882,-0.009423626067,-0.019392118348));
#18670=CARTESIAN_POINT('',(-0.037248972401,-0.00957599822699999,-0.019434471815));
#18671=CARTESIAN_POINT('',(-0.037406604261,-0.009407530512,-0.019816686195));
#18672=CARTESIAN_POINT('',(-0.037742059103,-0.009596469576,-0.019437127945));
#18673=CARTESIAN_POINT('',(-0.037308672836,-0.009746481892,-0.019465277981));
#18674=CARTESIAN_POINT('',(-0.037482251481,-0.009605458605,-0.0198675155));
#18675=CARTESIAN_POINT('',(-0.037795953594,-0.009737990873,-0.019459408654));
#18676=CARTESIAN_POINT('',(-0.037349209561,-0.00988085362499999,-0.019475955808));
#18677=CARTESIAN_POINT('',(-0.037536145973,-0.009767548722,-0.019892505579));
#18678=CARTESIAN_POINT('',(-0.037866774638,-0.00995526822,-0.019471266124));
#18679=CARTESIAN_POINT('',(-0.037401307565,-0.010081722694,-0.019473703662));
#18680=CARTESIAN_POINT('',(-0.037606967016,-0.010016452968,-0.019905364135));
#18681=CARTESIAN_POINT('',(-0.037888699602,-0.010028532389,-0.019471600233));
#18682=CARTESIAN_POINT('',(-0.037417279271,-0.010149079247,-0.019469741824));
#18683=CARTESIAN_POINT('',(-0.037628891981,-0.010100389312,-0.019905517967));
#18684=CARTESIAN_POINT('',(-0.037918925522,-0.010139765166,-0.0194662815));
#18685=CARTESIAN_POINT('',(-0.037439020962,-0.010250061616,-0.019459037412));
#18686=CARTESIAN_POINT('',(-0.037659117901,-0.010227838031,-0.01989910134));
#18687=CARTESIAN_POINT('',(-0.037928582819,-0.010177183975,-0.019463520333));
#18688=CARTESIAN_POINT('',(-0.037445936687,-0.010283943964,-0.019454625919));
#18689=CARTESIAN_POINT('',(-0.037668775198,-0.010270714068,-0.019895833342));
#18690=CARTESIAN_POINT('',(-0.037946745879,-0.010251529703,-0.019456070883));
#18691=CARTESIAN_POINT('',(-0.0374588757169999,-0.010350958591,-0.019444295419));
#18692=CARTESIAN_POINT('',(-0.037686938258,-0.01035590701,-0.019887098991));
#18693=CARTESIAN_POINT('',(-0.03795527555,-0.010288532493,-0.019451385246));
#18694=CARTESIAN_POINT('',(-0.037464908394,-0.010384139251,-0.019438369006));
#18695=CARTESIAN_POINT('',(-0.037695467929,-0.010398310834,-0.019881635422));
#18696=CARTESIAN_POINT('',(-0.037995201404,-0.0104727007,-0.019423189771));
#18697=CARTESIAN_POINT('',(-0.037493219634,-0.010549838583,-0.019404818528));
#18698=CARTESIAN_POINT('',(-0.037735393783,-0.010609372239,-0.01984887779));
#18699=CARTESIAN_POINT('',(-0.03801852767,-0.010617356474,-0.019385538099));
#18700=CARTESIAN_POINT('',(-0.037508976952,-0.010676036879,-0.019366609516));
#18701=CARTESIAN_POINT('',(-0.037758720049,-0.010775187757,-0.01980544701));
#18702=CARTESIAN_POINT('',(-0.038040144091,-0.010830087113,-0.019305249844));
#18703=CARTESIAN_POINT('',(-0.037523624808,-0.010861368197,-0.019291823728));
#18704=CARTESIAN_POINT('',(-0.03778033647,-0.011019102134,-0.019713124546));
#18705=CARTESIAN_POINT('',(-0.038045091154,-0.010900659463,-0.01927424932));
#18706=CARTESIAN_POINT('',(-0.037526947936,-0.010922751921,-0.019263695619));
#18707=CARTESIAN_POINT('',(-0.037785283533,-0.011100031176,-0.01967751236));
#18708=CARTESIAN_POINT('',(-0.038050108278,-0.011036551943,-0.019205674484));
#18709=CARTESIAN_POINT('',(-0.037530327064,-0.011041355675,-0.019202654737));
#18710=CARTESIAN_POINT('',(-0.037790300657,-0.011255891492,-0.01959879628));
#18711=CARTESIAN_POINT('',(-0.038050243047,-0.011102269591,-0.019167998017));
#18712=CARTESIAN_POINT('',(-0.037530417095,-0.011098746343,-0.01916971836));
#18713=CARTESIAN_POINT('',(-0.037790435426,-0.011331278423,-0.019555574534));
#18714=CARTESIAN_POINT('',(-0.038045857381,-0.011229333988,-0.019085998172));
#18715=CARTESIAN_POINT('',(-0.037527464034,-0.011210579299,-0.019098653928));
#18716=CARTESIAN_POINT('',(-0.03778604976,-0.011477065914,-0.019461552266));
#18717=CARTESIAN_POINT('',(-0.038041336883,-0.011290680666,-0.019041674687));
#18718=CARTESIAN_POINT('',(-0.037524429559,-0.011264860653,-0.019060637682));
#18719=CARTESIAN_POINT('',(-0.037781529262,-0.011547466388,-0.019410751623));
#18720=CARTESIAN_POINT('',(-0.038027559938,-0.011408940944,-0.018946286813));
#18721=CARTESIAN_POINT('',(-0.037515080889,-0.011370775304,-0.018978926179));
#18722=CARTESIAN_POINT('',(-0.037767752317,-0.011683211699,-0.019301463566));
#18723=CARTESIAN_POINT('',(-0.038018235775,-0.011465994202,-0.018895009009));
#18724=CARTESIAN_POINT('',(-0.037508746133,-0.011422411288,-0.018935184096));
#18725=CARTESIAN_POINT('',(-0.037758428154,-0.011748717175,-0.019242731993));
#18726=CARTESIAN_POINT('',(-0.037983863425,-0.011626135813,-0.018735057854));
#18727=CARTESIAN_POINT('',(-0.037485152239,-0.011569149469,-0.018798617961));
#18728=CARTESIAN_POINT('',(-0.037724055805,-0.011932636702,-0.01905958005));
#18729=CARTESIAN_POINT('',(-0.03795238138,-0.011719875549,-0.018619223276));
#18730=CARTESIAN_POINT('',(-0.037463427014,-0.011658126499,-0.018699531784));
#18731=CARTESIAN_POINT('',(-0.037692573758,-0.012040369285,-0.018927005758));
#18732=CARTESIAN_POINT('',(-0.037902538675,-0.01182142833,-0.018463435089));
#18733=CARTESIAN_POINT('',(-0.037427207905,-0.011759803085,-0.018561524169));
#18734=CARTESIAN_POINT('',(-0.037642731053,-0.012157190014,-0.018748770563));
#18735=CARTESIAN_POINT('',(-0.0378920119,-0.011840990207,-0.018431644379));
#18736=CARTESIAN_POINT('',(-0.037419583631,-0.011779451696,-0.018533495969));
#18737=CARTESIAN_POINT('',(-0.037632204279,-0.012179699312,-0.018712402395));
#18738=CARTESIAN_POINT('',(-0.037870126119,-0.011878130234,-0.018367644958));
#18739=CARTESIAN_POINT('',(-0.037403612981,-0.011817220648,-0.018476768706));
#18740=CARTESIAN_POINT('',(-0.037610318498,-0.012222448524,-0.018639193956));
#18741=CARTESIAN_POINT('',(-0.037858748966,-0.011895754219,-0.018335374301));
#18742=CARTESIAN_POINT('',(-0.037395262434,-0.011835384713,-0.018448035028));
#18743=CARTESIAN_POINT('',(-0.037598941345,-0.012242741131,-0.018602282796));
#18744=CARTESIAN_POINT('',(-0.037823348421,-0.011945883489,-0.018237779846));
#18745=CARTESIAN_POINT('',(-0.037369172913,-0.011887572482,-0.018360946022));
#18746=CARTESIAN_POINT('',(-0.0375635408,-0.012300482293,-0.018490662919));
#18747=CARTESIAN_POINT('',(-0.037798059306,-0.011975653238,-0.018171675593));
#18748=CARTESIAN_POINT('',(-0.037350277137,-0.011919662954,-0.018301226609));
#18749=CARTESIAN_POINT('',(-0.037538251684,-0.012334802364,-0.01841507009));
#18750=CARTESIAN_POINT('',(-0.037744193093,-0.012028207852,-0.018037491178));
#18751=CARTESIAN_POINT('',(-0.037309379895,-0.011978153369,-0.018178502137));
#18752=CARTESIAN_POINT('',(-0.037484385472,-0.012395455267,-0.018261646389));
#18753=CARTESIAN_POINT('',(-0.037715615604,-0.012050991651,-0.017969410681));
#18754=CARTESIAN_POINT('',(-0.037287455068,-0.012004589867,-0.018115639729));
#18755=CARTESIAN_POINT('',(-0.037455807983,-0.012421786873,-0.018183815137));
#18756=CARTESIAN_POINT('',(-0.037670271841,-0.012079999243,-0.017865841447));
#18757=CARTESIAN_POINT('',(-0.037251993154,-0.012039949422,-0.018018443323));
#18758=CARTESIAN_POINT('',(-0.03741046422,-0.012455375111,-0.018065427979));
#18759=CARTESIAN_POINT('',(-0.037654725402,-0.012088808864,-0.017831040227));
#18760=CARTESIAN_POINT('',(-0.037239813053,-0.012050965676,-0.017985742729));
#18761=CARTESIAN_POINT('',(-0.037394917781,-0.012465588496,-0.018025650255));
#18762=CARTESIAN_POINT('',(-0.037623119912,-0.012104555629,-0.017761655615));
#18763=CARTESIAN_POINT('',(-0.037214887215,-0.012071290256,-0.017920179797));
#18764=CARTESIAN_POINT('',(-0.037363312291,-0.012483871576,-0.017946348883));
#18765=CARTESIAN_POINT('',(-0.037607024828,-0.012111518654,-0.017726988147));
#18766=CARTESIAN_POINT('',(-0.037202122033,-0.012080639592,-0.017887250964));
#18767=CARTESIAN_POINT('',(-0.037347217206,-0.012491971204,-0.017906729123));
#18768=CARTESIAN_POINT('',(-0.037525118351,-0.012141933343,-0.01755377779));
#18769=CARTESIAN_POINT('',(-0.037137549676,-0.012122798947,-0.017723852461));
#18770=CARTESIAN_POINT('',(-0.03726531073,-0.012527433166,-0.017708787883));
#18771=CARTESIAN_POINT('',(-0.037455051799,-0.012152306816,-0.017415613082));
#18772=CARTESIAN_POINT('',(-0.037080651573,-0.012144510573,-0.017589399015));
#18773=CARTESIAN_POINT('',(-0.037195244178,-0.012539827994,-0.017550935495));
#18774=CARTESIAN_POINT('',(-0.037343235527,-0.012148213531,-0.01720905843));
#18775=CARTESIAN_POINT('',(-0.036986748025,-0.012157127057,-0.017382507888));
#18776=CARTESIAN_POINT('',(-0.037083427906,-0.012535928527,-0.017315007876));
#18777=CARTESIAN_POINT('',(-0.03730475018,-0.012143504287,-0.01714019209));
#18778=CARTESIAN_POINT('',(-0.03695443279,-0.012158057656,-0.017313516891));
#18779=CARTESIAN_POINT('',(-0.037044942559,-0.012530801323,-0.017236358679));
#18780=CARTESIAN_POINT('',(-0.03722687049,-0.012127824497,-0.017005091856));
#18781=CARTESIAN_POINT('',(-0.036888415857,-0.012153246959,-0.017177025003));
#18782=CARTESIAN_POINT('',(-0.036967062869,-0.012513372076,-0.01708208731));
#18783=CARTESIAN_POINT('',(-0.037187320072,-0.012116862461,-0.016938559819));
#18784=CARTESIAN_POINT('',(-0.036854627768,-0.012147650578,-0.017109245591));
#18785=CARTESIAN_POINT('',(-0.036927512451,-0.012501080898,-0.017006124553));
#18786=CARTESIAN_POINT('',(-0.03706685504,-0.012075016713,-0.016741914748));
#18787=CARTESIAN_POINT('',(-0.036751742399,-0.012121386905,-0.016909119768));
#18788=CARTESIAN_POINT('',(-0.036807047419,-0.012453943078,-0.016781637365));
#18789=CARTESIAN_POINT('',(-0.03698413842,-0.012035245207,-0.016614730411));
#18790=CARTESIAN_POINT('',(-0.036679594089,-0.012091526511,-0.016776553485));
#18791=CARTESIAN_POINT('',(-0.036724330798,-0.01240891457,-0.016636488213));
#18792=CARTESIAN_POINT('',(-0.036813690053,-0.011932224721,-0.016368219888));
#18793=CARTESIAN_POINT('',(-0.036528822624,-0.012005165032,-0.016516491866));
#18794=CARTESIAN_POINT('',(-0.036553882432,-0.012291955726,-0.016355253995));
#18795=CARTESIAN_POINT('',(-0.03672806298,-0.011870246798,-0.016251941319));
#18796=CARTESIAN_POINT('',(-0.036452219097,-0.011950532581,-0.016391983009));
#18797=CARTESIAN_POINT('',(-0.036468255359,-0.012221468356,-0.016222645908));
#18798=CARTESIAN_POINT('',(-0.036556082968,-0.011726690875,-0.01603279824));
#18799=CARTESIAN_POINT('',(-0.036296957641,-0.01181811194,-0.016155409747));
#18800=CARTESIAN_POINT('',(-0.036296275347,-0.012057999557,-0.015972835599));
#18801=CARTESIAN_POINT('',(-0.036469700557,-0.011645092454,-0.01592989329));
#18802=CARTESIAN_POINT('',(-0.036218299035,-0.011740996991,-0.016042857153));
#18803=CARTESIAN_POINT('',(-0.03620989256,-0.011964994531,-0.015855586742));
#18804=CARTESIAN_POINT('',(-0.0363829297,-0.011553263876,-0.015833944478));
#18805=CARTESIAN_POINT('',(-0.036137554584,-0.011650536133,-0.015935581221));
#18806=CARTESIAN_POINT('',(-0.036123122079,-0.011860244082,-0.015746332321));
#18807=CARTESIAN_POINT('',(-0.0387712812904532,-1.29150202956894E-11,-1.90102621199567E-11));
#18809=MECHANICAL_DESIGN_GEOMETRIC_PRESENTATION_REPRESENTATION('',(#8179),#18810);
#18810=(
GEOMETRIC_REPRESENTATION_CONTEXT(3)
GLOBAL_UNCERTAINTY_ASSIGNED_CONTEXT((#18817))
GLOBAL_UNIT_ASSIGNED_CONTEXT((#18826,#18825,#18824))
REPRESENTATION_CONTEXT('MAS-697','TOP_LEVEL_ASSEMBLY_PART')
);
#18816=(
GEOMETRIC_REPRESENTATION_CONTEXT(3)
GLOBAL_UNCERTAINTY_ASSIGNED_CONTEXT((#18823))
GLOBAL_UNIT_ASSIGNED_CONTEXT((#18826,#18825,#18824))
REPRESENTATION_CONTEXT('HubBody__ DE       35','COMPONENT_PART')
);
#18817=UNCERTAINTY_MEASURE_WITH_UNIT(LENGTH_MEASURE(1.E-8),#18826,
'DISTANCE_ACCURACY_VALUE','Maximum Tolerance applied to model');
#18823=UNCERTAINTY_MEASURE_WITH_UNIT(LENGTH_MEASURE(2.23351470508855E-5),
#18826,'DISTANCE_ACCURACY_VALUE','Maximum Tolerance applied to model');
#18824=(
NAMED_UNIT(*)
SI_UNIT($,.STERADIAN.)
SOLID_ANGLE_UNIT()
);
#18825=(
NAMED_UNIT(*)
PLANE_ANGLE_UNIT()
SI_UNIT($,.RADIAN.)
);
#18826=(
LENGTH_UNIT()
NAMED_UNIT(*)
SI_UNIT($,.METRE.)
);
#18838=PRODUCT_DEFINITION_SHAPE('','',#18846);
#18846=PRODUCT_DEFINITION('','',#18860,#18853);
#18853=PRODUCT_DEFINITION_CONTEXT('',#18890,'design');
#18860=PRODUCT_DEFINITION_FORMATION_WITH_SPECIFIED_SOURCE('','',#18874,
 .NOT_KNOWN.);
#18874=PRODUCT('HubBody__ DE       35','HubBody__ DE       35',
'HubBody__ DE       35',(#18888));
#18888=PRODUCT_CONTEXT('',#18890,'mechanical');
#18890=APPLICATION_CONTEXT('managed model based 3d engineering');
ENDSEC;
END-ISO-10303-21;
